ISO-10303-21;
HEADER;
/* Generated by software containing ST-Developer
 * from STEP Tools, Inc. (www.steptools.com) 
 */

FILE_DESCRIPTION(
/* description */ ('Independent compact industrial fixture table, bolted aluminum worktop
 on connected adjustable support base. Whole-mm nominal dimensions. No
 load rating assigned.'),
/* implementation_level */ '2;1');

FILE_NAME(
/* name */ 'Socket head cap screw M10x20.step',
/* time_stamp */ '2026-11-07T17:47:58-08:00',
/* author */ (''),
/* organization */ (''),
/* preprocessor_version */ 'ST-DEVELOPER v20.2',
/* originating_system */ 'Autodesk Translation Framework v15.17.0.0',
/* authorisation */ '');

FILE_SCHEMA (('AUTOMOTIVE_DESIGN { 1 0 10303 214 3 1 1 }'));
ENDSEC;

DATA;
#10=MECHANICAL_DESIGN_GEOMETRIC_PRESENTATION_REPRESENTATION('',(#2257),#97475);
#331=CONICAL_SURFACE('',#22676,4.5,0.785398163397448);
#348=B_SPLINE_SURFACE_WITH_KNOTS('',3,3,((#55084,#55085,#55086,#55087,#55088,
#55089,#55090,#55091,#55092,#55093,#55094,#55095,#55096,#55097,#55098,#55099,
#55100,#55101,#55102,#55103,#55104,#55105,#55106,#55107,#55108,#55109,#55110,
#55111,#55112,#55113,#55114,#55115,#55116,#55117,#55118,#55119,#55120,#55121,
#55122,#55123,#55124,#55125,#55126,#55127,#55128,#55129,#55130,#55131,#55132,
#55133,#55134,#55135,#55136,#55137,#55138,#55139,#55140,#55141,#55142,#55143,
#55144,#55145,#55146,#55147,#55148,#55149,#55150,#55151,#55152,#55153,#55154,
#55155,#55156,#55157,#55158,#55159,#55160,#55161,#55162,#55163,#55164,#55165,
#55166,#55167,#55168,#55169,#55170,#55171,#55172,#55173,#55174,#55175,#55176,
#55177,#55178,#55179,#55180,#55181,#55182,#55183,#55184,#55185,#55186,#55187,
#55188,#55189,#55190,#55191,#55192,#55193,#55194,#55195,#55196,#55197,#55198,
#55199,#55200,#55201,#55202,#55203,#55204,#55205,#55206,#55207,#55208,#55209,
#55210,#55211,#55212),(#55213,#55214,#55215,#55216,#55217,#55218,#55219,
#55220,#55221,#55222,#55223,#55224,#55225,#55226,#55227,#55228,#55229,#55230,
#55231,#55232,#55233,#55234,#55235,#55236,#55237,#55238,#55239,#55240,#55241,
#55242,#55243,#55244,#55245,#55246,#55247,#55248,#55249,#55250,#55251,#55252,
#55253,#55254,#55255,#55256,#55257,#55258,#55259,#55260,#55261,#55262,#55263,
#55264,#55265,#55266,#55267,#55268,#55269,#55270,#55271,#55272,#55273,#55274,
#55275,#55276,#55277,#55278,#55279,#55280,#55281,#55282,#55283,#55284,#55285,
#55286,#55287,#55288,#55289,#55290,#55291,#55292,#55293,#55294,#55295,#55296,
#55297,#55298,#55299,#55300,#55301,#55302,#55303,#55304,#55305,#55306,#55307,
#55308,#55309,#55310,#55311,#55312,#55313,#55314,#55315,#55316,#55317,#55318,
#55319,#55320,#55321,#55322,#55323,#55324,#55325,#55326,#55327,#55328,#55329,
#55330,#55331,#55332,#55333,#55334,#55335,#55336,#55337,#55338,#55339,#55340,
#55341),(#55342,#55343,#55344,#55345,#55346,#55347,#55348,#55349,#55350,
#55351,#55352,#55353,#55354,#55355,#55356,#55357,#55358,#55359,#55360,#55361,
#55362,#55363,#55364,#55365,#55366,#55367,#55368,#55369,#55370,#55371,#55372,
#55373,#55374,#55375,#55376,#55377,#55378,#55379,#55380,#55381,#55382,#55383,
#55384,#55385,#55386,#55387,#55388,#55389,#55390,#55391,#55392,#55393,#55394,
#55395,#55396,#55397,#55398,#55399,#55400,#55401,#55402,#55403,#55404,#55405,
#55406,#55407,#55408,#55409,#55410,#55411,#55412,#55413,#55414,#55415,#55416,
#55417,#55418,#55419,#55420,#55421,#55422,#55423,#55424,#55425,#55426,#55427,
#55428,#55429,#55430,#55431,#55432,#55433,#55434,#55435,#55436,#55437,#55438,
#55439,#55440,#55441,#55442,#55443,#55444,#55445,#55446,#55447,#55448,#55449,
#55450,#55451,#55452,#55453,#55454,#55455,#55456,#55457,#55458,#55459,#55460,
#55461,#55462,#55463,#55464,#55465,#55466,#55467,#55468,#55469,#55470),
(#55471,#55472,#55473,#55474,#55475,#55476,#55477,#55478,#55479,#55480,
#55481,#55482,#55483,#55484,#55485,#55486,#55487,#55488,#55489,#55490,#55491,
#55492,#55493,#55494,#55495,#55496,#55497,#55498,#55499,#55500,#55501,#55502,
#55503,#55504,#55505,#55506,#55507,#55508,#55509,#55510,#55511,#55512,#55513,
#55514,#55515,#55516,#55517,#55518,#55519,#55520,#55521,#55522,#55523,#55524,
#55525,#55526,#55527,#55528,#55529,#55530,#55531,#55532,#55533,#55534,#55535,
#55536,#55537,#55538,#55539,#55540,#55541,#55542,#55543,#55544,#55545,#55546,
#55547,#55548,#55549,#55550,#55551,#55552,#55553,#55554,#55555,#55556,#55557,
#55558,#55559,#55560,#55561,#55562,#55563,#55564,#55565,#55566,#55567,#55568,
#55569,#55570,#55571,#55572,#55573,#55574,#55575,#55576,#55577,#55578,#55579,
#55580,#55581,#55582,#55583,#55584,#55585,#55586,#55587,#55588,#55589,#55590,
#55591,#55592,#55593,#55594,#55595,#55596,#55597,#55598,#55599)),
 .UNSPECIFIED.,.F.,.F.,.F.,(4,4),(4,1,1,1,1,1,1,1,1,1,1,1,1,1,1,1,1,1,1,
1,1,1,1,1,1,1,1,1,1,1,1,1,1,1,1,1,1,1,1,1,1,1,1,1,1,1,1,1,1,1,1,1,1,1,1,
1,1,1,1,1,1,1,1,1,1,1,1,1,1,1,1,1,1,1,1,1,1,1,1,1,1,1,1,1,1,1,1,1,1,1,1,
1,1,1,1,1,1,1,1,1,1,1,1,1,1,1,1,1,1,1,1,1,1,1,1,1,1,1,1,1,1,1,1,1,1,1,4),
(0.,0.0658179306876173),(11.6150328478182,12.1123165623719,12.6096002769257,
13.6041677060331,14.5987351351405,15.5933025642479,16.5878699933554,17.5824374224628,
18.5770048515702,19.5715722806776,20.5661397097851,21.5607071388925,22.5552745679999,
23.5498419971074,24.5444094262148,25.5389768553222,26.5335442844296,27.5281117135371,
28.5226791426445,29.5172465717519,30.5118140008593,31.5063814299668,32.5009488590742,
33.4955162881816,34.490083717289,35.4846511463965,36.4792185755039,37.4737860046113,
38.4683534337187,39.4629208628262,40.4574882919336,41.452055721041,42.4466231501485,
43.4411905792559,44.4357580083633,45.4303254374707,46.4248928665782,47.4194602956856,
48.414027724793,49.4085951539004,50.4031625830079,51.3977300121153,52.3922974412227,
53.3868648703302,54.3814322994376,55.375999728545,56.3705671576524,57.3651345867599,
58.3597020158673,59.3542694449747,60.3488368740821,61.3434043031896,62.337971732297,
63.3325391614044,64.3271065905118,65.3216740196193,66.3162414487267,67.3108088778341,
68.3053763069416,69.299943736049,70.2945111651564,71.2890785942638,72.2836460233713,
73.2782134524787,74.2727808815861,75.2673483106935,76.261915739801,77.2564831689084,
78.2510505980158,79.2456180271232,80.2401854562307,81.2347528853381,82.2293203144455,
83.223887743553,84.2184551726604,85.2130226017678,86.2075900308752,87.2021574599827,
88.1967248890901,89.1912923181975,90.1858597473049,91.1804271764124,92.1749946055198,
93.1695620346272,94.1641294637347,95.1586968928421,96.1532643219495,97.1478317510569,
98.1423991801644,99.1369666092718,100.131534038379,101.126101467487,102.120668896594,
103.115236325701,104.109803754809,105.104371183916,106.098938613024,107.093506042131,
108.088073471239,109.082640900346,110.077208329453,111.071775758561,112.066343187668,
113.060910616776,114.055478045883,115.050045474991,116.044612904098,117.039180333205,
118.033747762313,119.02831519142,120.022882620528,121.017450049635,122.012017478743,
123.00658490785,124.001152336957,124.995719766065,125.990287195172,126.98485462428,
127.979422053387,128.973989482495,129.968556911602,130.963124340709,131.957691769817,
132.952259198924,133.946826628032,134.444110342585,134.941394057139),
 .UNSPECIFIED.);
#349=B_SPLINE_SURFACE_WITH_KNOTS('',3,3,((#55744,#55745,#55746,#55747,#55748,
#55749,#55750,#55751,#55752,#55753,#55754,#55755,#55756,#55757,#55758,#55759,
#55760,#55761,#55762,#55763,#55764,#55765,#55766,#55767,#55768,#55769,#55770,
#55771,#55772,#55773,#55774,#55775,#55776,#55777,#55778,#55779,#55780,#55781,
#55782,#55783,#55784,#55785,#55786,#55787,#55788,#55789,#55790,#55791,#55792,
#55793,#55794,#55795,#55796,#55797,#55798,#55799,#55800,#55801,#55802,#55803,
#55804,#55805,#55806,#55807,#55808,#55809,#55810,#55811,#55812,#55813,#55814,
#55815,#55816,#55817,#55818,#55819,#55820,#55821,#55822,#55823,#55824,#55825,
#55826,#55827,#55828,#55829,#55830,#55831,#55832,#55833,#55834,#55835,#55836,
#55837,#55838,#55839,#55840,#55841,#55842,#55843,#55844,#55845,#55846,#55847,
#55848,#55849,#55850,#55851,#55852,#55853,#55854,#55855,#55856,#55857,#55858,
#55859,#55860,#55861,#55862,#55863,#55864,#55865,#55866,#55867,#55868,#55869,
#55870,#55871,#55872,#55873,#55874),(#55875,#55876,#55877,#55878,#55879,
#55880,#55881,#55882,#55883,#55884,#55885,#55886,#55887,#55888,#55889,#55890,
#55891,#55892,#55893,#55894,#55895,#55896,#55897,#55898,#55899,#55900,#55901,
#55902,#55903,#55904,#55905,#55906,#55907,#55908,#55909,#55910,#55911,#55912,
#55913,#55914,#55915,#55916,#55917,#55918,#55919,#55920,#55921,#55922,#55923,
#55924,#55925,#55926,#55927,#55928,#55929,#55930,#55931,#55932,#55933,#55934,
#55935,#55936,#55937,#55938,#55939,#55940,#55941,#55942,#55943,#55944,#55945,
#55946,#55947,#55948,#55949,#55950,#55951,#55952,#55953,#55954,#55955,#55956,
#55957,#55958,#55959,#55960,#55961,#55962,#55963,#55964,#55965,#55966,#55967,
#55968,#55969,#55970,#55971,#55972,#55973,#55974,#55975,#55976,#55977,#55978,
#55979,#55980,#55981,#55982,#55983,#55984,#55985,#55986,#55987,#55988,#55989,
#55990,#55991,#55992,#55993,#55994,#55995,#55996,#55997,#55998,#55999,#56000,
#56001,#56002,#56003,#56004,#56005),(#56006,#56007,#56008,#56009,#56010,
#56011,#56012,#56013,#56014,#56015,#56016,#56017,#56018,#56019,#56020,#56021,
#56022,#56023,#56024,#56025,#56026,#56027,#56028,#56029,#56030,#56031,#56032,
#56033,#56034,#56035,#56036,#56037,#56038,#56039,#56040,#56041,#56042,#56043,
#56044,#56045,#56046,#56047,#56048,#56049,#56050,#56051,#56052,#56053,#56054,
#56055,#56056,#56057,#56058,#56059,#56060,#56061,#56062,#56063,#56064,#56065,
#56066,#56067,#56068,#56069,#56070,#56071,#56072,#56073,#56074,#56075,#56076,
#56077,#56078,#56079,#56080,#56081,#56082,#56083,#56084,#56085,#56086,#56087,
#56088,#56089,#56090,#56091,#56092,#56093,#56094,#56095,#56096,#56097,#56098,
#56099,#56100,#56101,#56102,#56103,#56104,#56105,#56106,#56107,#56108,#56109,
#56110,#56111,#56112,#56113,#56114,#56115,#56116,#56117,#56118,#56119,#56120,
#56121,#56122,#56123,#56124,#56125,#56126,#56127,#56128,#56129,#56130,#56131,
#56132,#56133,#56134,#56135,#56136),(#56137,#56138,#56139,#56140,#56141,
#56142,#56143,#56144,#56145,#56146,#56147,#56148,#56149,#56150,#56151,#56152,
#56153,#56154,#56155,#56156,#56157,#56158,#56159,#56160,#56161,#56162,#56163,
#56164,#56165,#56166,#56167,#56168,#56169,#56170,#56171,#56172,#56173,#56174,
#56175,#56176,#56177,#56178,#56179,#56180,#56181,#56182,#56183,#56184,#56185,
#56186,#56187,#56188,#56189,#56190,#56191,#56192,#56193,#56194,#56195,#56196,
#56197,#56198,#56199,#56200,#56201,#56202,#56203,#56204,#56205,#56206,#56207,
#56208,#56209,#56210,#56211,#56212,#56213,#56214,#56215,#56216,#56217,#56218,
#56219,#56220,#56221,#56222,#56223,#56224,#56225,#56226,#56227,#56228,#56229,
#56230,#56231,#56232,#56233,#56234,#56235,#56236,#56237,#56238,#56239,#56240,
#56241,#56242,#56243,#56244,#56245,#56246,#56247,#56248,#56249,#56250,#56251,
#56252,#56253,#56254,#56255,#56256,#56257,#56258,#56259,#56260,#56261,#56262,
#56263,#56264,#56265,#56266,#56267)),.UNSPECIFIED.,.F.,.F.,.F.,(4,4),(4,
1,1,1,1,1,1,1,1,1,1,1,1,1,1,1,1,1,1,1,1,1,1,1,1,1,1,1,1,1,1,1,1,1,1,1,1,
1,1,1,1,1,1,1,1,1,1,1,1,1,1,1,1,1,1,1,1,1,1,1,1,1,1,1,1,1,1,1,1,1,1,1,1,
1,1,1,1,1,1,1,1,1,1,1,1,1,1,1,1,1,1,1,1,1,1,1,1,1,1,1,1,1,1,1,1,1,1,1,1,
1,1,1,1,1,1,1,1,1,1,1,1,1,1,1,1,1,1,1,4),(0.,0.0658179306876173),(8.30838445208313,
8.80598005718054,9.30357566227795,10.2987668724728,11.2939580826676,12.2891492928624,
13.2843405030573,14.2795317132521,15.2747229234469,16.2699141336417,17.2651053438366,
18.2602965540314,19.2554877642262,20.250678974421,21.2458701846159,22.2410613948107,
23.2362526050055,24.2314438152003,25.2266350253952,26.22182623559,27.2170174457848,
28.2122086559796,29.2073998661744,30.2025910763693,31.1977822865641,32.1929734967589,
33.1881647069537,34.1833559171486,35.1785471273434,36.1737383375382,37.168929547733,
38.1641207579279,39.1593119681227,40.1545031783175,41.1496943885123,42.1448855987072,
43.140076808902,44.1352680190968,45.1304592292916,46.1256504394865,47.1208416496813,
48.1160328598761,49.1112240700709,50.1064152802658,51.1016064904606,52.0967977006554,
53.0919889108502,54.0871801210451,55.0823713312399,56.0775625414347,57.0727537516295,
58.0679449618244,59.0631361720192,60.058327382214,61.0535185924088,62.0487098026037,
63.0439010127985,64.0390922229933,65.0342834331881,66.029474643383,67.0246658535778,
68.0198570637726,69.0150482739674,70.0102394841623,71.0054306943571,72.0006219045519,
72.9958131147467,73.9910043249416,74.9861955351364,75.9813867453312,76.976577955526,
77.9717691657209,78.9669603759157,79.9621515861105,80.9573427963053,81.9525340065002,
82.947725216695,83.9429164268898,84.9381076370846,85.9332988472795,86.9284900574743,
87.9236812676691,88.9188724778639,89.9140636880588,90.9092548982536,91.9044461084484,
92.8996373186432,93.8948285288381,94.8900197390329,95.8852109492277,96.8804021594225,
97.8755933696174,98.8707845798122,99.865975790007,100.861167000202,101.856358210397,
102.851549420591,103.846740630786,104.841931840981,105.837123051176,106.832314261371,
107.827505471566,108.82269668176,109.817887891955,110.81307910215,111.808270312345,
112.80346152254,113.798652732735,114.793843942929,115.789035153124,116.784226363319,
117.779417573514,118.774608783709,119.769799993904,120.764991204098,121.760182414293,
122.755373624488,123.750564834683,124.745756044878,125.740947255072,126.736138465267,
127.731329675462,128.726520885657,129.721712095852,130.716903306047,131.712094516241,
132.707285726436,133.204881331534,133.702476936631),.UNSPECIFIED.);
#917=B_SPLINE_CURVE_WITH_KNOTS('',3,(#53336,#53337,#53338,#53339,#53340,
#53341,#53342,#53343,#53344,#53345),.UNSPECIFIED.,.F.,.F.,(4,3,3,4),(-4.09293042013065,
-3.97826971642971,-2.98370228732228,-2.06773127522702),.UNSPECIFIED.);
#918=B_SPLINE_CURVE_WITH_KNOTS('',3,(#53348,#53349,#53350,#53351,#53352,
#53353,#53354,#53355,#53356,#53357),.UNSPECIFIED.,.F.,.F.,(4,3,3,4),(0.,
0.49759560509741,0.995191210194833,1.11639350868605),.UNSPECIFIED.);
#919=B_SPLINE_CURVE_WITH_KNOTS('',3,(#53362,#53363,#53364,#53365,#53366,
#53367,#53368,#53369,#53370,#53371,#53372,#53373,#53374,#53375,#53376,#53377,
#53378,#53379,#53380,#53381,#53382,#53383),.UNSPECIFIED.,.F.,.F.,(4,3,3,
3,3,3,3,4),(-10.3761157273102,-9.94567429107427,-8.95110686196684,-7.95653943285942,
-6.96197200375199,-5.96740457464456,-4.97283714553713,-4.09293042013065),
 .UNSPECIFIED.);
#920=B_SPLINE_CURVE_WITH_KNOTS('',3,(#53384,#53385,#53386,#53387,#53388,
#53389,#53390,#53391,#53392,#53393,#53394,#53395,#53396,#53397,#53398,#53399,
#53400,#53401,#53402,#53403,#53404,#53405),.UNSPECIFIED.,.F.,.F.,(4,3,3,
3,3,3,3,4),(1.11639350868605,1.99038242038966,2.98557363058448,3.9807648407793,
4.97595605097413,5.97114726116895,6.96633847136377,7.39957881586564),
 .UNSPECIFIED.);
#921=B_SPLINE_CURVE_WITH_KNOTS('',3,(#53410,#53411,#53412,#53413,#53414,
#53415,#53416,#53417,#53418,#53419,#53420,#53421,#53422,#53423,#53424,#53425,
#53426,#53427,#53428,#53429,#53430,#53431),.UNSPECIFIED.,.F.,.F.,(4,3,3,
3,3,3,3,4),(-16.6593010344898,-15.9130788657188,-14.9185114366114,-13.923944007504,
-12.9293765783965,-11.9348091492891,-10.9402417201817,-10.3761157273102),
 .UNSPECIFIED.);
#922=B_SPLINE_CURVE_WITH_KNOTS('',3,(#53432,#53433,#53434,#53435,#53436,
#53437,#53438,#53439,#53440,#53441,#53442,#53443,#53444,#53445,#53446,#53447,
#53448,#53449,#53450,#53451,#53452,#53453),.UNSPECIFIED.,.F.,.F.,(4,3,3,
3,3,3,3,4),(7.39957881586564,7.9615296815586,8.95672089175343,9.95191210194825,
10.9471033121431,11.9422945223379,12.9374857325327,13.6827641230452),
 .UNSPECIFIED.);
#923=B_SPLINE_CURVE_WITH_KNOTS('',3,(#53458,#53459,#53460,#53461,#53462,
#53463,#53464,#53465,#53466,#53467,#53468,#53469,#53470,#53471,#53472,#53473,
#53474,#53475,#53476,#53477,#53478,#53479,#53480,#53481,#53482),
 .UNSPECIFIED.,.F.,.F.,(4,3,3,3,3,3,3,3,4),(-22.9424863416694,-22.8750508694708,
-21.8804834403634,-20.885916011256,-19.8913485821485,-18.8967811530411,
-17.9022137239337,-16.9076462948263,-16.6593010344898),.UNSPECIFIED.);
#924=B_SPLINE_CURVE_WITH_KNOTS('',3,(#53483,#53484,#53485,#53486,#53487,
#53488,#53489,#53490,#53491,#53492,#53493,#53494,#53495,#53496,#53497,#53498,
#53499,#53500,#53501,#53502,#53503,#53504,#53505,#53506,#53507),
 .UNSPECIFIED.,.F.,.F.,(4,3,3,3,3,3,3,3,4),(13.6827641230452,13.9326769427276,
14.9278681529224,15.9230593631172,16.918250573312,17.9134417835069,18.9086329937017,
19.9038242038965,19.9659494302248),.UNSPECIFIED.);
#925=B_SPLINE_CURVE_WITH_KNOTS('',3,(#53512,#53513,#53514,#53515,#53516,
#53517,#53518,#53519,#53520,#53521,#53522,#53523,#53524,#53525,#53526,#53527,
#53528,#53529,#53530,#53531,#53532,#53533),.UNSPECIFIED.,.F.,.F.,(4,3,3,
3,3,3,3,4),(-29.225671648849,-28.8424554441154,-27.847888015008,-26.8533205859005,
-25.8587531567931,-24.8641857276857,-23.8696182985782,-22.9424863416694),
 .UNSPECIFIED.);
#926=B_SPLINE_CURVE_WITH_KNOTS('',3,(#53534,#53535,#53536,#53537,#53538,
#53539,#53540,#53541,#53542,#53543,#53544,#53545,#53546,#53547,#53548,#53549,
#53550,#53551,#53552,#53553,#53554,#53555),.UNSPECIFIED.,.F.,.F.,(4,3,3,
3,3,3,3,4),(19.9659494302248,20.8990154140913,21.8942066242861,22.889397834481,
23.8845890446758,24.8797802548706,25.8749714650654,26.2491347374044),
 .UNSPECIFIED.);
#927=B_SPLINE_CURVE_WITH_KNOTS('',3,(#53560,#53561,#53562,#53563,#53564,
#53565,#53566,#53567,#53568,#53569,#53570,#53571,#53572,#53573,#53574,#53575,
#53576,#53577,#53578,#53579,#53580,#53581),.UNSPECIFIED.,.F.,.F.,(4,3,3,
3,3,3,3,4),(-35.5088569560286,-34.8098600187599,-33.8152925896525,-32.8207251605451,
-31.8261577314377,-30.8315903023302,-29.8370228732228,-29.225671648849),
 .UNSPECIFIED.);
#928=B_SPLINE_CURVE_WITH_KNOTS('',3,(#53582,#53583,#53584,#53585,#53586,
#53587,#53588,#53589,#53590,#53591,#53592,#53593,#53594,#53595,#53596,#53597,
#53598,#53599,#53600,#53601,#53602,#53603),.UNSPECIFIED.,.F.,.F.,(4,3,3,
3,3,3,3,4),(26.2491347374044,26.8701626752603,27.8653538854551,28.8605450956499,
29.8557363058448,30.8509275160396,31.8461187262344,32.532320044584),
 .UNSPECIFIED.);
#929=B_SPLINE_CURVE_WITH_KNOTS('',3,(#53608,#53609,#53610,#53611,#53612,
#53613,#53614,#53615,#53616,#53617,#53618,#53619,#53620,#53621,#53622,#53623,
#53624,#53625,#53626,#53627,#53628,#53629,#53630,#53631,#53632),
 .UNSPECIFIED.,.F.,.F.,(4,3,3,3,3,3,3,3,4),(-41.7920422632082,-41.7718320225119,
-40.7772645934045,-39.7826971642971,-38.7881297351896,-37.7935623060822,
-36.7989948769748,-35.8044274478674,-35.5088569560286),.UNSPECIFIED.);
#930=B_SPLINE_CURVE_WITH_KNOTS('',3,(#53633,#53634,#53635,#53636,#53637,
#53638,#53639,#53640,#53641,#53642,#53643,#53644,#53645,#53646,#53647,#53648,
#53649,#53650,#53651,#53652,#53653,#53654,#53655,#53656,#53657),
 .UNSPECIFIED.,.F.,.F.,(4,3,3,3,3,3,3,3,4),(32.532320044584,32.8413099364292,
33.8365011466241,34.8316923568189,35.8268835670137,36.8220747772085,37.8172659874034,
38.8124571975982,38.8155053517636),.UNSPECIFIED.);
#931=B_SPLINE_CURVE_WITH_KNOTS('',3,(#53662,#53663,#53664,#53665,#53666,
#53667,#53668,#53669,#53670,#53671,#53672,#53673,#53674,#53675,#53676,#53677,
#53678,#53679,#53680,#53681,#53682,#53683),.UNSPECIFIED.,.F.,.F.,(4,3,3,
3,3,3,3,4),(-48.0752275703878,-47.7392365971565,-46.7446691680491,-45.7501017389416,
-44.7555343098342,-43.7609668807268,-42.7663994516193,-41.7920422632082),
 .UNSPECIFIED.);
#932=B_SPLINE_CURVE_WITH_KNOTS('',3,(#53684,#53685,#53686,#53687,#53688,
#53689,#53690,#53691,#53692,#53693,#53694,#53695,#53696,#53697,#53698,#53699,
#53700,#53701,#53702,#53703,#53704,#53705),.UNSPECIFIED.,.F.,.F.,(4,3,3,
3,3,3,3,4),(38.8155053517636,39.807648407793,40.8028396179878,41.7980308281826,
42.7932220383775,43.7884132485723,44.7836044587671,45.0986906589432),
 .UNSPECIFIED.);
#933=B_SPLINE_CURVE_WITH_KNOTS('',3,(#53710,#53711,#53712,#53713,#53714,
#53715,#53716,#53717,#53718,#53719,#53720,#53721,#53722,#53723,#53724,#53725,
#53726,#53727,#53728,#53729,#53730,#53731),.UNSPECIFIED.,.F.,.F.,(4,3,3,
3,3,3,3,4),(-54.3584128775674,-53.7066411718011,-52.7120737426936,-51.7175063135862,
-50.7229388844788,-49.7283714553713,-48.7338040262639,-48.0752275703878),
 .UNSPECIFIED.);
#934=B_SPLINE_CURVE_WITH_KNOTS('',3,(#53732,#53733,#53734,#53735,#53736,
#53737,#53738,#53739,#53740,#53741,#53742,#53743,#53744,#53745,#53746,#53747,
#53748,#53749,#53750,#53751,#53752,#53753),.UNSPECIFIED.,.F.,.F.,(4,3,3,
3,3,3,3,4),(45.0986906589432,45.7787956689619,46.7739868791568,47.7691780893516,
48.7643692995464,49.7595605097412,50.7547517199361,51.3818759661228),
 .UNSPECIFIED.);
#935=B_SPLINE_CURVE_WITH_KNOTS('',3,(#53758,#53759,#53760,#53761,#53762,
#53763,#53764,#53765,#53766,#53767,#53768,#53769,#53770,#53771,#53772,#53773,
#53774,#53775,#53776,#53777,#53778,#53779),.UNSPECIFIED.,.F.,.F.,(4,3,3,
3,3,3,3,4),(-60.641598184747,-59.6740457464456,-58.6794783173382,-57.6849108882308,
-56.6903434591233,-55.6957760300159,-54.7012086009085,-54.3584128775674),
 .UNSPECIFIED.);
#936=B_SPLINE_CURVE_WITH_KNOTS('',3,(#53780,#53781,#53782,#53783,#53784,
#53785,#53786,#53787,#53788,#53789,#53790,#53791,#53792,#53793,#53794,#53795,
#53796,#53797,#53798,#53799,#53800,#53801),.UNSPECIFIED.,.F.,.F.,(4,3,3,
3,3,3,3,4),(51.3818759661228,51.7499429301309,52.7451341403257,53.7403253505205,
54.7355165607154,55.7307077709102,56.725898981105,57.6650612733024),
 .UNSPECIFIED.);
#937=B_SPLINE_CURVE_WITH_KNOTS('',3,(#53806,#53807,#53808,#53809,#53810,
#53811,#53812,#53813,#53814,#53815,#53816,#53817,#53818,#53819,#53820,#53821,
#53822,#53823,#53824,#53825,#53826,#53827,#53828,#53829,#53830),
 .UNSPECIFIED.,.F.,.F.,(4,3,3,3,3,3,3,3,4),(-66.9247834919265,-66.6360177501976,
-65.6414503210902,-64.6468828919827,-63.6523154628753,-62.6577480337679,
-61.6631806046605,-60.668613175553,-60.641598184747),.UNSPECIFIED.);
#938=B_SPLINE_CURVE_WITH_KNOTS('',3,(#53831,#53832,#53833,#53834,#53835,
#53836,#53837,#53838,#53839,#53840,#53841,#53842,#53843,#53844,#53845,#53846,
#53847,#53848,#53849,#53850,#53851,#53852,#53853,#53854,#53855),
 .UNSPECIFIED.,.F.,.F.,(4,3,3,3,3,3,3,3,4),(57.6650612733024,57.7210901912998,
58.7162814014946,59.7114726116895,60.7066638218843,61.7018550320791,62.697046242274,
63.6922374524688,63.9482465804819),.UNSPECIFIED.);
#939=B_SPLINE_CURVE_WITH_KNOTS('',3,(#53860,#53861,#53862,#53863,#53864,
#53865,#53866,#53867,#53868,#53869,#53870,#53871,#53872,#53873,#53874,#53875,
#53876,#53877,#53878,#53879,#53880,#53881),.UNSPECIFIED.,.F.,.F.,(4,3,3,
3,3,3,3,4),(-73.2079687991061,-72.6034223248422,-71.6088548957347,-70.6142874666273,
-69.6197200375199,-68.6251526084124,-67.630585179305,-66.9247834919265),
 .UNSPECIFIED.);
#940=B_SPLINE_CURVE_WITH_KNOTS('',3,(#53882,#53883,#53884,#53885,#53886,
#53887,#53888,#53889,#53890,#53891,#53892,#53893,#53894,#53895,#53896,#53897,
#53898,#53899,#53900,#53901,#53902,#53903),.UNSPECIFIED.,.F.,.F.,(4,3,3,
3,3,3,3,4),(63.9482465804819,64.6874286626636,65.6826198728584,66.6778110830533,
67.6730022932481,68.6681935034429,69.6633847136378,70.2314318876615),
 .UNSPECIFIED.);
#941=B_SPLINE_CURVE_WITH_KNOTS('',3,(#53908,#53909,#53910,#53911,#53912,
#53913,#53914,#53915,#53916,#53917,#53918,#53919,#53920,#53921,#53922,#53923,
#53924,#53925,#53926,#53927,#53928,#53929),.UNSPECIFIED.,.F.,.F.,(4,3,3,
3,3,3,3,4),(-79.4911541062857,-78.5708268994867,-77.5762594703793,-76.5816920412719,
-75.5871246121644,-74.592557183057,-73.5979897539496,-73.2079687991061),
 .UNSPECIFIED.);
#942=B_SPLINE_CURVE_WITH_KNOTS('',3,(#53930,#53931,#53932,#53933,#53934,
#53935,#53936,#53937,#53938,#53939,#53940,#53941,#53942,#53943,#53944,#53945,
#53946,#53947,#53948,#53949,#53950,#53951),.UNSPECIFIED.,.F.,.F.,(4,3,3,
3,3,3,3,4),(70.2314318876615,70.6585759238326,71.6537671340274,72.6489583442222,
73.644149554417,74.6393407646119,75.6345319748067,76.5146171948411),
 .UNSPECIFIED.);
#943=B_SPLINE_CURVE_WITH_KNOTS('',3,(#53956,#53957,#53958,#53959,#53960,
#53961,#53962,#53963,#53964,#53965,#53966,#53967,#53968,#53969,#53970,#53971,
#53972,#53973,#53974,#53975,#53976,#53977,#53978,#53979,#53980),
 .UNSPECIFIED.,.F.,.F.,(4,3,3,3,3,3,3,3,4),(-85.7743394134653,-85.5327989032387,
-84.5382314741313,-83.5436640450238,-82.5490966159164,-81.554529186809,
-80.5599617577016,-79.5653943285942,-79.4911541062857),.UNSPECIFIED.);
#944=B_SPLINE_CURVE_WITH_KNOTS('',3,(#53981,#53982,#53983,#53984,#53985,
#53986,#53987,#53988,#53989,#53990,#53991,#53992,#53993,#53994,#53995,#53996,
#53997,#53998,#53999,#54000,#54001,#54002,#54003,#54004,#54005),
 .UNSPECIFIED.,.F.,.F.,(4,3,3,3,3,3,3,3,4),(76.5146171948411,76.6297231850015,
77.6249143951963,78.6201056053912,79.615296815586,80.6104880257808,81.6056792359756,
82.6008704461705,82.7978025020207),.UNSPECIFIED.);
#945=B_SPLINE_CURVE_WITH_KNOTS('',3,(#54010,#54011,#54012,#54013,#54014,
#54015,#54016,#54017,#54018,#54019,#54020,#54021,#54022,#54023,#54024,#54025,
#54026,#54027,#54028,#54029,#54030,#54031),.UNSPECIFIED.,.F.,.F.,(4,3,3,
3,3,3,3,4),(-92.0575247206449,-91.5002034778833,-90.5056360487758,-89.5110686196684,
-88.516501190561,-87.5219337614536,-86.5273663323461,-85.7743394134653),
 .UNSPECIFIED.);
#946=B_SPLINE_CURVE_WITH_KNOTS('',3,(#54032,#54033,#54034,#54035,#54036,
#54037,#54038,#54039,#54040,#54041,#54042,#54043,#54044,#54045,#54046,#54047,
#54048,#54049,#54050,#54051,#54052,#54053),.UNSPECIFIED.,.F.,.F.,(4,3,3,
3,3,3,3,4),(82.7978025020207,83.5960616563653,84.5912528665601,85.5864440767549,
86.5816352869498,87.5768264971446,88.5720177073394,89.0809878092003),
 .UNSPECIFIED.);
#947=B_SPLINE_CURVE_WITH_KNOTS('',3,(#54058,#54059,#54060,#54061,#54062,
#54063,#54064,#54065,#54066,#54067,#54068,#54069,#54070,#54071,#54072,#54073,
#54074,#54075,#54076,#54077,#54078,#54079),.UNSPECIFIED.,.F.,.F.,(4,3,3,
3,3,3,3,4),(-98.3407100278245,-97.4676080525278,-96.4730406234204,-95.478473194313,
-94.4839057652055,-93.4893383360981,-92.4947709069907,-92.0575247206449),
 .UNSPECIFIED.);
#948=B_SPLINE_CURVE_WITH_KNOTS('',3,(#54080,#54081,#54082,#54083,#54084,
#54085,#54086,#54087,#54088,#54089,#54090,#54091,#54092,#54093,#54094,#54095,
#54096,#54097,#54098,#54099,#54100,#54101),.UNSPECIFIED.,.F.,.F.,(4,3,3,
3,3,3,3,4),(89.0809878092003,89.5672089175342,90.5624001277291,91.5575913379239,
92.5527825481187,93.5479737583135,94.5431649685084,95.3641731163799),
 .UNSPECIFIED.);
#949=B_SPLINE_CURVE_WITH_KNOTS('',3,(#54106,#54107,#54108,#54109,#54110,
#54111,#54112,#54113,#54114,#54115,#54116,#54117,#54118,#54119,#54120,#54121,
#54122,#54123,#54124,#54125,#54126,#54127,#54128,#54129,#54130),
 .UNSPECIFIED.,.F.,.F.,(4,3,3,3,3,3,3,3,4),(-104.623895335004,-104.42958005628,
-103.435012627172,-102.440445198065,-101.445877768958,-100.45131033985,
-99.4567429107427,-98.4621754816353,-98.3407100278245),.UNSPECIFIED.);
#950=B_SPLINE_CURVE_WITH_KNOTS('',3,(#54131,#54132,#54133,#54134,#54135,
#54136,#54137,#54138,#54139,#54140,#54141,#54142,#54143,#54144,#54145,#54146,
#54147,#54148,#54149,#54150,#54151,#54152,#54153,#54154,#54155),
 .UNSPECIFIED.,.F.,.F.,(4,3,3,3,3,3,3,3,4),(95.3641731163799,95.5383561787032,
96.533547388898,97.5287385990929,98.5239298092877,99.5191210194825,100.514312229677,
101.509503439872,101.64735842356),.UNSPECIFIED.);
#951=B_SPLINE_CURVE_WITH_KNOTS('',3,(#54160,#54161,#54162,#54163,#54164,
#54165,#54166,#54167,#54168,#54169,#54170,#54171,#54172,#54173,#54174,#54175,
#54176,#54177,#54178,#54179,#54180,#54181),.UNSPECIFIED.,.F.,.F.,(4,3,3,
3,3,3,3,4),(-110.907080642184,-110.396984630924,-109.402417201817,-108.40784977271,
-107.413282343602,-106.418714914495,-105.424147485387,-104.623895335004),
 .UNSPECIFIED.);
#952=B_SPLINE_CURVE_WITH_KNOTS('',3,(#54182,#54183,#54184,#54185,#54186,
#54187,#54188,#54189,#54190,#54191,#54192,#54193,#54194,#54195,#54196,#54197,
#54198,#54199,#54200,#54201,#54202,#54203),.UNSPECIFIED.,.F.,.F.,(4,3,3,
3,3,3,3,4),(101.64735842356,102.504694650067,103.499885860262,104.495077070457,
105.490268280651,106.485459490846,107.480650701041,107.930543730739),
 .UNSPECIFIED.);
#953=B_SPLINE_CURVE_WITH_KNOTS('',3,(#54208,#54209,#54210,#54211,#54212,
#54213,#54214,#54215,#54216,#54217,#54218,#54219,#54220,#54221,#54222,#54223,
#54224,#54225,#54226,#54227,#54228,#54229),.UNSPECIFIED.,.F.,.F.,(4,3,3,
3,3,3,3,4),(-117.190265949363,-116.364389205569,-115.369821776462,-114.375254347354,
-113.380686918247,-112.386119489139,-111.391552060032,-110.907080642184),
 .UNSPECIFIED.);
#954=B_SPLINE_CURVE_WITH_KNOTS('',3,(#54230,#54231,#54232,#54233,#54234,
#54235,#54236,#54237,#54238,#54239,#54240,#54241,#54242,#54243,#54244,#54245,
#54246,#54247,#54248,#54249,#54250,#54251),.UNSPECIFIED.,.F.,.F.,(4,3,3,
3,3,3,3,4),(107.930543730739,108.475841911236,109.471033121431,110.466224331626,
111.46141554182,112.456606752015,113.45179796221,114.213729037919),
 .UNSPECIFIED.);
#955=B_SPLINE_CURVE_WITH_KNOTS('',3,(#54257,#54258,#54259,#54260,#54261,
#54262,#54263,#54264,#54265,#54266,#54267),.UNSPECIFIED.,.F.,.F.,(4,1,1,
1,1,1,1,1,4),(128.805298797182,128.973989482495,129.968556911602,130.963124340709,
131.957691769817,132.952259198924,133.946826628032,134.444110342585,134.941394057139),
 .UNSPECIFIED.);
#956=B_SPLINE_CURVE_WITH_KNOTS('',3,(#54270,#54271,#54272,#54273,#54274,
#54275,#54276,#54277,#54278),.UNSPECIFIED.,.F.,.F.,(4,1,1,1,1,1,4),(128.805298797182,
129.721712095852,130.716903306047,131.712094516241,132.707285726436,133.204881331534,
133.702476936631),.UNSPECIFIED.);
#957=B_SPLINE_CURVE_WITH_KNOTS('',3,(#54283,#54284,#54285,#54286,#54287,
#54288,#54289,#54290,#54291,#54292),.UNSPECIFIED.,.F.,.F.,(4,1,1,1,1,1,
1,4),(122.522113490002,123.00658490785,124.001152336957,124.995719766065,
125.990287195172,126.98485462428,127.979422053387,128.805298797182),
 .UNSPECIFIED.);
#958=B_SPLINE_CURVE_WITH_KNOTS('',3,(#54293,#54294,#54295,#54296,#54297,
#54298,#54299,#54300,#54301,#54302,#54303),.UNSPECIFIED.,.F.,.F.,(4,1,1,
1,1,1,1,1,4),(122.522113490002,122.755373624488,123.750564834683,124.745756044878,
125.740947255072,126.736138465267,127.731329675462,128.726520885657,128.805298797182),
 .UNSPECIFIED.);
#959=B_SPLINE_CURVE_WITH_KNOTS('',3,(#54308,#54309,#54310,#54311,#54312,
#54313,#54314,#54315,#54316,#54317),.UNSPECIFIED.,.F.,.F.,(4,1,1,1,1,1,
1,4),(116.238928182822,117.039180333205,118.033747762313,119.02831519142,
120.022882620528,121.017450049635,122.012017478743,122.522113490002),
 .UNSPECIFIED.);
#960=B_SPLINE_CURVE_WITH_KNOTS('',3,(#54318,#54319,#54320,#54321,#54322,
#54323,#54324,#54325,#54326,#54327),.UNSPECIFIED.,.F.,.F.,(4,1,1,1,1,1,
1,4),(116.238928182822,116.784226363319,117.779417573514,118.774608783709,
119.769799993904,120.764991204098,121.760182414293,122.522113490002),
 .UNSPECIFIED.);
#961=B_SPLINE_CURVE_WITH_KNOTS('',3,(#54332,#54333,#54334,#54335,#54336,
#54337,#54338,#54339,#54340,#54341,#54342),.UNSPECIFIED.,.F.,.F.,(4,1,1,
1,1,1,1,1,4),(109.955742875643,110.077208329453,111.071775758561,112.066343187668,
113.060910616776,114.055478045883,115.050045474991,116.044612904098,116.238928182822),
 .UNSPECIFIED.);
#962=B_SPLINE_CURVE_WITH_KNOTS('',3,(#54343,#54344,#54345,#54346,#54347,
#54348,#54349,#54350,#54351,#54352),.UNSPECIFIED.,.F.,.F.,(4,1,1,1,1,1,
1,4),(109.955742875643,110.81307910215,111.808270312345,112.80346152254,
113.798652732735,114.793843942929,115.789035153124,116.238928182822),
 .UNSPECIFIED.);
#963=B_SPLINE_CURVE_WITH_KNOTS('',3,(#54357,#54358,#54359,#54360,#54361,
#54362,#54363,#54364,#54365,#54366),.UNSPECIFIED.,.F.,.F.,(4,1,1,1,1,1,
1,4),(103.672557568463,104.109803754809,105.104371183916,106.098938613024,
107.093506042131,108.088073471239,109.082640900346,109.955742875643),
 .UNSPECIFIED.);
#964=B_SPLINE_CURVE_WITH_KNOTS('',3,(#54367,#54368,#54369,#54370,#54371,
#54372,#54373,#54374,#54375,#54376,#54377),.UNSPECIFIED.,.F.,.F.,(4,1,1,
1,1,1,1,1,4),(103.672557568463,103.846740630786,104.841931840981,105.837123051176,
106.832314261371,107.827505471566,108.82269668176,109.817887891955,109.955742875643),
 .UNSPECIFIED.);
#965=B_SPLINE_CURVE_WITH_KNOTS('',3,(#54382,#54383,#54384,#54385,#54386,
#54387,#54388,#54389,#54390,#54391),.UNSPECIFIED.,.F.,.F.,(4,1,1,1,1,1,
1,4),(97.3893722612836,98.1423991801644,99.1369666092718,100.131534038379,
101.126101467487,102.120668896594,103.115236325701,103.672557568463),
 .UNSPECIFIED.);
#966=B_SPLINE_CURVE_WITH_KNOTS('',3,(#54392,#54393,#54394,#54395,#54396,
#54397,#54398,#54399,#54400,#54401),.UNSPECIFIED.,.F.,.F.,(4,1,1,1,1,1,
1,4),(97.3893722612835,97.8755933696174,98.8707845798122,99.865975790007,
100.861167000202,101.856358210397,102.851549420591,103.672557568463),
 .UNSPECIFIED.);
#967=B_SPLINE_CURVE_WITH_KNOTS('',3,(#54406,#54407,#54408,#54409,#54410,
#54411,#54412,#54413,#54414,#54415,#54416),.UNSPECIFIED.,.F.,.F.,(4,1,1,
1,1,1,1,1,4),(91.106186954104,91.1804271764124,92.1749946055198,93.1695620346272,
94.1641294637347,95.1586968928421,96.1532643219495,97.1478317510569,97.3893722612836),
 .UNSPECIFIED.);
#968=B_SPLINE_CURVE_WITH_KNOTS('',3,(#54417,#54418,#54419,#54420,#54421,
#54422,#54423,#54424,#54425,#54426),.UNSPECIFIED.,.F.,.F.,(4,1,1,1,1,1,
1,4),(91.106186954104,91.9044461084484,92.8996373186432,93.8948285288381,
94.8900197390329,95.8852109492277,96.8804021594225,97.3893722612835),
 .UNSPECIFIED.);
#969=B_SPLINE_CURVE_WITH_KNOTS('',3,(#54431,#54432,#54433,#54434,#54435,
#54436,#54437,#54438,#54439,#54440),.UNSPECIFIED.,.F.,.F.,(4,1,1,1,1,1,
1,4),(84.8230016469244,85.2130226017678,86.2075900308752,87.2021574599827,
88.1967248890901,89.1912923181975,90.1858597473049,91.106186954104),
 .UNSPECIFIED.);
#970=B_SPLINE_CURVE_WITH_KNOTS('',3,(#54441,#54442,#54443,#54444,#54445,
#54446,#54447,#54448,#54449,#54450,#54451),.UNSPECIFIED.,.F.,.F.,(4,1,1,
1,1,1,1,1,4),(84.8230016469244,84.9381076370846,85.9332988472795,86.9284900574743,
87.9236812676691,88.9188724778639,89.9140636880588,90.9092548982536,91.106186954104),
 .UNSPECIFIED.);
#971=B_SPLINE_CURVE_WITH_KNOTS('',3,(#54456,#54457,#54458,#54459,#54460,
#54461,#54462,#54463,#54464,#54465),.UNSPECIFIED.,.F.,.F.,(4,1,1,1,1,1,
1,4),(78.5398163397448,79.2456180271232,80.2401854562307,81.2347528853381,
82.2293203144455,83.223887743553,84.2184551726604,84.8230016469244),
 .UNSPECIFIED.);
#972=B_SPLINE_CURVE_WITH_KNOTS('',3,(#54466,#54467,#54468,#54469,#54470,
#54471,#54472,#54473,#54474,#54475),.UNSPECIFIED.,.F.,.F.,(4,1,1,1,1,1,
1,4),(78.5398163397448,78.9669603759157,79.9621515861105,80.9573427963053,
81.9525340065002,82.947725216695,83.9429164268898,84.8230016469244),
 .UNSPECIFIED.);
#973=B_SPLINE_CURVE_WITH_KNOTS('',3,(#54480,#54481,#54482,#54483,#54484,
#54485,#54486,#54487,#54488,#54489,#54490),.UNSPECIFIED.,.F.,.F.,(4,1,1,
1,1,1,1,1,4),(72.2566310325652,72.2836460233713,73.2782134524787,74.2727808815861,
75.2673483106935,76.261915739801,77.2564831689084,78.2510505980158,78.5398163397448),
 .UNSPECIFIED.);
#974=B_SPLINE_CURVE_WITH_KNOTS('',3,(#54491,#54492,#54493,#54494,#54495,
#54496,#54497,#54498,#54499,#54500),.UNSPECIFIED.,.F.,.F.,(4,1,1,1,1,1,
1,4),(72.2566310325652,72.9958131147467,73.9910043249416,74.9861955351364,
75.9813867453312,76.976577955526,77.9717691657209,78.5398163397448),
 .UNSPECIFIED.);
#975=B_SPLINE_CURVE_WITH_KNOTS('',3,(#54505,#54506,#54507,#54508,#54509,
#54510,#54511,#54512,#54513,#54514),.UNSPECIFIED.,.F.,.F.,(4,1,1,1,1,1,
1,4),(65.9734457253856,66.3162414487267,67.3108088778341,68.3053763069416,
69.299943736049,70.2945111651564,71.2890785942638,72.2566310325652),
 .UNSPECIFIED.);
#976=B_SPLINE_CURVE_WITH_KNOTS('',3,(#54515,#54516,#54517,#54518,#54519,
#54520,#54521,#54522,#54523,#54524,#54525),.UNSPECIFIED.,.F.,.F.,(4,1,1,
1,1,1,1,1,4),(65.9734457253856,66.029474643383,67.0246658535778,68.0198570637726,
69.0150482739674,70.0102394841623,71.0054306943571,72.0006219045519,72.2566310325652),
 .UNSPECIFIED.);
#977=B_SPLINE_CURVE_WITH_KNOTS('',3,(#54530,#54531,#54532,#54533,#54534,
#54535,#54536,#54537,#54538,#54539),.UNSPECIFIED.,.F.,.F.,(4,1,1,1,1,1,
1,4),(59.690260418206,60.3488368740821,61.3434043031896,62.337971732297,
63.3325391614044,64.3271065905118,65.3216740196193,65.9734457253856),
 .UNSPECIFIED.);
#978=B_SPLINE_CURVE_WITH_KNOTS('',3,(#54540,#54541,#54542,#54543,#54544,
#54545,#54546,#54547,#54548,#54549),.UNSPECIFIED.,.F.,.F.,(4,1,1,1,1,1,
1,4),(59.690260418206,60.058327382214,61.0535185924088,62.0487098026037,
63.0439010127985,64.0390922229933,65.0342834331881,65.9734457253856),
 .UNSPECIFIED.);
#979=B_SPLINE_CURVE_WITH_KNOTS('',3,(#54554,#54555,#54556,#54557,#54558,
#54559,#54560,#54561,#54562,#54563),.UNSPECIFIED.,.F.,.F.,(4,1,1,1,1,1,
1,4),(53.4070751110264,54.3814322994376,55.375999728545,56.3705671576524,
57.3651345867599,58.3597020158673,59.3542694449747,59.690260418206),
 .UNSPECIFIED.);
#980=B_SPLINE_CURVE_WITH_KNOTS('',3,(#54564,#54565,#54566,#54567,#54568,
#54569,#54570,#54571,#54572,#54573),.UNSPECIFIED.,.F.,.F.,(4,1,1,1,1,1,
1,4),(53.4070751110264,54.0871801210451,55.0823713312399,56.0775625414347,
57.0727537516295,58.0679449618244,59.0631361720192,59.690260418206),
 .UNSPECIFIED.);
#981=B_SPLINE_CURVE_WITH_KNOTS('',3,(#54578,#54579,#54580,#54581,#54582,
#54583,#54584,#54585,#54586,#54587,#54588),.UNSPECIFIED.,.F.,.F.,(4,1,1,
1,1,1,1,1,4),(47.1238898038468,47.4194602956856,48.414027724793,49.4085951539004,
50.4031625830079,51.3977300121153,52.3922974412227,53.3868648703302,53.4070751110264),
 .UNSPECIFIED.);
#982=B_SPLINE_CURVE_WITH_KNOTS('',3,(#54589,#54590,#54591,#54592,#54593,
#54594,#54595,#54596,#54597,#54598),.UNSPECIFIED.,.F.,.F.,(4,1,1,1,1,1,
1,4),(47.1238898038468,48.1160328598761,49.1112240700709,50.1064152802658,
51.1016064904606,52.0967977006554,53.0919889108502,53.4070751110264),
 .UNSPECIFIED.);
#983=B_SPLINE_CURVE_WITH_KNOTS('',3,(#54603,#54604,#54605,#54606,#54607,
#54608,#54609,#54610,#54611,#54612),.UNSPECIFIED.,.F.,.F.,(4,1,1,1,1,1,
1,4),(40.8407044966672,41.452055721041,42.4466231501485,43.4411905792559,
44.4357580083633,45.4303254374707,46.4248928665782,47.1238898038468),
 .UNSPECIFIED.);
#984=B_SPLINE_CURVE_WITH_KNOTS('',3,(#54613,#54614,#54615,#54616,#54617,
#54618,#54619,#54620,#54621,#54622,#54623),.UNSPECIFIED.,.F.,.F.,(4,1,1,
1,1,1,1,1,4),(40.8407044966672,41.1496943885123,42.1448855987072,43.140076808902,
44.1352680190968,45.1304592292916,46.1256504394865,47.1208416496813,47.1238898038468),
 .UNSPECIFIED.);
#985=B_SPLINE_CURVE_WITH_KNOTS('',3,(#54628,#54629,#54630,#54631,#54632,
#54633,#54634,#54635,#54636,#54637),.UNSPECIFIED.,.F.,.F.,(4,1,1,1,1,1,
1,4),(34.5575191894876,35.4846511463965,36.4792185755039,37.4737860046113,
38.4683534337187,39.4629208628262,40.4574882919336,40.8407044966672),
 .UNSPECIFIED.);
#986=B_SPLINE_CURVE_WITH_KNOTS('',3,(#54638,#54639,#54640,#54641,#54642,
#54643,#54644,#54645,#54646,#54647),.UNSPECIFIED.,.F.,.F.,(4,1,1,1,1,1,
1,4),(34.5575191894876,35.1785471273434,36.1737383375382,37.168929547733,
38.1641207579279,39.1593119681227,40.1545031783175,40.8407044966672),
 .UNSPECIFIED.);
#987=B_SPLINE_CURVE_WITH_KNOTS('',3,(#54652,#54653,#54654,#54655,#54656,
#54657,#54658,#54659,#54660,#54661,#54662),.UNSPECIFIED.,.F.,.F.,(4,1,1,
1,1,1,1,1,4),(28.274333882308,28.5226791426445,29.5172465717519,30.5118140008593,
31.5063814299668,32.5009488590742,33.4955162881816,34.490083717289,34.5575191894876),
 .UNSPECIFIED.);
#988=B_SPLINE_CURVE_WITH_KNOTS('',3,(#54663,#54664,#54665,#54666,#54667,
#54668,#54669,#54670,#54671,#54672),.UNSPECIFIED.,.F.,.F.,(4,1,1,1,1,1,
1,4),(28.274333882308,29.2073998661744,30.2025910763693,31.1977822865641,
32.1929734967589,33.1881647069537,34.1833559171486,34.5575191894876),
 .UNSPECIFIED.);
#989=B_SPLINE_CURVE_WITH_KNOTS('',3,(#54677,#54678,#54679,#54680,#54681,
#54682,#54683,#54684,#54685,#54686),.UNSPECIFIED.,.F.,.F.,(4,1,1,1,1,1,
1,4),(21.9911485751285,22.5552745679999,23.5498419971074,24.5444094262148,
25.5389768553222,26.5335442844296,27.5281117135371,28.274333882308),
 .UNSPECIFIED.);
#990=B_SPLINE_CURVE_WITH_KNOTS('',3,(#54687,#54688,#54689,#54690,#54691,
#54692,#54693,#54694,#54695,#54696,#54697),.UNSPECIFIED.,.F.,.F.,(4,1,1,
1,1,1,1,1,4),(21.9911485751285,22.2410613948107,23.2362526050055,24.2314438152003,
25.2266350253952,26.22182623559,27.2170174457848,28.2122086559796,28.274333882308),
 .UNSPECIFIED.);
#991=B_SPLINE_CURVE_WITH_KNOTS('',3,(#54702,#54703,#54704,#54705,#54706,
#54707,#54708,#54709,#54710,#54711),.UNSPECIFIED.,.F.,.F.,(4,1,1,1,1,1,
1,4),(15.7079632679489,16.5878699933554,17.5824374224628,18.5770048515702,
19.5715722806776,20.5661397097851,21.5607071388925,21.9911485751285),
 .UNSPECIFIED.);
#992=B_SPLINE_CURVE_WITH_KNOTS('',3,(#54712,#54713,#54714,#54715,#54716,
#54717,#54718,#54719,#54720,#54721),.UNSPECIFIED.,.F.,.F.,(4,1,1,1,1,1,
1,4),(15.7079632679489,16.2699141336417,17.2651053438366,18.2602965540314,
19.2554877642262,20.250678974421,21.2458701846159,21.9911485751285),
 .UNSPECIFIED.);
#993=B_SPLINE_CURVE_WITH_KNOTS('',3,(#54724,#54725,#54726,#54727,#54728,
#54729,#54730,#54731,#54732,#54733,#54734,#54735,#54736,#54737,#54738,#54739,
#54740,#54741,#54742,#54743,#54744,#54745,#54746,#54747,#54748,#54749,#54750,
#54751,#54752,#54753,#54754,#54755,#54756,#54757,#54758,#54759,#54760,#54761,
#54762,#54763,#54764,#54765,#54766,#54767,#54768,#54769,#54770,#54771,#54772,
#54773,#54774,#54775,#54776,#54777,#54778,#54779,#54780,#54781,#54782,#54783,
#54784,#54785,#54786,#54787,#54788,#54789,#54790,#54791,#54792,#54793,#54794,
#54795,#54796,#54797,#54798,#54799,#54800,#54801,#54802,#54803,#54804,#54805,
#54806,#54807,#54808,#54809,#54810,#54811,#54812,#54813,#54814,#54815,#54816,
#54817,#54818,#54819,#54820,#54821,#54822,#54823,#54824,#54825,#54826,#54827,
#54828,#54829,#54830,#54831,#54832,#54833,#54834,#54835,#54836,#54837,#54838,
#54839,#54840,#54841,#54842,#54843,#54844,#54845,#54846,#54847,#54848,#54849,
#54850,#54851,#54852,#54853,#54854,#54855,#54856,#54857,#54858,#54859,#54860,
#54861,#54862,#54863,#54864,#54865,#54866,#54867,#54868,#54869,#54870,#54871,
#54872,#54873,#54874,#54875,#54876,#54877,#54878,#54879,#54880,#54881,#54882,
#54883,#54884,#54885,#54886,#54887,#54888,#54889,#54890,#54891,#54892,#54893,
#54894,#54895,#54896,#54897,#54898,#54899,#54900,#54901,#54902,#54903,#54904,
#54905,#54906,#54907,#54908,#54909,#54910,#54911,#54912,#54913,#54914,#54915,
#54916,#54917,#54918,#54919,#54920,#54921,#54922,#54923,#54924,#54925,#54926,
#54927,#54928,#54929,#54930,#54931,#54932,#54933,#54934,#54935,#54936,#54937,
#54938,#54939,#54940,#54941,#54942,#54943,#54944,#54945,#54946,#54947,#54948,
#54949,#54950,#54951,#54952,#54953,#54954,#54955,#54956,#54957,#54958,#54959,
#54960,#54961,#54962,#54963,#54964,#54965,#54966,#54967),.UNSPECIFIED.,
 .F.,.F.,(4,3,3,3,3,3,3,3,3,3,3,3,3,3,3,3,3,3,3,3,3,3,3,3,3,3,3,3,3,3,3,
3,3,3,3,3,3,3,3,3,3,3,3,3,3,3,3,3,3,3,3,3,3,3,3,3,3,3,3,3,3,3,3,3,3,3,3,
3,3,3,3,3,3,3,3,3,3,3,3,3,3,4),(-2.64334436896556,-2.60354403016607,-2.56319357704322,
-2.52826625024512,-2.51459318907079,-2.50781535649548,-2.46564981317316,
-2.42348426985084,-2.39566963603287,-2.38341570939638,-2.37761610684016,
-2.336849738158,-2.29583153162079,-2.25519438983726,-2.22808079457215,-2.2136427889914,
-2.20824896814423,-2.20096719930704,-2.16123852890373,-2.12054358173304,
-2.07915011465577,-2.03779648847865,-2.03243166702702,-1.99089005776529,
-1.94895701700167,-1.90713874879756,-1.86743433790788,-1.85926764668736,
-1.85203534200324,-1.80992713326301,-1.76842432689819,-1.74832110523882,
-1.70676763322338,-1.68046855645703,-1.67322668686903,-1.63229330306282,
-1.58900444080018,-1.54654889761395,-1.51397808603242,-1.5045713939363,
-1.49689579776549,-1.49148547399684,-1.44889513044297,-1.40637477884859,
-1.36441427917375,-1.32519834206773,-1.31745702219618,-1.31155026142285,
-1.28598240496172,-1.24479777214057,-1.20266268120784,-1.15989915790716,
-1.13825803467134,-1.13225377395059,-1.12622665290763,-1.08347961800304,
-1.04027268262164,-0.997123369249094,-0.954546729607404,-0.947141190072399,
-0.941377976925763,-0.897944447185484,-0.855190214624572,-0.813641186133967,
-0.785925562678236,-0.769826109785476,-0.761910560472749,-0.75632393840638,
-0.714342458530382,-0.67097419230323,-0.627232222714931,-0.595102096230848,
-0.581045165894062,-0.572765453161588,-0.566918945151293,-0.523130330920948,
-0.47917700856887,-0.435659870904986,-0.402925540873628,-0.383690774196495,
-0.377633521738216,-0.37019121084227),.UNSPECIFIED.);
#994=B_SPLINE_CURVE_WITH_KNOTS('',3,(#54969,#54970,#54971,#54972,#54973,
#54974,#54975,#54976,#54977,#54978,#54979,#54980,#54981,#54982,#54983,#54984,
#54985,#54986,#54987,#54988,#54989,#54990,#54991,#54992,#54993,#54994,#54995,
#54996,#54997,#54998,#54999,#55000,#55001,#55002,#55003,#55004,#55005,#55006,
#55007,#55008,#55009,#55010,#55011,#55012,#55013,#55014,#55015,#55016,#55017,
#55018,#55019,#55020,#55021,#55022,#55023,#55024,#55025,#55026,#55027,#55028,
#55029,#55030,#55031,#55032,#55033,#55034,#55035,#55036,#55037,#55038,#55039,
#55040,#55041),.UNSPECIFIED.,.F.,.F.,(4,3,3,3,3,3,3,3,3,3,3,3,3,3,3,3,3,
3,3,3,3,3,3,3,4),(-0.710745924398683,-0.666804013499017,-0.623090002091155,
-0.580490043399667,-0.549769720878275,-0.540030794848239,-0.533787755766615,
-0.491609440904295,-0.4576087533141,-0.414988201685294,-0.372400295436586,
-0.356121723662545,-0.350309819512417,-0.308708315030754,-0.266458526938774,
-0.224208738846794,-0.196182646490945,-0.183254318429312,-0.17525918271343,
-0.169900496948286,-0.127425372711214,-0.0868708094010787,-0.0467252344004481,
-0.00739903503843566,0.),.UNSPECIFIED.);
#995=B_SPLINE_CURVE_WITH_KNOTS('',3,(#55044,#55045,#55046,#55047,#55048,
#55049,#55050,#55051,#55052,#55053,#55054,#55055,#55056,#55057,#55058,#55059,
#55060,#55061,#55062,#55063,#55064,#55065,#55066,#55067,#55068,#55069,#55070,
#55071,#55072,#55073,#55074,#55075,#55076,#55077,#55078,#55079,#55080),
 .UNSPECIFIED.,.F.,.F.,(4,3,3,3,3,3,3,3,3,3,3,3,4),(-0.37019121084227,-0.331697325929431,
-0.288622232780515,-0.244797719637212,-0.21419800468256,-0.2008106293899,
-0.194172952745162,-0.188472403894731,-0.144967619206762,-0.100508059630889,
-0.0559598465844598,-0.0119678329618413,0.),.UNSPECIFIED.);
#996=B_SPLINE_CURVE_WITH_KNOTS('',3,(#55601,#55602,#55603,#55604,#55605,
#55606,#55607,#55608,#55609),.UNSPECIFIED.,.F.,.F.,(4,1,1,1,1,1,4),(11.6150328478182,
12.1123165623719,12.6096002769257,13.6041677060331,14.5987351351405,15.5933025642479,
15.7079632679489),.UNSPECIFIED.);
#997=B_SPLINE_CURVE_WITH_KNOTS('',3,(#55610,#55611,#55612,#55613,#55614,
#55615,#55616,#55617,#55618,#55619,#55620,#55621,#55622,#55623,#55624,#55625,
#55626,#55627,#55628,#55629,#55630,#55631,#55632,#55633,#55634,#55635,#55636,
#55637,#55638,#55639,#55640,#55641,#55642,#55643,#55644,#55645,#55646,#55647,
#55648,#55649,#55650,#55651,#55652,#55653,#55654,#55655,#55656,#55657,#55658,
#55659,#55660,#55661,#55662,#55663,#55664,#55665,#55666,#55667,#55668,#55669,
#55670,#55671,#55672,#55673,#55674,#55675,#55676,#55677,#55678,#55679,#55680,
#55681,#55682,#55683,#55684,#55685,#55686,#55687,#55688,#55689,#55690,#55691,
#55692,#55693,#55694,#55695,#55696,#55697,#55698,#55699,#55700,#55701,#55702,
#55703,#55704,#55705,#55706,#55707,#55708,#55709,#55710,#55711,#55712),
 .UNSPECIFIED.,.F.,.F.,(4,3,3,3,3,3,3,3,3,3,3,3,3,3,3,3,3,3,3,3,3,3,3,3,
3,3,3,3,3,3,3,3,3,3,4),(-0.965990216419481,-0.9272199902169,-0.883653696268922,
-0.856578499606751,-0.840281614965736,-0.83272424860471,-0.78942649842623,
-0.747054504832225,-0.728516757634848,-0.714850133126621,-0.708733859333935,
-0.665685633827477,-0.622719517527392,-0.579652275564091,-0.547351844091615,
-0.533932274491217,-0.525881927440116,-0.484249432147785,-0.450450549674188,
-0.408562082241703,-0.366597621077022,-0.351118396676314,-0.345479700399037,
-0.304353213451827,-0.263090931261655,-0.221828649071483,-0.194100067937547,
-0.181335497105944,-0.172973757166477,-0.167228677968348,-0.125421508476261,
-0.0849791978641806,-0.0449278087924871,-0.005690172937603,0.),
 .UNSPECIFIED.);
#998=B_SPLINE_CURVE_WITH_KNOTS('',3,(#55713,#55714,#55715,#55716,#55717,
#55718,#55719,#55720,#55721,#55722,#55723,#55724,#55725,#55726,#55727,#55728,
#55729,#55730,#55731),.UNSPECIFIED.,.F.,.F.,(4,3,3,3,3,3,4),(-121.812676859456,
-121.337226351106,-120.342658921999,-119.348091492891,-118.353524063784,
-117.358956634676,-117.190265949363),.UNSPECIFIED.);
#999=B_SPLINE_CURVE_WITH_KNOTS('',3,(#55734,#55735,#55736,#55737,#55738,
#55739,#55740,#55741,#55742),.UNSPECIFIED.,.F.,.F.,(4,1,1,1,1,1,4),(10.3761157273101,
11.2939580826676,12.2891492928624,13.2843405030573,14.2795317132521,15.2747229234469,
15.7079632679489),.UNSPECIFIED.);
#1000=B_SPLINE_CURVE_WITH_KNOTS('',3,(#56268,#56269,#56270,#56271,#56272,
#56273,#56274,#56275,#56276,#56277,#56278,#56279,#56280,#56281,#56282,#56283,
#56284,#56285,#56286,#56287,#56288,#56289),.UNSPECIFIED.,.F.,.F.,(4,3,3,
3,3,3,3,4),(114.213729037919,114.446989172405,115.4421803826,116.437371592795,
117.432562802989,118.427754013184,119.422945223379,119.744945584229),
 .UNSPECIFIED.);
#1001=B_SPLINE_CURVE_WITH_KNOTS('',3,(#56290,#56291,#56292,#56293,#56294,
#56295,#56296,#56297,#56298,#56299,#56300,#56301,#56302,#56303,#56304,#56305,
#56306,#56307,#56308,#56309,#56310,#56311,#56312,#56313,#56314,#56315,#56316,
#56317,#56318,#56319,#56320,#56321,#56322,#56323,#56324,#56325,#56326,#56327,
#56328,#56329,#56330,#56331,#56332,#56333,#56334,#56335,#56336,#56337,#56338,
#56339,#56340,#56341,#56342,#56343,#56344,#56345,#56346,#56347,#56348,#56349,
#56350,#56351,#56352,#56353,#56354,#56355,#56356,#56357,#56358,#56359,#56360,
#56361,#56362,#56363,#56364,#56365,#56366,#56367,#56368,#56369,#56370,#56371,
#56372,#56373,#56374,#56375,#56376,#56377,#56378,#56379,#56380,#56381,#56382,
#56383,#56384,#56385,#56386,#56387,#56388,#56389,#56390,#56391,#56392,#56393,
#56394,#56395),.UNSPECIFIED.,.F.,.F.,(4,3,3,3,3,3,3,3,3,3,3,3,3,3,3,3,3,
3,3,3,3,3,3,3,3,3,3,3,3,3,3,3,3,3,3,4),(-0.968477696161952,-0.934401878411372,
-0.894940908856935,-0.869057110968003,-0.857761995024893,-0.84957581141373,
-0.809420536841839,-0.768342987565862,-0.750371559757621,-0.741288256886726,
-0.734041921366352,-0.692568544969978,-0.650621991967233,-0.60816652963393,
-0.576324932883953,-0.562465720811907,-0.556565387998925,-0.513962262185476,
-0.480800142634022,-0.43927778705218,-0.397173024145668,-0.382659788254531,
-0.376822993230344,-0.334735665268914,-0.292008067784669,-0.248907378913767,
-0.243684959408641,-0.213224339482561,-0.199897818264901,-0.191569349313896,
-0.186008989480452,-0.142614739306227,-0.0987671132040068,-0.0550446346348842,
-0.0119839009752852,0.),.UNSPECIFIED.);
#2219=SHAPE_REPRESENTATION_RELATIONSHIP('SRR','None',#97613,#2238);
#2238=ADVANCED_BREP_SHAPE_REPRESENTATION('',(#2276),#97463);
#2257=STYLED_ITEM('',(#97720),#2276);
#2276=MANIFOLD_SOLID_BREP('Body1',#21818);
#2339=FACE_BOUND('',#4207,.T.);
#2340=FACE_BOUND('',#4210,.T.);
#2466=PLANE('',#22682);
#2467=PLANE('',#22683);
#2468=PLANE('',#22684);
#2469=PLANE('',#22685);
#2470=PLANE('',#22686);
#2471=PLANE('',#22687);
#2472=PLANE('',#22688);
#2473=PLANE('',#22689);
#2474=PLANE('',#22693);
#2475=PLANE('',#22694);
#2951=FACE_OUTER_BOUND('',#4156,.T.);
#2952=FACE_OUTER_BOUND('',#4157,.T.);
#2953=FACE_OUTER_BOUND('',#4158,.T.);
#2954=FACE_OUTER_BOUND('',#4159,.T.);
#2955=FACE_OUTER_BOUND('',#4160,.T.);
#2956=FACE_OUTER_BOUND('',#4161,.T.);
#2957=FACE_OUTER_BOUND('',#4162,.T.);
#2958=FACE_OUTER_BOUND('',#4163,.T.);
#2959=FACE_OUTER_BOUND('',#4164,.T.);
#2960=FACE_OUTER_BOUND('',#4165,.T.);
#2961=FACE_OUTER_BOUND('',#4166,.T.);
#2962=FACE_OUTER_BOUND('',#4167,.T.);
#2963=FACE_OUTER_BOUND('',#4168,.T.);
#2964=FACE_OUTER_BOUND('',#4169,.T.);
#2965=FACE_OUTER_BOUND('',#4170,.T.);
#2966=FACE_OUTER_BOUND('',#4171,.T.);
#2967=FACE_OUTER_BOUND('',#4172,.T.);
#2968=FACE_OUTER_BOUND('',#4173,.T.);
#2969=FACE_OUTER_BOUND('',#4174,.T.);
#2970=FACE_OUTER_BOUND('',#4175,.T.);
#2971=FACE_OUTER_BOUND('',#4176,.T.);
#2972=FACE_OUTER_BOUND('',#4177,.T.);
#2973=FACE_OUTER_BOUND('',#4178,.T.);
#2974=FACE_OUTER_BOUND('',#4179,.T.);
#2975=FACE_OUTER_BOUND('',#4180,.T.);
#2976=FACE_OUTER_BOUND('',#4181,.T.);
#2977=FACE_OUTER_BOUND('',#4182,.T.);
#2978=FACE_OUTER_BOUND('',#4183,.T.);
#2979=FACE_OUTER_BOUND('',#4184,.T.);
#2980=FACE_OUTER_BOUND('',#4185,.T.);
#2981=FACE_OUTER_BOUND('',#4186,.T.);
#2982=FACE_OUTER_BOUND('',#4187,.T.);
#2983=FACE_OUTER_BOUND('',#4188,.T.);
#2984=FACE_OUTER_BOUND('',#4189,.T.);
#2985=FACE_OUTER_BOUND('',#4190,.T.);
#2986=FACE_OUTER_BOUND('',#4191,.T.);
#2987=FACE_OUTER_BOUND('',#4192,.T.);
#2988=FACE_OUTER_BOUND('',#4193,.T.);
#2989=FACE_OUTER_BOUND('',#4194,.T.);
#2990=FACE_OUTER_BOUND('',#4195,.T.);
#2991=FACE_OUTER_BOUND('',#4196,.T.);
#2992=FACE_OUTER_BOUND('',#4197,.T.);
#2993=FACE_OUTER_BOUND('',#4198,.T.);
#2994=FACE_OUTER_BOUND('',#4199,.T.);
#2995=FACE_OUTER_BOUND('',#4200,.T.);
#2996=FACE_OUTER_BOUND('',#4201,.T.);
#2997=FACE_OUTER_BOUND('',#4202,.T.);
#2998=FACE_OUTER_BOUND('',#4203,.T.);
#2999=FACE_OUTER_BOUND('',#4204,.T.);
#3000=FACE_OUTER_BOUND('',#4205,.T.);
#3001=FACE_OUTER_BOUND('',#4206,.T.);
#3002=FACE_OUTER_BOUND('',#4208,.T.);
#3003=FACE_OUTER_BOUND('',#4209,.T.);
#3004=FACE_OUTER_BOUND('',#4211,.T.);
#4156=EDGE_LOOP('',(#15482,#15483,#15484,#15485));
#4157=EDGE_LOOP('',(#15486,#15487,#15488,#15489));
#4158=EDGE_LOOP('',(#15490,#15491,#15492,#15493));
#4159=EDGE_LOOP('',(#15494,#15495,#15496,#15497));
#4160=EDGE_LOOP('',(#15498,#15499,#15500,#15501));
#4161=EDGE_LOOP('',(#15502,#15503,#15504,#15505));
#4162=EDGE_LOOP('',(#15506,#15507,#15508,#15509));
#4163=EDGE_LOOP('',(#15510,#15511,#15512,#15513));
#4164=EDGE_LOOP('',(#15514,#15515,#15516,#15517));
#4165=EDGE_LOOP('',(#15518,#15519,#15520,#15521));
#4166=EDGE_LOOP('',(#15522,#15523,#15524,#15525));
#4167=EDGE_LOOP('',(#15526,#15527,#15528,#15529));
#4168=EDGE_LOOP('',(#15530,#15531,#15532,#15533));
#4169=EDGE_LOOP('',(#15534,#15535,#15536,#15537));
#4170=EDGE_LOOP('',(#15538,#15539,#15540,#15541));
#4171=EDGE_LOOP('',(#15542,#15543,#15544,#15545));
#4172=EDGE_LOOP('',(#15546,#15547,#15548,#15549));
#4173=EDGE_LOOP('',(#15550,#15551,#15552,#15553));
#4174=EDGE_LOOP('',(#15554,#15555,#15556,#15557));
#4175=EDGE_LOOP('',(#15558,#15559,#15560,#15561));
#4176=EDGE_LOOP('',(#15562,#15563,#15564,#15565));
#4177=EDGE_LOOP('',(#15566,#15567,#15568,#15569));
#4178=EDGE_LOOP('',(#15570,#15571,#15572,#15573));
#4179=EDGE_LOOP('',(#15574,#15575,#15576,#15577));
#4180=EDGE_LOOP('',(#15578,#15579,#15580,#15581));
#4181=EDGE_LOOP('',(#15582,#15583,#15584,#15585));
#4182=EDGE_LOOP('',(#15586,#15587,#15588,#15589));
#4183=EDGE_LOOP('',(#15590,#15591,#15592,#15593));
#4184=EDGE_LOOP('',(#15594,#15595,#15596,#15597));
#4185=EDGE_LOOP('',(#15598,#15599,#15600,#15601));
#4186=EDGE_LOOP('',(#15602,#15603,#15604,#15605));
#4187=EDGE_LOOP('',(#15606,#15607,#15608,#15609));
#4188=EDGE_LOOP('',(#15610,#15611,#15612,#15613));
#4189=EDGE_LOOP('',(#15614,#15615,#15616,#15617));
#4190=EDGE_LOOP('',(#15618,#15619,#15620,#15621));
#4191=EDGE_LOOP('',(#15622,#15623,#15624,#15625));
#4192=EDGE_LOOP('',(#15626,#15627,#15628,#15629));
#4193=EDGE_LOOP('',(#15630,#15631,#15632,#15633));
#4194=EDGE_LOOP('',(#15634,#15635,#15636,#15637,#15638,#15639,#15640,#15641));
#4195=EDGE_LOOP('',(#15642,#15643,#15644,#15645,#15646,#15647,#15648,#15649,
#15650,#15651,#15652,#15653,#15654,#15655,#15656,#15657,#15658,#15659,#15660,
#15661,#15662,#15663,#15664,#15665,#15666,#15667,#15668,#15669,#15670,#15671,
#15672,#15673,#15674,#15675,#15676,#15677,#15678,#15679,#15680,#15681,#15682,
#15683));
#4196=EDGE_LOOP('',(#15684,#15685,#15686,#15687));
#4197=EDGE_LOOP('',(#15688,#15689,#15690,#15691,#15692,#15693,#15694,#15695,
#15696,#15697,#15698,#15699,#15700,#15701,#15702,#15703,#15704,#15705,#15706,
#15707,#15708,#15709,#15710,#15711,#15712,#15713,#15714,#15715,#15716,#15717,
#15718,#15719,#15720,#15721,#15722,#15723,#15724,#15725,#15726,#15727,#15728,
#15729,#15730));
#4198=EDGE_LOOP('',(#15731,#15732,#15733,#15734));
#4199=EDGE_LOOP('',(#15735,#15736,#15737,#15738));
#4200=EDGE_LOOP('',(#15739,#15740,#15741,#15742));
#4201=EDGE_LOOP('',(#15743,#15744,#15745,#15746));
#4202=EDGE_LOOP('',(#15747,#15748,#15749,#15750));
#4203=EDGE_LOOP('',(#15751,#15752,#15753,#15754));
#4204=EDGE_LOOP('',(#15755,#15756,#15757,#15758));
#4205=EDGE_LOOP('',(#15759,#15760,#15761,#15762,#15763,#15764));
#4206=EDGE_LOOP('',(#15765));
#4207=EDGE_LOOP('',(#15766,#15767,#15768,#15769));
#4208=EDGE_LOOP('',(#15770,#15771,#15772,#15773));
#4209=EDGE_LOOP('',(#15774));
#4210=EDGE_LOOP('',(#15775,#15776,#15777,#15778,#15779,#15780));
#4211=EDGE_LOOP('',(#15781));
#5435=LINE('',#53334,#6649);
#5436=LINE('',#53361,#6650);
#5437=LINE('',#53409,#6651);
#5438=LINE('',#53457,#6652);
#5439=LINE('',#53511,#6653);
#5440=LINE('',#53559,#6654);
#5441=LINE('',#53607,#6655);
#5442=LINE('',#53661,#6656);
#5443=LINE('',#53709,#6657);
#5444=LINE('',#53757,#6658);
#5445=LINE('',#53805,#6659);
#5446=LINE('',#53859,#6660);
#5447=LINE('',#53907,#6661);
#5448=LINE('',#53955,#6662);
#5449=LINE('',#54009,#6663);
#5450=LINE('',#54057,#6664);
#5451=LINE('',#54105,#6665);
#5452=LINE('',#54159,#6666);
#5453=LINE('',#54207,#6667);
#5454=LINE('',#54255,#6668);
#5455=LINE('',#54282,#6669);
#5456=LINE('',#54307,#6670);
#5457=LINE('',#54331,#6671);
#5458=LINE('',#54356,#6672);
#5459=LINE('',#54381,#6673);
#5460=LINE('',#54405,#6674);
#5461=LINE('',#54430,#6675);
#5462=LINE('',#54455,#6676);
#5463=LINE('',#54479,#6677);
#5464=LINE('',#54504,#6678);
#5465=LINE('',#54529,#6679);
#5466=LINE('',#54553,#6680);
#5467=LINE('',#54577,#6681);
#5468=LINE('',#54602,#6682);
#5469=LINE('',#54627,#6683);
#5470=LINE('',#54651,#6684);
#5471=LINE('',#54676,#6685);
#5472=LINE('',#54701,#6686);
#5473=LINE('',#55082,#6687);
#5474=LINE('',#56400,#6688);
#5475=LINE('',#56402,#6689);
#5476=LINE('',#56404,#6690);
#5477=LINE('',#56405,#6691);
#5478=LINE('',#56408,#6692);
#5479=LINE('',#56410,#6693);
#5480=LINE('',#56411,#6694);
#5481=LINE('',#56414,#6695);
#5482=LINE('',#56416,#6696);
#5483=LINE('',#56417,#6697);
#5484=LINE('',#56420,#6698);
#5485=LINE('',#56422,#6699);
#5486=LINE('',#56423,#6700);
#5487=LINE('',#56426,#6701);
#5488=LINE('',#56428,#6702);
#5489=LINE('',#56429,#6703);
#5490=LINE('',#56431,#6704);
#5491=LINE('',#56432,#6705);
#5492=LINE('',#56439,#6706);
#6649=VECTOR('',#25195,5.);
#6650=VECTOR('',#25200,5.);
#6651=VECTOR('',#25203,5.);
#6652=VECTOR('',#25206,5.);
#6653=VECTOR('',#25209,5.);
#6654=VECTOR('',#25212,5.);
#6655=VECTOR('',#25215,5.);
#6656=VECTOR('',#25218,5.);
#6657=VECTOR('',#25221,5.);
#6658=VECTOR('',#25224,5.);
#6659=VECTOR('',#25227,5.);
#6660=VECTOR('',#25230,5.);
#6661=VECTOR('',#25233,5.);
#6662=VECTOR('',#25236,5.);
#6663=VECTOR('',#25239,5.);
#6664=VECTOR('',#25242,5.);
#6665=VECTOR('',#25245,5.);
#6666=VECTOR('',#25248,5.);
#6667=VECTOR('',#25251,5.);
#6668=VECTOR('',#25254,4.372);
#6669=VECTOR('',#25259,4.372);
#6670=VECTOR('',#25262,4.372);
#6671=VECTOR('',#25265,4.372);
#6672=VECTOR('',#25268,4.372);
#6673=VECTOR('',#25271,4.372);
#6674=VECTOR('',#25274,4.372);
#6675=VECTOR('',#25277,4.372);
#6676=VECTOR('',#25280,4.372);
#6677=VECTOR('',#25283,4.372);
#6678=VECTOR('',#25286,4.372);
#6679=VECTOR('',#25289,4.372);
#6680=VECTOR('',#25292,4.372);
#6681=VECTOR('',#25295,4.372);
#6682=VECTOR('',#25298,4.372);
#6683=VECTOR('',#25301,4.372);
#6684=VECTOR('',#25304,4.372);
#6685=VECTOR('',#25307,4.372);
#6686=VECTOR('',#25310,4.372);
#6687=VECTOR('',#25315,4.5);
#6688=VECTOR('',#25326,10.);
#6689=VECTOR('',#25327,10.);
#6690=VECTOR('',#25328,10.);
#6691=VECTOR('',#25329,10.);
#6692=VECTOR('',#25332,10.);
#6693=VECTOR('',#25333,10.);
#6694=VECTOR('',#25334,10.);
#6695=VECTOR('',#25337,10.);
#6696=VECTOR('',#25338,10.);
#6697=VECTOR('',#25339,10.);
#6698=VECTOR('',#25342,10.);
#6699=VECTOR('',#25343,10.);
#6700=VECTOR('',#25344,10.);
#6701=VECTOR('',#25347,10.);
#6702=VECTOR('',#25348,10.);
#6703=VECTOR('',#25349,10.);
#6704=VECTOR('',#25352,10.);
#6705=VECTOR('',#25353,10.);
#6706=VECTOR('',#25362,8.);
#7509=CIRCLE('',#22637,4.942);
#7510=CIRCLE('',#22657,4.372);
#7511=CIRCLE('',#22677,4.942);
#7512=CIRCLE('',#22678,4.);
#7513=CIRCLE('',#22680,4.372);
#7514=CIRCLE('',#22690,8.);
#7515=CIRCLE('',#22692,8.);
#8403=VERTEX_POINT('',#53332);
#8404=VERTEX_POINT('',#53333);
#8405=VERTEX_POINT('',#53335);
#8406=VERTEX_POINT('',#53346);
#8407=VERTEX_POINT('',#53359);
#8408=VERTEX_POINT('',#53360);
#8409=VERTEX_POINT('',#53407);
#8410=VERTEX_POINT('',#53408);
#8411=VERTEX_POINT('',#53455);
#8412=VERTEX_POINT('',#53456);
#8413=VERTEX_POINT('',#53509);
#8414=VERTEX_POINT('',#53510);
#8415=VERTEX_POINT('',#53557);
#8416=VERTEX_POINT('',#53558);
#8417=VERTEX_POINT('',#53605);
#8418=VERTEX_POINT('',#53606);
#8419=VERTEX_POINT('',#53659);
#8420=VERTEX_POINT('',#53660);
#8421=VERTEX_POINT('',#53707);
#8422=VERTEX_POINT('',#53708);
#8423=VERTEX_POINT('',#53755);
#8424=VERTEX_POINT('',#53756);
#8425=VERTEX_POINT('',#53803);
#8426=VERTEX_POINT('',#53804);
#8427=VERTEX_POINT('',#53857);
#8428=VERTEX_POINT('',#53858);
#8429=VERTEX_POINT('',#53905);
#8430=VERTEX_POINT('',#53906);
#8431=VERTEX_POINT('',#53953);
#8432=VERTEX_POINT('',#53954);
#8433=VERTEX_POINT('',#54007);
#8434=VERTEX_POINT('',#54008);
#8435=VERTEX_POINT('',#54055);
#8436=VERTEX_POINT('',#54056);
#8437=VERTEX_POINT('',#54103);
#8438=VERTEX_POINT('',#54104);
#8439=VERTEX_POINT('',#54157);
#8440=VERTEX_POINT('',#54158);
#8441=VERTEX_POINT('',#54205);
#8442=VERTEX_POINT('',#54206);
#8443=VERTEX_POINT('',#54253);
#8444=VERTEX_POINT('',#54254);
#8445=VERTEX_POINT('',#54256);
#8446=VERTEX_POINT('',#54268);
#8447=VERTEX_POINT('',#54280);
#8448=VERTEX_POINT('',#54281);
#8449=VERTEX_POINT('',#54305);
#8450=VERTEX_POINT('',#54306);
#8451=VERTEX_POINT('',#54329);
#8452=VERTEX_POINT('',#54330);
#8453=VERTEX_POINT('',#54354);
#8454=VERTEX_POINT('',#54355);
#8455=VERTEX_POINT('',#54379);
#8456=VERTEX_POINT('',#54380);
#8457=VERTEX_POINT('',#54403);
#8458=VERTEX_POINT('',#54404);
#8459=VERTEX_POINT('',#54428);
#8460=VERTEX_POINT('',#54429);
#8461=VERTEX_POINT('',#54453);
#8462=VERTEX_POINT('',#54454);
#8463=VERTEX_POINT('',#54477);
#8464=VERTEX_POINT('',#54478);
#8465=VERTEX_POINT('',#54502);
#8466=VERTEX_POINT('',#54503);
#8467=VERTEX_POINT('',#54527);
#8468=VERTEX_POINT('',#54528);
#8469=VERTEX_POINT('',#54551);
#8470=VERTEX_POINT('',#54552);
#8471=VERTEX_POINT('',#54575);
#8472=VERTEX_POINT('',#54576);
#8473=VERTEX_POINT('',#54600);
#8474=VERTEX_POINT('',#54601);
#8475=VERTEX_POINT('',#54625);
#8476=VERTEX_POINT('',#54626);
#8477=VERTEX_POINT('',#54649);
#8478=VERTEX_POINT('',#54650);
#8479=VERTEX_POINT('',#54674);
#8480=VERTEX_POINT('',#54675);
#8481=VERTEX_POINT('',#54699);
#8482=VERTEX_POINT('',#54700);
#8483=VERTEX_POINT('',#54723);
#8484=VERTEX_POINT('',#54968);
#8485=VERTEX_POINT('',#55042);
#8486=VERTEX_POINT('',#55081);
#8487=VERTEX_POINT('',#55600);
#8488=VERTEX_POINT('',#55733);
#8489=VERTEX_POINT('',#56398);
#8490=VERTEX_POINT('',#56399);
#8491=VERTEX_POINT('',#56401);
#8492=VERTEX_POINT('',#56403);
#8493=VERTEX_POINT('',#56407);
#8494=VERTEX_POINT('',#56409);
#8495=VERTEX_POINT('',#56413);
#8496=VERTEX_POINT('',#56415);
#8497=VERTEX_POINT('',#56419);
#8498=VERTEX_POINT('',#56421);
#8499=VERTEX_POINT('',#56425);
#8500=VERTEX_POINT('',#56427);
#8501=VERTEX_POINT('',#56435);
#8502=VERTEX_POINT('',#56438);
#10998=EDGE_CURVE('',#8403,#8404,#5435,.T.);
#10999=EDGE_CURVE('',#8403,#8405,#917,.T.);
#11000=EDGE_CURVE('',#8405,#8406,#7509,.F.);
#11001=EDGE_CURVE('',#8406,#8404,#918,.T.);
#11002=EDGE_CURVE('',#8407,#8408,#5436,.T.);
#11003=EDGE_CURVE('',#8407,#8403,#919,.T.);
#11004=EDGE_CURVE('',#8404,#8408,#920,.T.);
#11005=EDGE_CURVE('',#8409,#8410,#5437,.T.);
#11006=EDGE_CURVE('',#8409,#8407,#921,.T.);
#11007=EDGE_CURVE('',#8408,#8410,#922,.T.);
#11008=EDGE_CURVE('',#8411,#8412,#5438,.T.);
#11009=EDGE_CURVE('',#8411,#8409,#923,.T.);
#11010=EDGE_CURVE('',#8410,#8412,#924,.T.);
#11011=EDGE_CURVE('',#8413,#8414,#5439,.T.);
#11012=EDGE_CURVE('',#8413,#8411,#925,.T.);
#11013=EDGE_CURVE('',#8412,#8414,#926,.T.);
#11014=EDGE_CURVE('',#8415,#8416,#5440,.T.);
#11015=EDGE_CURVE('',#8415,#8413,#927,.T.);
#11016=EDGE_CURVE('',#8414,#8416,#928,.T.);
#11017=EDGE_CURVE('',#8417,#8418,#5441,.T.);
#11018=EDGE_CURVE('',#8417,#8415,#929,.T.);
#11019=EDGE_CURVE('',#8416,#8418,#930,.T.);
#11020=EDGE_CURVE('',#8419,#8420,#5442,.T.);
#11021=EDGE_CURVE('',#8419,#8417,#931,.T.);
#11022=EDGE_CURVE('',#8418,#8420,#932,.T.);
#11023=EDGE_CURVE('',#8421,#8422,#5443,.T.);
#11024=EDGE_CURVE('',#8421,#8419,#933,.T.);
#11025=EDGE_CURVE('',#8420,#8422,#934,.T.);
#11026=EDGE_CURVE('',#8423,#8424,#5444,.T.);
#11027=EDGE_CURVE('',#8423,#8421,#935,.T.);
#11028=EDGE_CURVE('',#8422,#8424,#936,.T.);
#11029=EDGE_CURVE('',#8425,#8426,#5445,.T.);
#11030=EDGE_CURVE('',#8425,#8423,#937,.T.);
#11031=EDGE_CURVE('',#8424,#8426,#938,.T.);
#11032=EDGE_CURVE('',#8427,#8428,#5446,.T.);
#11033=EDGE_CURVE('',#8427,#8425,#939,.T.);
#11034=EDGE_CURVE('',#8426,#8428,#940,.T.);
#11035=EDGE_CURVE('',#8429,#8430,#5447,.T.);
#11036=EDGE_CURVE('',#8429,#8427,#941,.T.);
#11037=EDGE_CURVE('',#8428,#8430,#942,.T.);
#11038=EDGE_CURVE('',#8431,#8432,#5448,.T.);
#11039=EDGE_CURVE('',#8431,#8429,#943,.T.);
#11040=EDGE_CURVE('',#8430,#8432,#944,.T.);
#11041=EDGE_CURVE('',#8433,#8434,#5449,.T.);
#11042=EDGE_CURVE('',#8433,#8431,#945,.T.);
#11043=EDGE_CURVE('',#8432,#8434,#946,.T.);
#11044=EDGE_CURVE('',#8435,#8436,#5450,.T.);
#11045=EDGE_CURVE('',#8435,#8433,#947,.T.);
#11046=EDGE_CURVE('',#8434,#8436,#948,.T.);
#11047=EDGE_CURVE('',#8437,#8438,#5451,.T.);
#11048=EDGE_CURVE('',#8437,#8435,#949,.T.);
#11049=EDGE_CURVE('',#8436,#8438,#950,.T.);
#11050=EDGE_CURVE('',#8439,#8440,#5452,.T.);
#11051=EDGE_CURVE('',#8439,#8437,#951,.T.);
#11052=EDGE_CURVE('',#8438,#8440,#952,.T.);
#11053=EDGE_CURVE('',#8441,#8442,#5453,.T.);
#11054=EDGE_CURVE('',#8441,#8439,#953,.T.);
#11055=EDGE_CURVE('',#8440,#8442,#954,.T.);
#11056=EDGE_CURVE('',#8443,#8444,#5454,.T.);
#11057=EDGE_CURVE('',#8443,#8445,#955,.T.);
#11058=EDGE_CURVE('',#8445,#8446,#7510,.T.);
#11059=EDGE_CURVE('',#8444,#8446,#956,.T.);
#11060=EDGE_CURVE('',#8447,#8448,#5455,.T.);
#11061=EDGE_CURVE('',#8447,#8443,#957,.T.);
#11062=EDGE_CURVE('',#8448,#8444,#958,.T.);
#11063=EDGE_CURVE('',#8449,#8450,#5456,.T.);
#11064=EDGE_CURVE('',#8449,#8447,#959,.T.);
#11065=EDGE_CURVE('',#8450,#8448,#960,.T.);
#11066=EDGE_CURVE('',#8451,#8452,#5457,.T.);
#11067=EDGE_CURVE('',#8451,#8449,#961,.T.);
#11068=EDGE_CURVE('',#8452,#8450,#962,.T.);
#11069=EDGE_CURVE('',#8453,#8454,#5458,.T.);
#11070=EDGE_CURVE('',#8453,#8451,#963,.T.);
#11071=EDGE_CURVE('',#8454,#8452,#964,.T.);
#11072=EDGE_CURVE('',#8455,#8456,#5459,.T.);
#11073=EDGE_CURVE('',#8455,#8453,#965,.T.);
#11074=EDGE_CURVE('',#8456,#8454,#966,.T.);
#11075=EDGE_CURVE('',#8457,#8458,#5460,.T.);
#11076=EDGE_CURVE('',#8457,#8455,#967,.T.);
#11077=EDGE_CURVE('',#8458,#8456,#968,.T.);
#11078=EDGE_CURVE('',#8459,#8460,#5461,.T.);
#11079=EDGE_CURVE('',#8459,#8457,#969,.T.);
#11080=EDGE_CURVE('',#8460,#8458,#970,.T.);
#11081=EDGE_CURVE('',#8461,#8462,#5462,.T.);
#11082=EDGE_CURVE('',#8461,#8459,#971,.T.);
#11083=EDGE_CURVE('',#8462,#8460,#972,.T.);
#11084=EDGE_CURVE('',#8463,#8464,#5463,.T.);
#11085=EDGE_CURVE('',#8463,#8461,#973,.T.);
#11086=EDGE_CURVE('',#8464,#8462,#974,.T.);
#11087=EDGE_CURVE('',#8465,#8466,#5464,.T.);
#11088=EDGE_CURVE('',#8465,#8463,#975,.T.);
#11089=EDGE_CURVE('',#8466,#8464,#976,.T.);
#11090=EDGE_CURVE('',#8467,#8468,#5465,.T.);
#11091=EDGE_CURVE('',#8467,#8465,#977,.T.);
#11092=EDGE_CURVE('',#8468,#8466,#978,.T.);
#11093=EDGE_CURVE('',#8469,#8470,#5466,.T.);
#11094=EDGE_CURVE('',#8469,#8467,#979,.T.);
#11095=EDGE_CURVE('',#8470,#8468,#980,.T.);
#11096=EDGE_CURVE('',#8471,#8472,#5467,.T.);
#11097=EDGE_CURVE('',#8471,#8469,#981,.T.);
#11098=EDGE_CURVE('',#8472,#8470,#982,.T.);
#11099=EDGE_CURVE('',#8473,#8474,#5468,.T.);
#11100=EDGE_CURVE('',#8473,#8471,#983,.T.);
#11101=EDGE_CURVE('',#8474,#8472,#984,.T.);
#11102=EDGE_CURVE('',#8475,#8476,#5469,.T.);
#11103=EDGE_CURVE('',#8475,#8473,#985,.T.);
#11104=EDGE_CURVE('',#8476,#8474,#986,.T.);
#11105=EDGE_CURVE('',#8477,#8478,#5470,.T.);
#11106=EDGE_CURVE('',#8477,#8475,#987,.T.);
#11107=EDGE_CURVE('',#8478,#8476,#988,.T.);
#11108=EDGE_CURVE('',#8479,#8480,#5471,.T.);
#11109=EDGE_CURVE('',#8479,#8477,#989,.T.);
#11110=EDGE_CURVE('',#8480,#8478,#990,.T.);
#11111=EDGE_CURVE('',#8481,#8482,#5472,.T.);
#11112=EDGE_CURVE('',#8481,#8479,#991,.T.);
#11113=EDGE_CURVE('',#8482,#8480,#992,.T.);
#11114=EDGE_CURVE('',#8446,#8483,#993,.T.);
#11115=EDGE_CURVE('',#8484,#8445,#994,.T.);
#11116=EDGE_CURVE('',#8485,#8484,#7511,.T.);
#11117=EDGE_CURVE('',#8483,#8485,#995,.T.);
#11118=EDGE_CURVE('',#8483,#8486,#5473,.T.);
#11119=EDGE_CURVE('',#8486,#8486,#7512,.T.);
#11120=EDGE_CURVE('',#8487,#8481,#996,.T.);
#11121=EDGE_CURVE('',#8405,#8487,#997,.T.);
#11122=EDGE_CURVE('',#8484,#8441,#998,.T.);
#11123=EDGE_CURVE('',#8488,#8482,#999,.T.);
#11124=EDGE_CURVE('',#8487,#8488,#7513,.T.);
#11125=EDGE_CURVE('',#8442,#8485,#1000,.T.);
#11126=EDGE_CURVE('',#8488,#8406,#1001,.T.);
#11127=EDGE_CURVE('',#8489,#8490,#5474,.T.);
#11128=EDGE_CURVE('',#8489,#8491,#5475,.T.);
#11129=EDGE_CURVE('',#8491,#8492,#5476,.T.);
#11130=EDGE_CURVE('',#8490,#8492,#5477,.T.);
#11131=EDGE_CURVE('',#8493,#8489,#5478,.T.);
#11132=EDGE_CURVE('',#8493,#8494,#5479,.T.);
#11133=EDGE_CURVE('',#8494,#8491,#5480,.T.);
#11134=EDGE_CURVE('',#8495,#8493,#5481,.T.);
#11135=EDGE_CURVE('',#8495,#8496,#5482,.T.);
#11136=EDGE_CURVE('',#8496,#8494,#5483,.T.);
#11137=EDGE_CURVE('',#8497,#8495,#5484,.T.);
#11138=EDGE_CURVE('',#8497,#8498,#5485,.T.);
#11139=EDGE_CURVE('',#8498,#8496,#5486,.T.);
#11140=EDGE_CURVE('',#8499,#8497,#5487,.T.);
#11141=EDGE_CURVE('',#8499,#8500,#5488,.T.);
#11142=EDGE_CURVE('',#8500,#8498,#5489,.T.);
#11143=EDGE_CURVE('',#8490,#8499,#5490,.T.);
#11144=EDGE_CURVE('',#8492,#8500,#5491,.T.);
#11145=EDGE_CURVE('',#8501,#8501,#7514,.T.);
#11146=EDGE_CURVE('',#8501,#8502,#5492,.T.);
#11147=EDGE_CURVE('',#8502,#8502,#7515,.T.);
#15482=ORIENTED_EDGE('',*,*,#10998,.F.);
#15483=ORIENTED_EDGE('',*,*,#10999,.T.);
#15484=ORIENTED_EDGE('',*,*,#11000,.T.);
#15485=ORIENTED_EDGE('',*,*,#11001,.T.);
#15486=ORIENTED_EDGE('',*,*,#11002,.F.);
#15487=ORIENTED_EDGE('',*,*,#11003,.T.);
#15488=ORIENTED_EDGE('',*,*,#10998,.T.);
#15489=ORIENTED_EDGE('',*,*,#11004,.T.);
#15490=ORIENTED_EDGE('',*,*,#11005,.F.);
#15491=ORIENTED_EDGE('',*,*,#11006,.T.);
#15492=ORIENTED_EDGE('',*,*,#11002,.T.);
#15493=ORIENTED_EDGE('',*,*,#11007,.T.);
#15494=ORIENTED_EDGE('',*,*,#11008,.F.);
#15495=ORIENTED_EDGE('',*,*,#11009,.T.);
#15496=ORIENTED_EDGE('',*,*,#11005,.T.);
#15497=ORIENTED_EDGE('',*,*,#11010,.T.);
#15498=ORIENTED_EDGE('',*,*,#11011,.F.);
#15499=ORIENTED_EDGE('',*,*,#11012,.T.);
#15500=ORIENTED_EDGE('',*,*,#11008,.T.);
#15501=ORIENTED_EDGE('',*,*,#11013,.T.);
#15502=ORIENTED_EDGE('',*,*,#11014,.F.);
#15503=ORIENTED_EDGE('',*,*,#11015,.T.);
#15504=ORIENTED_EDGE('',*,*,#11011,.T.);
#15505=ORIENTED_EDGE('',*,*,#11016,.T.);
#15506=ORIENTED_EDGE('',*,*,#11017,.F.);
#15507=ORIENTED_EDGE('',*,*,#11018,.T.);
#15508=ORIENTED_EDGE('',*,*,#11014,.T.);
#15509=ORIENTED_EDGE('',*,*,#11019,.T.);
#15510=ORIENTED_EDGE('',*,*,#11020,.F.);
#15511=ORIENTED_EDGE('',*,*,#11021,.T.);
#15512=ORIENTED_EDGE('',*,*,#11017,.T.);
#15513=ORIENTED_EDGE('',*,*,#11022,.T.);
#15514=ORIENTED_EDGE('',*,*,#11023,.F.);
#15515=ORIENTED_EDGE('',*,*,#11024,.T.);
#15516=ORIENTED_EDGE('',*,*,#11020,.T.);
#15517=ORIENTED_EDGE('',*,*,#11025,.T.);
#15518=ORIENTED_EDGE('',*,*,#11026,.F.);
#15519=ORIENTED_EDGE('',*,*,#11027,.T.);
#15520=ORIENTED_EDGE('',*,*,#11023,.T.);
#15521=ORIENTED_EDGE('',*,*,#11028,.T.);
#15522=ORIENTED_EDGE('',*,*,#11029,.F.);
#15523=ORIENTED_EDGE('',*,*,#11030,.T.);
#15524=ORIENTED_EDGE('',*,*,#11026,.T.);
#15525=ORIENTED_EDGE('',*,*,#11031,.T.);
#15526=ORIENTED_EDGE('',*,*,#11032,.F.);
#15527=ORIENTED_EDGE('',*,*,#11033,.T.);
#15528=ORIENTED_EDGE('',*,*,#11029,.T.);
#15529=ORIENTED_EDGE('',*,*,#11034,.T.);
#15530=ORIENTED_EDGE('',*,*,#11035,.F.);
#15531=ORIENTED_EDGE('',*,*,#11036,.T.);
#15532=ORIENTED_EDGE('',*,*,#11032,.T.);
#15533=ORIENTED_EDGE('',*,*,#11037,.T.);
#15534=ORIENTED_EDGE('',*,*,#11038,.F.);
#15535=ORIENTED_EDGE('',*,*,#11039,.T.);
#15536=ORIENTED_EDGE('',*,*,#11035,.T.);
#15537=ORIENTED_EDGE('',*,*,#11040,.T.);
#15538=ORIENTED_EDGE('',*,*,#11041,.F.);
#15539=ORIENTED_EDGE('',*,*,#11042,.T.);
#15540=ORIENTED_EDGE('',*,*,#11038,.T.);
#15541=ORIENTED_EDGE('',*,*,#11043,.T.);
#15542=ORIENTED_EDGE('',*,*,#11044,.F.);
#15543=ORIENTED_EDGE('',*,*,#11045,.T.);
#15544=ORIENTED_EDGE('',*,*,#11041,.T.);
#15545=ORIENTED_EDGE('',*,*,#11046,.T.);
#15546=ORIENTED_EDGE('',*,*,#11047,.F.);
#15547=ORIENTED_EDGE('',*,*,#11048,.T.);
#15548=ORIENTED_EDGE('',*,*,#11044,.T.);
#15549=ORIENTED_EDGE('',*,*,#11049,.T.);
#15550=ORIENTED_EDGE('',*,*,#11050,.F.);
#15551=ORIENTED_EDGE('',*,*,#11051,.T.);
#15552=ORIENTED_EDGE('',*,*,#11047,.T.);
#15553=ORIENTED_EDGE('',*,*,#11052,.T.);
#15554=ORIENTED_EDGE('',*,*,#11053,.F.);
#15555=ORIENTED_EDGE('',*,*,#11054,.T.);
#15556=ORIENTED_EDGE('',*,*,#11050,.T.);
#15557=ORIENTED_EDGE('',*,*,#11055,.T.);
#15558=ORIENTED_EDGE('',*,*,#11056,.F.);
#15559=ORIENTED_EDGE('',*,*,#11057,.T.);
#15560=ORIENTED_EDGE('',*,*,#11058,.T.);
#15561=ORIENTED_EDGE('',*,*,#11059,.F.);
#15562=ORIENTED_EDGE('',*,*,#11060,.F.);
#15563=ORIENTED_EDGE('',*,*,#11061,.T.);
#15564=ORIENTED_EDGE('',*,*,#11056,.T.);
#15565=ORIENTED_EDGE('',*,*,#11062,.F.);
#15566=ORIENTED_EDGE('',*,*,#11063,.F.);
#15567=ORIENTED_EDGE('',*,*,#11064,.T.);
#15568=ORIENTED_EDGE('',*,*,#11060,.T.);
#15569=ORIENTED_EDGE('',*,*,#11065,.F.);
#15570=ORIENTED_EDGE('',*,*,#11066,.F.);
#15571=ORIENTED_EDGE('',*,*,#11067,.T.);
#15572=ORIENTED_EDGE('',*,*,#11063,.T.);
#15573=ORIENTED_EDGE('',*,*,#11068,.F.);
#15574=ORIENTED_EDGE('',*,*,#11069,.F.);
#15575=ORIENTED_EDGE('',*,*,#11070,.T.);
#15576=ORIENTED_EDGE('',*,*,#11066,.T.);
#15577=ORIENTED_EDGE('',*,*,#11071,.F.);
#15578=ORIENTED_EDGE('',*,*,#11072,.F.);
#15579=ORIENTED_EDGE('',*,*,#11073,.T.);
#15580=ORIENTED_EDGE('',*,*,#11069,.T.);
#15581=ORIENTED_EDGE('',*,*,#11074,.F.);
#15582=ORIENTED_EDGE('',*,*,#11075,.F.);
#15583=ORIENTED_EDGE('',*,*,#11076,.T.);
#15584=ORIENTED_EDGE('',*,*,#11072,.T.);
#15585=ORIENTED_EDGE('',*,*,#11077,.F.);
#15586=ORIENTED_EDGE('',*,*,#11078,.F.);
#15587=ORIENTED_EDGE('',*,*,#11079,.T.);
#15588=ORIENTED_EDGE('',*,*,#11075,.T.);
#15589=ORIENTED_EDGE('',*,*,#11080,.F.);
#15590=ORIENTED_EDGE('',*,*,#11081,.F.);
#15591=ORIENTED_EDGE('',*,*,#11082,.T.);
#15592=ORIENTED_EDGE('',*,*,#11078,.T.);
#15593=ORIENTED_EDGE('',*,*,#11083,.F.);
#15594=ORIENTED_EDGE('',*,*,#11084,.F.);
#15595=ORIENTED_EDGE('',*,*,#11085,.T.);
#15596=ORIENTED_EDGE('',*,*,#11081,.T.);
#15597=ORIENTED_EDGE('',*,*,#11086,.F.);
#15598=ORIENTED_EDGE('',*,*,#11087,.F.);
#15599=ORIENTED_EDGE('',*,*,#11088,.T.);
#15600=ORIENTED_EDGE('',*,*,#11084,.T.);
#15601=ORIENTED_EDGE('',*,*,#11089,.F.);
#15602=ORIENTED_EDGE('',*,*,#11090,.F.);
#15603=ORIENTED_EDGE('',*,*,#11091,.T.);
#15604=ORIENTED_EDGE('',*,*,#11087,.T.);
#15605=ORIENTED_EDGE('',*,*,#11092,.F.);
#15606=ORIENTED_EDGE('',*,*,#11093,.F.);
#15607=ORIENTED_EDGE('',*,*,#11094,.T.);
#15608=ORIENTED_EDGE('',*,*,#11090,.T.);
#15609=ORIENTED_EDGE('',*,*,#11095,.F.);
#15610=ORIENTED_EDGE('',*,*,#11096,.F.);
#15611=ORIENTED_EDGE('',*,*,#11097,.T.);
#15612=ORIENTED_EDGE('',*,*,#11093,.T.);
#15613=ORIENTED_EDGE('',*,*,#11098,.F.);
#15614=ORIENTED_EDGE('',*,*,#11099,.F.);
#15615=ORIENTED_EDGE('',*,*,#11100,.T.);
#15616=ORIENTED_EDGE('',*,*,#11096,.T.);
#15617=ORIENTED_EDGE('',*,*,#11101,.F.);
#15618=ORIENTED_EDGE('',*,*,#11102,.F.);
#15619=ORIENTED_EDGE('',*,*,#11103,.T.);
#15620=ORIENTED_EDGE('',*,*,#11099,.T.);
#15621=ORIENTED_EDGE('',*,*,#11104,.F.);
#15622=ORIENTED_EDGE('',*,*,#11105,.F.);
#15623=ORIENTED_EDGE('',*,*,#11106,.T.);
#15624=ORIENTED_EDGE('',*,*,#11102,.T.);
#15625=ORIENTED_EDGE('',*,*,#11107,.F.);
#15626=ORIENTED_EDGE('',*,*,#11108,.F.);
#15627=ORIENTED_EDGE('',*,*,#11109,.T.);
#15628=ORIENTED_EDGE('',*,*,#11105,.T.);
#15629=ORIENTED_EDGE('',*,*,#11110,.F.);
#15630=ORIENTED_EDGE('',*,*,#11111,.F.);
#15631=ORIENTED_EDGE('',*,*,#11112,.T.);
#15632=ORIENTED_EDGE('',*,*,#11108,.T.);
#15633=ORIENTED_EDGE('',*,*,#11113,.F.);
#15634=ORIENTED_EDGE('',*,*,#11114,.F.);
#15635=ORIENTED_EDGE('',*,*,#11058,.F.);
#15636=ORIENTED_EDGE('',*,*,#11115,.F.);
#15637=ORIENTED_EDGE('',*,*,#11116,.F.);
#15638=ORIENTED_EDGE('',*,*,#11117,.F.);
#15639=ORIENTED_EDGE('',*,*,#11118,.T.);
#15640=ORIENTED_EDGE('',*,*,#11119,.F.);
#15641=ORIENTED_EDGE('',*,*,#11118,.F.);
#15642=ORIENTED_EDGE('',*,*,#11115,.T.);
#15643=ORIENTED_EDGE('',*,*,#11057,.F.);
#15644=ORIENTED_EDGE('',*,*,#11061,.F.);
#15645=ORIENTED_EDGE('',*,*,#11064,.F.);
#15646=ORIENTED_EDGE('',*,*,#11067,.F.);
#15647=ORIENTED_EDGE('',*,*,#11070,.F.);
#15648=ORIENTED_EDGE('',*,*,#11073,.F.);
#15649=ORIENTED_EDGE('',*,*,#11076,.F.);
#15650=ORIENTED_EDGE('',*,*,#11079,.F.);
#15651=ORIENTED_EDGE('',*,*,#11082,.F.);
#15652=ORIENTED_EDGE('',*,*,#11085,.F.);
#15653=ORIENTED_EDGE('',*,*,#11088,.F.);
#15654=ORIENTED_EDGE('',*,*,#11091,.F.);
#15655=ORIENTED_EDGE('',*,*,#11094,.F.);
#15656=ORIENTED_EDGE('',*,*,#11097,.F.);
#15657=ORIENTED_EDGE('',*,*,#11100,.F.);
#15658=ORIENTED_EDGE('',*,*,#11103,.F.);
#15659=ORIENTED_EDGE('',*,*,#11106,.F.);
#15660=ORIENTED_EDGE('',*,*,#11109,.F.);
#15661=ORIENTED_EDGE('',*,*,#11112,.F.);
#15662=ORIENTED_EDGE('',*,*,#11120,.F.);
#15663=ORIENTED_EDGE('',*,*,#11121,.F.);
#15664=ORIENTED_EDGE('',*,*,#10999,.F.);
#15665=ORIENTED_EDGE('',*,*,#11003,.F.);
#15666=ORIENTED_EDGE('',*,*,#11006,.F.);
#15667=ORIENTED_EDGE('',*,*,#11009,.F.);
#15668=ORIENTED_EDGE('',*,*,#11012,.F.);
#15669=ORIENTED_EDGE('',*,*,#11015,.F.);
#15670=ORIENTED_EDGE('',*,*,#11018,.F.);
#15671=ORIENTED_EDGE('',*,*,#11021,.F.);
#15672=ORIENTED_EDGE('',*,*,#11024,.F.);
#15673=ORIENTED_EDGE('',*,*,#11027,.F.);
#15674=ORIENTED_EDGE('',*,*,#11030,.F.);
#15675=ORIENTED_EDGE('',*,*,#11033,.F.);
#15676=ORIENTED_EDGE('',*,*,#11036,.F.);
#15677=ORIENTED_EDGE('',*,*,#11039,.F.);
#15678=ORIENTED_EDGE('',*,*,#11042,.F.);
#15679=ORIENTED_EDGE('',*,*,#11045,.F.);
#15680=ORIENTED_EDGE('',*,*,#11048,.F.);
#15681=ORIENTED_EDGE('',*,*,#11051,.F.);
#15682=ORIENTED_EDGE('',*,*,#11054,.F.);
#15683=ORIENTED_EDGE('',*,*,#11122,.F.);
#15684=ORIENTED_EDGE('',*,*,#11111,.T.);
#15685=ORIENTED_EDGE('',*,*,#11123,.F.);
#15686=ORIENTED_EDGE('',*,*,#11124,.F.);
#15687=ORIENTED_EDGE('',*,*,#11120,.T.);
#15688=ORIENTED_EDGE('',*,*,#11114,.T.);
#15689=ORIENTED_EDGE('',*,*,#11117,.T.);
#15690=ORIENTED_EDGE('',*,*,#11125,.F.);
#15691=ORIENTED_EDGE('',*,*,#11055,.F.);
#15692=ORIENTED_EDGE('',*,*,#11052,.F.);
#15693=ORIENTED_EDGE('',*,*,#11049,.F.);
#15694=ORIENTED_EDGE('',*,*,#11046,.F.);
#15695=ORIENTED_EDGE('',*,*,#11043,.F.);
#15696=ORIENTED_EDGE('',*,*,#11040,.F.);
#15697=ORIENTED_EDGE('',*,*,#11037,.F.);
#15698=ORIENTED_EDGE('',*,*,#11034,.F.);
#15699=ORIENTED_EDGE('',*,*,#11031,.F.);
#15700=ORIENTED_EDGE('',*,*,#11028,.F.);
#15701=ORIENTED_EDGE('',*,*,#11025,.F.);
#15702=ORIENTED_EDGE('',*,*,#11022,.F.);
#15703=ORIENTED_EDGE('',*,*,#11019,.F.);
#15704=ORIENTED_EDGE('',*,*,#11016,.F.);
#15705=ORIENTED_EDGE('',*,*,#11013,.F.);
#15706=ORIENTED_EDGE('',*,*,#11010,.F.);
#15707=ORIENTED_EDGE('',*,*,#11007,.F.);
#15708=ORIENTED_EDGE('',*,*,#11004,.F.);
#15709=ORIENTED_EDGE('',*,*,#11001,.F.);
#15710=ORIENTED_EDGE('',*,*,#11126,.F.);
#15711=ORIENTED_EDGE('',*,*,#11123,.T.);
#15712=ORIENTED_EDGE('',*,*,#11113,.T.);
#15713=ORIENTED_EDGE('',*,*,#11110,.T.);
#15714=ORIENTED_EDGE('',*,*,#11107,.T.);
#15715=ORIENTED_EDGE('',*,*,#11104,.T.);
#15716=ORIENTED_EDGE('',*,*,#11101,.T.);
#15717=ORIENTED_EDGE('',*,*,#11098,.T.);
#15718=ORIENTED_EDGE('',*,*,#11095,.T.);
#15719=ORIENTED_EDGE('',*,*,#11092,.T.);
#15720=ORIENTED_EDGE('',*,*,#11089,.T.);
#15721=ORIENTED_EDGE('',*,*,#11086,.T.);
#15722=ORIENTED_EDGE('',*,*,#11083,.T.);
#15723=ORIENTED_EDGE('',*,*,#11080,.T.);
#15724=ORIENTED_EDGE('',*,*,#11077,.T.);
#15725=ORIENTED_EDGE('',*,*,#11074,.T.);
#15726=ORIENTED_EDGE('',*,*,#11071,.T.);
#15727=ORIENTED_EDGE('',*,*,#11068,.T.);
#15728=ORIENTED_EDGE('',*,*,#11065,.T.);
#15729=ORIENTED_EDGE('',*,*,#11062,.T.);
#15730=ORIENTED_EDGE('',*,*,#11059,.T.);
#15731=ORIENTED_EDGE('',*,*,#11053,.T.);
#15732=ORIENTED_EDGE('',*,*,#11125,.T.);
#15733=ORIENTED_EDGE('',*,*,#11116,.T.);
#15734=ORIENTED_EDGE('',*,*,#11122,.T.);
#15735=ORIENTED_EDGE('',*,*,#11127,.F.);
#15736=ORIENTED_EDGE('',*,*,#11128,.T.);
#15737=ORIENTED_EDGE('',*,*,#11129,.T.);
#15738=ORIENTED_EDGE('',*,*,#11130,.F.);
#15739=ORIENTED_EDGE('',*,*,#11131,.F.);
#15740=ORIENTED_EDGE('',*,*,#11132,.T.);
#15741=ORIENTED_EDGE('',*,*,#11133,.T.);
#15742=ORIENTED_EDGE('',*,*,#11128,.F.);
#15743=ORIENTED_EDGE('',*,*,#11134,.F.);
#15744=ORIENTED_EDGE('',*,*,#11135,.T.);
#15745=ORIENTED_EDGE('',*,*,#11136,.T.);
#15746=ORIENTED_EDGE('',*,*,#11132,.F.);
#15747=ORIENTED_EDGE('',*,*,#11137,.F.);
#15748=ORIENTED_EDGE('',*,*,#11138,.T.);
#15749=ORIENTED_EDGE('',*,*,#11139,.T.);
#15750=ORIENTED_EDGE('',*,*,#11135,.F.);
#15751=ORIENTED_EDGE('',*,*,#11140,.F.);
#15752=ORIENTED_EDGE('',*,*,#11141,.T.);
#15753=ORIENTED_EDGE('',*,*,#11142,.T.);
#15754=ORIENTED_EDGE('',*,*,#11138,.F.);
#15755=ORIENTED_EDGE('',*,*,#11143,.F.);
#15756=ORIENTED_EDGE('',*,*,#11130,.T.);
#15757=ORIENTED_EDGE('',*,*,#11144,.T.);
#15758=ORIENTED_EDGE('',*,*,#11141,.F.);
#15759=ORIENTED_EDGE('',*,*,#11144,.F.);
#15760=ORIENTED_EDGE('',*,*,#11129,.F.);
#15761=ORIENTED_EDGE('',*,*,#11133,.F.);
#15762=ORIENTED_EDGE('',*,*,#11136,.F.);
#15763=ORIENTED_EDGE('',*,*,#11139,.F.);
#15764=ORIENTED_EDGE('',*,*,#11142,.F.);
#15765=ORIENTED_EDGE('',*,*,#11145,.T.);
#15766=ORIENTED_EDGE('',*,*,#11121,.T.);
#15767=ORIENTED_EDGE('',*,*,#11124,.T.);
#15768=ORIENTED_EDGE('',*,*,#11126,.T.);
#15769=ORIENTED_EDGE('',*,*,#11000,.F.);
#15770=ORIENTED_EDGE('',*,*,#11145,.F.);
#15771=ORIENTED_EDGE('',*,*,#11146,.T.);
#15772=ORIENTED_EDGE('',*,*,#11147,.T.);
#15773=ORIENTED_EDGE('',*,*,#11146,.F.);
#15774=ORIENTED_EDGE('',*,*,#11147,.F.);
#15775=ORIENTED_EDGE('',*,*,#11127,.T.);
#15776=ORIENTED_EDGE('',*,*,#11143,.T.);
#15777=ORIENTED_EDGE('',*,*,#11140,.T.);
#15778=ORIENTED_EDGE('',*,*,#11137,.T.);
#15779=ORIENTED_EDGE('',*,*,#11134,.T.);
#15780=ORIENTED_EDGE('',*,*,#11131,.T.);
#15781=ORIENTED_EDGE('',*,*,#11119,.T.);
#20022=CYLINDRICAL_SURFACE('',#22636,4.942);
#20023=CYLINDRICAL_SURFACE('',#22638,4.942);
#20024=CYLINDRICAL_SURFACE('',#22639,4.942);
#20025=CYLINDRICAL_SURFACE('',#22640,4.942);
#20026=CYLINDRICAL_SURFACE('',#22641,4.942);
#20027=CYLINDRICAL_SURFACE('',#22642,4.942);
#20028=CYLINDRICAL_SURFACE('',#22643,4.942);
#20029=CYLINDRICAL_SURFACE('',#22644,4.942);
#20030=CYLINDRICAL_SURFACE('',#22645,4.942);
#20031=CYLINDRICAL_SURFACE('',#22646,4.942);
#20032=CYLINDRICAL_SURFACE('',#22647,4.942);
#20033=CYLINDRICAL_SURFACE('',#22648,4.942);
#20034=CYLINDRICAL_SURFACE('',#22649,4.942);
#20035=CYLINDRICAL_SURFACE('',#22650,4.942);
#20036=CYLINDRICAL_SURFACE('',#22651,4.942);
#20037=CYLINDRICAL_SURFACE('',#22652,4.942);
#20038=CYLINDRICAL_SURFACE('',#22653,4.942);
#20039=CYLINDRICAL_SURFACE('',#22654,4.942);
#20040=CYLINDRICAL_SURFACE('',#22655,4.942);
#20041=CYLINDRICAL_SURFACE('',#22656,4.372);
#20042=CYLINDRICAL_SURFACE('',#22658,4.372);
#20043=CYLINDRICAL_SURFACE('',#22659,4.372);
#20044=CYLINDRICAL_SURFACE('',#22660,4.372);
#20045=CYLINDRICAL_SURFACE('',#22661,4.372);
#20046=CYLINDRICAL_SURFACE('',#22662,4.372);
#20047=CYLINDRICAL_SURFACE('',#22663,4.372);
#20048=CYLINDRICAL_SURFACE('',#22664,4.372);
#20049=CYLINDRICAL_SURFACE('',#22665,4.372);
#20050=CYLINDRICAL_SURFACE('',#22666,4.372);
#20051=CYLINDRICAL_SURFACE('',#22667,4.372);
#20052=CYLINDRICAL_SURFACE('',#22668,4.372);
#20053=CYLINDRICAL_SURFACE('',#22669,4.372);
#20054=CYLINDRICAL_SURFACE('',#22670,4.372);
#20055=CYLINDRICAL_SURFACE('',#22671,4.372);
#20056=CYLINDRICAL_SURFACE('',#22672,4.372);
#20057=CYLINDRICAL_SURFACE('',#22673,4.372);
#20058=CYLINDRICAL_SURFACE('',#22674,4.372);
#20059=CYLINDRICAL_SURFACE('',#22675,4.372);
#20060=CYLINDRICAL_SURFACE('',#22679,4.372);
#20061=CYLINDRICAL_SURFACE('',#22681,4.942);
#20062=CYLINDRICAL_SURFACE('',#22691,8.);
#21071=ADVANCED_FACE('',(#2951),#20022,.T.);
#21072=ADVANCED_FACE('',(#2952),#20023,.T.);
#21073=ADVANCED_FACE('',(#2953),#20024,.T.);
#21074=ADVANCED_FACE('',(#2954),#20025,.T.);
#21075=ADVANCED_FACE('',(#2955),#20026,.T.);
#21076=ADVANCED_FACE('',(#2956),#20027,.T.);
#21077=ADVANCED_FACE('',(#2957),#20028,.T.);
#21078=ADVANCED_FACE('',(#2958),#20029,.T.);
#21079=ADVANCED_FACE('',(#2959),#20030,.T.);
#21080=ADVANCED_FACE('',(#2960),#20031,.T.);
#21081=ADVANCED_FACE('',(#2961),#20032,.T.);
#21082=ADVANCED_FACE('',(#2962),#20033,.T.);
#21083=ADVANCED_FACE('',(#2963),#20034,.T.);
#21084=ADVANCED_FACE('',(#2964),#20035,.T.);
#21085=ADVANCED_FACE('',(#2965),#20036,.T.);
#21086=ADVANCED_FACE('',(#2966),#20037,.T.);
#21087=ADVANCED_FACE('',(#2967),#20038,.T.);
#21088=ADVANCED_FACE('',(#2968),#20039,.T.);
#21089=ADVANCED_FACE('',(#2969),#20040,.T.);
#21090=ADVANCED_FACE('',(#2970),#20041,.T.);
#21091=ADVANCED_FACE('',(#2971),#20042,.T.);
#21092=ADVANCED_FACE('',(#2972),#20043,.T.);
#21093=ADVANCED_FACE('',(#2973),#20044,.T.);
#21094=ADVANCED_FACE('',(#2974),#20045,.T.);
#21095=ADVANCED_FACE('',(#2975),#20046,.T.);
#21096=ADVANCED_FACE('',(#2976),#20047,.T.);
#21097=ADVANCED_FACE('',(#2977),#20048,.T.);
#21098=ADVANCED_FACE('',(#2978),#20049,.T.);
#21099=ADVANCED_FACE('',(#2979),#20050,.T.);
#21100=ADVANCED_FACE('',(#2980),#20051,.T.);
#21101=ADVANCED_FACE('',(#2981),#20052,.T.);
#21102=ADVANCED_FACE('',(#2982),#20053,.T.);
#21103=ADVANCED_FACE('',(#2983),#20054,.T.);
#21104=ADVANCED_FACE('',(#2984),#20055,.T.);
#21105=ADVANCED_FACE('',(#2985),#20056,.T.);
#21106=ADVANCED_FACE('',(#2986),#20057,.T.);
#21107=ADVANCED_FACE('',(#2987),#20058,.T.);
#21108=ADVANCED_FACE('',(#2988),#20059,.T.);
#21109=ADVANCED_FACE('',(#2989),#331,.T.);
#21110=ADVANCED_FACE('',(#2990),#348,.F.);
#21111=ADVANCED_FACE('',(#2991),#20060,.T.);
#21112=ADVANCED_FACE('',(#2992),#349,.F.);
#21113=ADVANCED_FACE('',(#2993),#20061,.T.);
#21114=ADVANCED_FACE('',(#2994),#2466,.F.);
#21115=ADVANCED_FACE('',(#2995),#2467,.F.);
#21116=ADVANCED_FACE('',(#2996),#2468,.F.);
#21117=ADVANCED_FACE('',(#2997),#2469,.F.);
#21118=ADVANCED_FACE('',(#2998),#2470,.F.);
#21119=ADVANCED_FACE('',(#2999),#2471,.F.);
#21120=ADVANCED_FACE('',(#3000),#2472,.F.);
#21121=ADVANCED_FACE('',(#3001,#2339),#2473,.T.);
#21122=ADVANCED_FACE('',(#3002),#20062,.T.);
#21123=ADVANCED_FACE('',(#3003,#2340),#2474,.F.);
#21124=ADVANCED_FACE('',(#3004),#2475,.T.);
#21818=CLOSED_SHELL('',(#21071,#21072,#21073,#21074,#21075,#21076,#21077,
#21078,#21079,#21080,#21081,#21082,#21083,#21084,#21085,#21086,#21087,#21088,
#21089,#21090,#21091,#21092,#21093,#21094,#21095,#21096,#21097,#21098,#21099,
#21100,#21101,#21102,#21103,#21104,#21105,#21106,#21107,#21108,#21109,#21110,
#21111,#21112,#21113,#21114,#21115,#21116,#21117,#21118,#21119,#21120,#21121,
#21122,#21123,#21124));
#22635=AXIS2_PLACEMENT_3D('',#53330,#25191,#25192);
#22636=AXIS2_PLACEMENT_3D('',#53331,#25193,#25194);
#22637=AXIS2_PLACEMENT_3D('',#53347,#25196,#25197);
#22638=AXIS2_PLACEMENT_3D('',#53358,#25198,#25199);
#22639=AXIS2_PLACEMENT_3D('',#53406,#25201,#25202);
#22640=AXIS2_PLACEMENT_3D('',#53454,#25204,#25205);
#22641=AXIS2_PLACEMENT_3D('',#53508,#25207,#25208);
#22642=AXIS2_PLACEMENT_3D('',#53556,#25210,#25211);
#22643=AXIS2_PLACEMENT_3D('',#53604,#25213,#25214);
#22644=AXIS2_PLACEMENT_3D('',#53658,#25216,#25217);
#22645=AXIS2_PLACEMENT_3D('',#53706,#25219,#25220);
#22646=AXIS2_PLACEMENT_3D('',#53754,#25222,#25223);
#22647=AXIS2_PLACEMENT_3D('',#53802,#25225,#25226);
#22648=AXIS2_PLACEMENT_3D('',#53856,#25228,#25229);
#22649=AXIS2_PLACEMENT_3D('',#53904,#25231,#25232);
#22650=AXIS2_PLACEMENT_3D('',#53952,#25234,#25235);
#22651=AXIS2_PLACEMENT_3D('',#54006,#25237,#25238);
#22652=AXIS2_PLACEMENT_3D('',#54054,#25240,#25241);
#22653=AXIS2_PLACEMENT_3D('',#54102,#25243,#25244);
#22654=AXIS2_PLACEMENT_3D('',#54156,#25246,#25247);
#22655=AXIS2_PLACEMENT_3D('',#54204,#25249,#25250);
#22656=AXIS2_PLACEMENT_3D('',#54252,#25252,#25253);
#22657=AXIS2_PLACEMENT_3D('',#54269,#25255,#25256);
#22658=AXIS2_PLACEMENT_3D('',#54279,#25257,#25258);
#22659=AXIS2_PLACEMENT_3D('',#54304,#25260,#25261);
#22660=AXIS2_PLACEMENT_3D('',#54328,#25263,#25264);
#22661=AXIS2_PLACEMENT_3D('',#54353,#25266,#25267);
#22662=AXIS2_PLACEMENT_3D('',#54378,#25269,#25270);
#22663=AXIS2_PLACEMENT_3D('',#54402,#25272,#25273);
#22664=AXIS2_PLACEMENT_3D('',#54427,#25275,#25276);
#22665=AXIS2_PLACEMENT_3D('',#54452,#25278,#25279);
#22666=AXIS2_PLACEMENT_3D('',#54476,#25281,#25282);
#22667=AXIS2_PLACEMENT_3D('',#54501,#25284,#25285);
#22668=AXIS2_PLACEMENT_3D('',#54526,#25287,#25288);
#22669=AXIS2_PLACEMENT_3D('',#54550,#25290,#25291);
#22670=AXIS2_PLACEMENT_3D('',#54574,#25293,#25294);
#22671=AXIS2_PLACEMENT_3D('',#54599,#25296,#25297);
#22672=AXIS2_PLACEMENT_3D('',#54624,#25299,#25300);
#22673=AXIS2_PLACEMENT_3D('',#54648,#25302,#25303);
#22674=AXIS2_PLACEMENT_3D('',#54673,#25305,#25306);
#22675=AXIS2_PLACEMENT_3D('',#54698,#25308,#25309);
#22676=AXIS2_PLACEMENT_3D('',#54722,#25311,#25312);
#22677=AXIS2_PLACEMENT_3D('',#55043,#25313,#25314);
#22678=AXIS2_PLACEMENT_3D('',#55083,#25316,#25317);
#22679=AXIS2_PLACEMENT_3D('',#55732,#25318,#25319);
#22680=AXIS2_PLACEMENT_3D('',#55743,#25320,#25321);
#22681=AXIS2_PLACEMENT_3D('',#56396,#25322,#25323);
#22682=AXIS2_PLACEMENT_3D('',#56397,#25324,#25325);
#22683=AXIS2_PLACEMENT_3D('',#56406,#25330,#25331);
#22684=AXIS2_PLACEMENT_3D('',#56412,#25335,#25336);
#22685=AXIS2_PLACEMENT_3D('',#56418,#25340,#25341);
#22686=AXIS2_PLACEMENT_3D('',#56424,#25345,#25346);
#22687=AXIS2_PLACEMENT_3D('',#56430,#25350,#25351);
#22688=AXIS2_PLACEMENT_3D('',#56433,#25354,#25355);
#22689=AXIS2_PLACEMENT_3D('',#56434,#25356,#25357);
#22690=AXIS2_PLACEMENT_3D('',#56436,#25358,#25359);
#22691=AXIS2_PLACEMENT_3D('',#56437,#25360,#25361);
#22692=AXIS2_PLACEMENT_3D('',#56440,#25363,#25364);
#22693=AXIS2_PLACEMENT_3D('',#56441,#25365,#25366);
#22694=AXIS2_PLACEMENT_3D('',#56442,#25367,#25368);
#25191=DIRECTION('axis',(0.,0.,1.));
#25192=DIRECTION('refdir',(1.,0.,0.));
#25193=DIRECTION('center_axis',(0.,0.,1.));
#25194=DIRECTION('ref_axis',(1.,0.,0.));
#25195=DIRECTION('',(0.,0.,-1.));
#25196=DIRECTION('center_axis',(0.,0.,-1.));
#25197=DIRECTION('ref_axis',(1.,0.,0.));
#25198=DIRECTION('center_axis',(0.,0.,1.));
#25199=DIRECTION('ref_axis',(1.,0.,0.));
#25200=DIRECTION('',(0.,0.,-1.));
#25201=DIRECTION('center_axis',(0.,0.,1.));
#25202=DIRECTION('ref_axis',(1.,0.,0.));
#25203=DIRECTION('',(0.,0.,-1.));
#25204=DIRECTION('center_axis',(0.,0.,1.));
#25205=DIRECTION('ref_axis',(1.,0.,0.));
#25206=DIRECTION('',(0.,0.,-1.));
#25207=DIRECTION('center_axis',(0.,0.,1.));
#25208=DIRECTION('ref_axis',(1.,0.,0.));
#25209=DIRECTION('',(0.,0.,-1.));
#25210=DIRECTION('center_axis',(0.,0.,1.));
#25211=DIRECTION('ref_axis',(1.,0.,0.));
#25212=DIRECTION('',(0.,0.,-1.));
#25213=DIRECTION('center_axis',(0.,0.,1.));
#25214=DIRECTION('ref_axis',(1.,0.,0.));
#25215=DIRECTION('',(0.,0.,-1.));
#25216=DIRECTION('center_axis',(0.,0.,1.));
#25217=DIRECTION('ref_axis',(1.,0.,0.));
#25218=DIRECTION('',(0.,0.,-1.));
#25219=DIRECTION('center_axis',(0.,0.,1.));
#25220=DIRECTION('ref_axis',(1.,0.,0.));
#25221=DIRECTION('',(0.,0.,-1.));
#25222=DIRECTION('center_axis',(0.,0.,1.));
#25223=DIRECTION('ref_axis',(1.,0.,0.));
#25224=DIRECTION('',(0.,0.,-1.));
#25225=DIRECTION('center_axis',(0.,0.,1.));
#25226=DIRECTION('ref_axis',(1.,0.,0.));
#25227=DIRECTION('',(0.,0.,-1.));
#25228=DIRECTION('center_axis',(0.,0.,1.));
#25229=DIRECTION('ref_axis',(1.,0.,0.));
#25230=DIRECTION('',(0.,0.,-1.));
#25231=DIRECTION('center_axis',(0.,0.,1.));
#25232=DIRECTION('ref_axis',(1.,0.,0.));
#25233=DIRECTION('',(0.,0.,-1.));
#25234=DIRECTION('center_axis',(0.,0.,1.));
#25235=DIRECTION('ref_axis',(1.,0.,0.));
#25236=DIRECTION('',(0.,0.,-1.));
#25237=DIRECTION('center_axis',(0.,0.,1.));
#25238=DIRECTION('ref_axis',(1.,0.,0.));
#25239=DIRECTION('',(0.,0.,-1.));
#25240=DIRECTION('center_axis',(0.,0.,1.));
#25241=DIRECTION('ref_axis',(1.,0.,0.));
#25242=DIRECTION('',(0.,0.,-1.));
#25243=DIRECTION('center_axis',(0.,0.,1.));
#25244=DIRECTION('ref_axis',(1.,0.,0.));
#25245=DIRECTION('',(0.,0.,-1.));
#25246=DIRECTION('center_axis',(0.,0.,1.));
#25247=DIRECTION('ref_axis',(1.,0.,0.));
#25248=DIRECTION('',(0.,0.,-1.));
#25249=DIRECTION('center_axis',(0.,0.,1.));
#25250=DIRECTION('ref_axis',(1.,0.,0.));
#25251=DIRECTION('',(0.,0.,-1.));
#25252=DIRECTION('center_axis',(0.,0.,1.));
#25253=DIRECTION('ref_axis',(0.997281310794726,-0.0736884464455154,0.));
#25254=DIRECTION('',(0.,0.,1.));
#25255=DIRECTION('center_axis',(0.,0.,-1.));
#25256=DIRECTION('ref_axis',(1.,1.00674340327557E-13,0.));
#25257=DIRECTION('center_axis',(0.,0.,1.));
#25258=DIRECTION('ref_axis',(1.,1.00674340327557E-13,0.));
#25259=DIRECTION('',(0.,0.,1.));
#25260=DIRECTION('center_axis',(0.,0.,1.));
#25261=DIRECTION('ref_axis',(1.,1.00674340327557E-13,0.));
#25262=DIRECTION('',(0.,0.,1.));
#25263=DIRECTION('center_axis',(0.,0.,1.));
#25264=DIRECTION('ref_axis',(1.,1.00674340327557E-13,0.));
#25265=DIRECTION('',(0.,0.,1.));
#25266=DIRECTION('center_axis',(0.,0.,1.));
#25267=DIRECTION('ref_axis',(1.,1.00674340327557E-13,0.));
#25268=DIRECTION('',(0.,0.,1.));
#25269=DIRECTION('center_axis',(0.,0.,1.));
#25270=DIRECTION('ref_axis',(1.,1.00674340327557E-13,0.));
#25271=DIRECTION('',(0.,0.,1.));
#25272=DIRECTION('center_axis',(0.,0.,1.));
#25273=DIRECTION('ref_axis',(1.,1.00674340327557E-13,0.));
#25274=DIRECTION('',(0.,0.,1.));
#25275=DIRECTION('center_axis',(0.,0.,1.));
#25276=DIRECTION('ref_axis',(1.,1.00674340327557E-13,0.));
#25277=DIRECTION('',(0.,0.,1.));
#25278=DIRECTION('center_axis',(0.,0.,1.));
#25279=DIRECTION('ref_axis',(1.,1.00674340327557E-13,0.));
#25280=DIRECTION('',(0.,0.,1.));
#25281=DIRECTION('center_axis',(0.,0.,1.));
#25282=DIRECTION('ref_axis',(1.,1.00674340327557E-13,0.));
#25283=DIRECTION('',(0.,0.,1.));
#25284=DIRECTION('center_axis',(0.,0.,1.));
#25285=DIRECTION('ref_axis',(1.,1.00674340327557E-13,0.));
#25286=DIRECTION('',(0.,0.,1.));
#25287=DIRECTION('center_axis',(0.,0.,1.));
#25288=DIRECTION('ref_axis',(1.,1.00674340327557E-13,0.));
#25289=DIRECTION('',(0.,0.,1.));
#25290=DIRECTION('center_axis',(0.,0.,1.));
#25291=DIRECTION('ref_axis',(1.,1.00674340327557E-13,0.));
#25292=DIRECTION('',(0.,0.,1.));
#25293=DIRECTION('center_axis',(0.,0.,1.));
#25294=DIRECTION('ref_axis',(1.,1.00674340327557E-13,0.));
#25295=DIRECTION('',(0.,0.,1.));
#25296=DIRECTION('center_axis',(0.,0.,1.));
#25297=DIRECTION('ref_axis',(1.,1.00674340327557E-13,0.));
#25298=DIRECTION('',(0.,0.,1.));
#25299=DIRECTION('center_axis',(0.,0.,1.));
#25300=DIRECTION('ref_axis',(1.,1.00674340327557E-13,0.));
#25301=DIRECTION('',(0.,0.,1.));
#25302=DIRECTION('center_axis',(0.,0.,1.));
#25303=DIRECTION('ref_axis',(1.,1.00674340327557E-13,0.));
#25304=DIRECTION('',(0.,0.,1.));
#25305=DIRECTION('center_axis',(0.,0.,1.));
#25306=DIRECTION('ref_axis',(1.,1.00674340327557E-13,0.));
#25307=DIRECTION('',(0.,0.,1.));
#25308=DIRECTION('center_axis',(0.,0.,1.));
#25309=DIRECTION('ref_axis',(1.,1.00674340327557E-13,0.));
#25310=DIRECTION('',(0.,0.,1.));
#25311=DIRECTION('center_axis',(0.,0.,-1.));
#25312=DIRECTION('ref_axis',(1.,0.,0.));
#25313=DIRECTION('center_axis',(0.,0.,-1.));
#25314=DIRECTION('ref_axis',(1.,0.,0.));
#25315=DIRECTION('',(0.707106781186547,8.65956056235493E-17,0.707106781186548));
#25316=DIRECTION('center_axis',(0.,0.,1.));
#25317=DIRECTION('ref_axis',(1.,0.,0.));
#25318=DIRECTION('center_axis',(0.,0.,1.));
#25319=DIRECTION('ref_axis',(1.,1.00674340327557E-13,0.));
#25320=DIRECTION('center_axis',(0.,0.,-1.));
#25321=DIRECTION('ref_axis',(1.,1.00674340327557E-13,0.));
#25322=DIRECTION('center_axis',(0.,0.,1.));
#25323=DIRECTION('ref_axis',(1.,0.,0.));
#25324=DIRECTION('center_axis',(-2.40370335797945E-16,-1.,0.));
#25325=DIRECTION('ref_axis',(1.,-2.40370335797945E-16,0.));
#25326=DIRECTION('',(1.,-2.40370335797945E-16,0.));
#25327=DIRECTION('',(0.,0.,1.));
#25328=DIRECTION('',(1.,-2.40370335797945E-16,0.));
#25329=DIRECTION('',(0.,0.,1.));
#25330=DIRECTION('center_axis',(-0.866025403784439,-0.5,0.));
#25331=DIRECTION('ref_axis',(0.5,-0.866025403784439,0.));
#25332=DIRECTION('',(0.5,-0.866025403784439,0.));
#25333=DIRECTION('',(0.,0.,1.));
#25334=DIRECTION('',(0.5,-0.866025403784439,0.));
#25335=DIRECTION('center_axis',(-0.866025403784439,0.5,0.));
#25336=DIRECTION('ref_axis',(-0.5,-0.866025403784439,0.));
#25337=DIRECTION('',(-0.5,-0.866025403784439,0.));
#25338=DIRECTION('',(0.,0.,1.));
#25339=DIRECTION('',(-0.5,-0.866025403784439,0.));
#25340=DIRECTION('center_axis',(1.20185167898973E-16,1.,0.));
#25341=DIRECTION('ref_axis',(-1.,1.20185167898973E-16,0.));
#25342=DIRECTION('',(-1.,1.20185167898973E-16,0.));
#25343=DIRECTION('',(0.,0.,1.));
#25344=DIRECTION('',(-1.,1.20185167898973E-16,0.));
#25345=DIRECTION('center_axis',(0.866025403784439,0.5,0.));
#25346=DIRECTION('ref_axis',(-0.5,0.866025403784439,0.));
#25347=DIRECTION('',(-0.5,0.866025403784439,0.));
#25348=DIRECTION('',(0.,0.,1.));
#25349=DIRECTION('',(-0.5,0.866025403784439,0.));
#25350=DIRECTION('center_axis',(0.866025403784439,-0.5,0.));
#25351=DIRECTION('ref_axis',(0.5,0.866025403784439,0.));
#25352=DIRECTION('',(0.5,0.866025403784439,0.));
#25353=DIRECTION('',(0.5,0.866025403784439,0.));
#25354=DIRECTION('center_axis',(0.,0.,1.));
#25355=DIRECTION('ref_axis',(1.,0.,0.));
#25356=DIRECTION('center_axis',(0.,0.,1.));
#25357=DIRECTION('ref_axis',(1.,0.,0.));
#25358=DIRECTION('center_axis',(0.,0.,1.));
#25359=DIRECTION('ref_axis',(1.,0.,0.));
#25360=DIRECTION('center_axis',(0.,0.,1.));
#25361=DIRECTION('ref_axis',(1.,0.,0.));
#25362=DIRECTION('',(0.,0.,-1.));
#25363=DIRECTION('center_axis',(0.,0.,1.));
#25364=DIRECTION('ref_axis',(1.,0.,0.));
#25365=DIRECTION('center_axis',(0.,0.,1.));
#25366=DIRECTION('ref_axis',(1.,0.,0.));
#25367=DIRECTION('center_axis',(0.,0.,1.));
#25368=DIRECTION('ref_axis',(1.,0.,0.));
#53330=CARTESIAN_POINT('',(0.,0.,0.));
#53331=CARTESIAN_POINT('Origin',(0.,0.,0.));
#53332=CARTESIAN_POINT('',(-4.94697864382552,0.00278476180115707,0.322320454656892));
#53333=CARTESIAN_POINT('',(-4.94423617559418,0.00148231834052548,0.177679545343088));
#53334=CARTESIAN_POINT('',(-4.942,-6.05220448138622E-16,0.));
#53335=CARTESIAN_POINT('',(2.16917135428609,4.440502182833,0.));
#53336=CARTESIAN_POINT('Ctrl Pts',(-4.94697864382552,0.00278476180115707,
0.322320454656892));
#53337=CARTESIAN_POINT('Ctrl Pts',(-4.94837427497074,0.191084575140575,
0.316237515399425));
#53338=CARTESIAN_POINT('Ctrl Pts',(-4.93857638297692,0.379246871981659,
0.310154576141959));
#53339=CARTESIAN_POINT('Ctrl Pts',(-4.91710439111276,0.566072733558586,
0.304071636884492));
#53340=CARTESIAN_POINT('Ctrl Pts',(-4.73085624282078,2.18660104746097,0.251308196024277));
#53341=CARTESIAN_POINT('Ctrl Pts',(-3.66626808942587,3.70657817799375,0.198544755164062));
#53342=CARTESIAN_POINT('Ctrl Pts',(-2.20523483873771,4.43248249176653,0.145781314303847));
#53343=CARTESIAN_POINT('Ctrl Pts',(-0.85966080708188,5.10102168731156,0.097187542869231));
#53344=CARTESIAN_POINT('Ctrl Pts',(0.822175421307706,5.09603339682298,0.0485937714346156));
#53345=CARTESIAN_POINT('Ctrl Pts',(2.17571852337094,4.44456444733847,3.90312782094782E-17));
#53346=CARTESIAN_POINT('',(-2.16917135428615,4.44050218283297,0.));
#53347=CARTESIAN_POINT('Origin',(0.,0.,0.));
#53348=CARTESIAN_POINT('Ctrl Pts',(-2.16917135428615,4.44050218283297,1.94289029309402E-15));
#53349=CARTESIAN_POINT('Ctrl Pts',(-2.90569614448719,4.08071213863431,0.0263982667373533));
#53350=CARTESIAN_POINT('Ctrl Pts',(-3.54537901519776,3.53418981917855,0.0527965334747045));
#53351=CARTESIAN_POINT('Ctrl Pts',(-4.02261725675323,2.86672087533204,0.0791948002120558));
#53352=CARTESIAN_POINT('Ctrl Pts',(-4.49985549830871,2.1992519314855,0.105593066949408));
#53353=CARTESIAN_POINT('Ctrl Pts',(-4.81464911070909,1.41083636324821,0.13199133368676));
#53354=CARTESIAN_POINT('Ctrl Pts',(-4.91161341297729,0.598206782831744,
0.158389600424112));
#53355=CARTESIAN_POINT('Ctrl Pts',(-4.93523158039298,0.400269799547603,
0.164819582063771));
#53356=CARTESIAN_POINT('Ctrl Pts',(-4.94592610470609,0.200896217803435,
0.171249563703429));
#53357=CARTESIAN_POINT('Ctrl Pts',(-4.94423617559418,0.00148231834052548,
0.177679545343088));
#53358=CARTESIAN_POINT('Origin',(0.,0.,0.));
#53359=CARTESIAN_POINT('',(-4.93459216488855,0.00173983556611496,1.32232045465689));
#53360=CARTESIAN_POINT('',(-4.93449003509191,0.0016461999684793,1.17767954534309));
#53361=CARTESIAN_POINT('',(-4.942,-6.05220448138622E-16,0.));
#53362=CARTESIAN_POINT('Ctrl Pts',(-4.93459216488855,0.00173983556611496,
1.32232045465689));
#53363=CARTESIAN_POINT('Ctrl Pts',(-4.93685941200801,0.71330292763056,1.29948482722738));
#53364=CARTESIAN_POINT('Ctrl Pts',(-4.79300629668486,1.42399221307712,1.27664919979787));
#53365=CARTESIAN_POINT('Ctrl Pts',(-4.49846232996172,2.06549179869028,1.25381357236836));
#53366=CARTESIAN_POINT('Ctrl Pts',(-3.81789626200921,3.5477250130758,1.20105013150815));
#53367=CARTESIAN_POINT('Ctrl Pts',(-2.33282804601649,4.66057109067704,1.14828669064793));
#53368=CARTESIAN_POINT('Ctrl Pts',(-0.719110050159326,4.89750101325702,
1.09552324978772));
#53369=CARTESIAN_POINT('Ctrl Pts',(0.89460794569784,5.13443093583701,1.0427598089275));
#53370=CARTESIAN_POINT('Ctrl Pts',(2.63697572141945,4.49544470339575,0.989996368067287));
#53371=CARTESIAN_POINT('Ctrl Pts',(3.71488022775187,3.27143294682148,0.937232927207072));
#53372=CARTESIAN_POINT('Ctrl Pts',(4.79278473408429,2.04742119024721,0.884469486346857));
#53373=CARTESIAN_POINT('Ctrl Pts',(5.20622597102753,0.238383909539938,0.831706045486642));
#53374=CARTESIAN_POINT('Ctrl Pts',(4.76722694025552,-1.33245018266074,0.778942604626427));
#53375=CARTESIAN_POINT('Ctrl Pts',(4.32822790948351,-2.90328427486142,0.726179163766212));
#53376=CARTESIAN_POINT('Ctrl Pts',(3.03678861099627,-4.2359151785555,0.673415722905997));
#53377=CARTESIAN_POINT('Ctrl Pts',(1.48031593870399,-4.72357537917557,0.620652282045782));
#53378=CARTESIAN_POINT('Ctrl Pts',(-0.0761567335882804,-5.21123557979564,
0.567888841185567));
#53379=CARTESIAN_POINT('Ctrl Pts',(-1.89766277968558,-4.8539250773417,0.515125400325352));
#53380=CARTESIAN_POINT('Ctrl Pts',(-3.1544617311397,-3.81473007747874,0.462361959465137));
#53381=CARTESIAN_POINT('Ctrl Pts',(-4.26636809113457,-2.89534076044788,
0.415681457862388));
#53382=CARTESIAN_POINT('Ctrl Pts',(-4.93626856451128,-1.44222880258692,
0.36900095625964));
#53383=CARTESIAN_POINT('Ctrl Pts',(-4.94697864382552,0.00278476180115707,
0.322320454656892));
#53384=CARTESIAN_POINT('Ctrl Pts',(-4.94423617559418,0.00148231834052548,
0.177679545343088));
#53385=CARTESIAN_POINT('Ctrl Pts',(-4.93205010879707,-1.4364898912607,0.224046097178133));
#53386=CARTESIAN_POINT('Ctrl Pts',(-4.27589205183812,-2.87655855846778,
0.270412649013179));
#53387=CARTESIAN_POINT('Ctrl Pts',(-3.17793668728658,-3.7951739429827,0.316779200848224));
#53388=CARTESIAN_POINT('Ctrl Pts',(-1.92771999305178,-4.8411802984146,0.369575734322928));
#53389=CARTESIAN_POINT('Ctrl Pts',(-0.104675240574504,-5.21107779972881,
0.422372267797632));
#53390=CARTESIAN_POINT('Ctrl Pts',(1.45583984202071,-4.73188592100135,0.475168801272336));
#53391=CARTESIAN_POINT('Ctrl Pts',(3.01635492461593,-4.25269404227389,0.527965334747039));
#53392=CARTESIAN_POINT('Ctrl Pts',(4.31434033732908,-2.92441278350478,0.580761868221743));
#53393=CARTESIAN_POINT('Ctrl Pts',(4.76068268187915,-1.35442587380419,0.633558401696447));
#53394=CARTESIAN_POINT('Ctrl Pts',(5.20702502642923,0.215561035896397,0.686354935171151));
#53395=CARTESIAN_POINT('Ctrl Pts',(4.80172430281623,2.02725359652845,0.739151468645856));
#53396=CARTESIAN_POINT('Ctrl Pts',(3.72825744985575,3.25624139915875,0.791948002120559));
#53397=CARTESIAN_POINT('Ctrl Pts',(2.65479059689527,4.48522920178905,0.844744535595263));
#53398=CARTESIAN_POINT('Ctrl Pts',(0.9131576145873,5.13151224641759,0.897541069069967));
#53399=CARTESIAN_POINT('Ctrl Pts',(-0.702426516917608,4.90003317713487,
0.950337602544671));
#53400=CARTESIAN_POINT('Ctrl Pts',(-2.31801064842252,4.66855410785214,1.00313413601937));
#53401=CARTESIAN_POINT('Ctrl Pts',(-3.80754592912437,3.55931292465815,1.05593066949408));
#53402=CARTESIAN_POINT('Ctrl Pts',(-4.49264215512641,2.07804350324001,1.10872720296878));
#53403=CARTESIAN_POINT('Ctrl Pts',(-4.79088768013657,1.43319689701884,1.13171131709355));
#53404=CARTESIAN_POINT('Ctrl Pts',(-4.93667954029292,0.71784517544428,1.15469543121832));
#53405=CARTESIAN_POINT('Ctrl Pts',(-4.93449003509191,0.0016461999684793,
1.17767954534309));
#53406=CARTESIAN_POINT('Origin',(0.,0.,0.));
#53407=CARTESIAN_POINT('',(-4.9411817412373,-0.00444225127051057,2.32232045465689));
#53408=CARTESIAN_POINT('',(-4.94111085608669,-0.00445469630641156,2.17767954534309));
#53409=CARTESIAN_POINT('',(-4.942,-6.05220448138622E-16,0.));
#53410=CARTESIAN_POINT('Ctrl Pts',(-4.9411817412373,-0.00444225127051057,
2.32232045465689));
#53411=CARTESIAN_POINT('Ctrl Pts',(-4.93017412883888,1.22499555075574,2.28273213905534));
#53412=CARTESIAN_POINT('Ctrl Pts',(-4.46534239547945,2.46186324317617,2.24314382345379));
#53413=CARTESIAN_POINT('Ctrl Pts',(-3.63458175569093,3.36040592443024,2.20355550785224));
#53414=CARTESIAN_POINT('Ctrl Pts',(-2.52734116663296,4.55798664748753,2.15079206699202));
#53415=CARTESIAN_POINT('Ctrl Pts',(-0.770077330248272,5.15457871251208,
2.0980286261318));
#53416=CARTESIAN_POINT('Ctrl Pts',(0.837419729043101,4.87865187630481,2.04526518527159));
#53417=CARTESIAN_POINT('Ctrl Pts',(2.44491678833447,4.60272504009754,1.99250174441137));
#53418=CARTESIAN_POINT('Ctrl Pts',(3.90264707053253,3.45427930265847,1.93973830355116));
#53419=CARTESIAN_POINT('Ctrl Pts',(4.54714538443732,1.95601310903264,1.88697486269094));
#53420=CARTESIAN_POINT('Ctrl Pts',(5.19164369834212,0.45774691540682,1.83421142183073));
#53421=CARTESIAN_POINT('Ctrl Pts',(5.02291004395365,-1.39033973440576,1.78144798097051));
#53422=CARTESIAN_POINT('Ctrl Pts',(4.11774488359116,-2.74712173291455,1.7286845401103));
#53423=CARTESIAN_POINT('Ctrl Pts',(3.21257972322867,-4.10390373142335,1.67592109925008));
#53424=CARTESIAN_POINT('Ctrl Pts',(1.57098305689217,-4.96938107862837,1.62315765838987));
#53425=CARTESIAN_POINT('Ctrl Pts',(-0.0599057143251611,-4.94964036759779,
1.57039421752965));
#53426=CARTESIAN_POINT('Ctrl Pts',(-1.69079448554249,-4.92989965656721,
1.51763077666944));
#53427=CARTESIAN_POINT('Ctrl Pts',(-3.31097536164064,-4.02494088730103,
1.46486733580922));
#53428=CARTESIAN_POINT('Ctrl Pts',(-4.18303383973357,-2.64665132708304,
1.41210389494901));
#53429=CARTESIAN_POINT('Ctrl Pts',(-4.67767185058986,-1.86487530680844,
1.3821760815183));
#53430=CARTESIAN_POINT('Ctrl Pts',(-4.9316207664016,-0.930817306961143,
1.3522482680876));
#53431=CARTESIAN_POINT('Ctrl Pts',(-4.93459216488855,0.00173983556611496,
1.32232045465689));
#53432=CARTESIAN_POINT('Ctrl Pts',(-4.93449003509191,0.0016461999684793,
1.17767954534309));
#53433=CARTESIAN_POINT('Ctrl Pts',(-4.9316500541004,-0.927326919420464,
1.20749196469302));
#53434=CARTESIAN_POINT('Ctrl Pts',(-4.67984069516382,-1.85772549042789,
1.23730438404296));
#53435=CARTESIAN_POINT('Ctrl Pts',(-4.18882172046978,-2.63753729589231,
1.26711680339289));
#53436=CARTESIAN_POINT('Ctrl Pts',(-3.31924788850886,-4.01855101396421,
1.3199133368676));
#53437=CARTESIAN_POINT('Ctrl Pts',(-1.69944305328478,-4.92728079046571,
1.3727098703423));
#53438=CARTESIAN_POINT('Ctrl Pts',(-0.0675730918879967,-4.94957507244757,
1.42550640381701));
#53439=CARTESIAN_POINT('Ctrl Pts',(1.56429686950879,-4.97186935442943,1.47830293729171));
#53440=CARTESIAN_POINT('Ctrl Pts',(3.20823195707828,-4.10772814189165,1.53109947076641));
#53441=CARTESIAN_POINT('Ctrl Pts',(4.11520771620268,-2.7509467593832,1.58389600424112));
#53442=CARTESIAN_POINT('Ctrl Pts',(5.02218347532707,-1.39416537687474,1.63669253771582));
#53443=CARTESIAN_POINT('Ctrl Pts',(5.19219990600637,0.455256175604397,1.68948907119053));
#53444=CARTESIAN_POINT('Ctrl Pts',(4.54776321553941,1.95463753781542,1.74228560466523));
#53445=CARTESIAN_POINT('Ctrl Pts',(3.90332652507246,3.45401890002643,1.79508213813993));
#53446=CARTESIAN_POINT('Ctrl Pts',(2.44443671345924,4.60336007196933,1.84787867161464));
#53447=CARTESIAN_POINT('Ctrl Pts',(0.835860696338233,4.878943390804,1.90067520508934));
#53448=CARTESIAN_POINT('Ctrl Pts',(-0.772715320782773,5.15452670963867,
1.95347173856405));
#53449=CARTESIAN_POINT('Ctrl Pts',(-2.53097754341157,4.55635217536511,2.00626827203875));
#53450=CARTESIAN_POINT('Ctrl Pts',(-3.63776731536415,3.3569886406566,2.05906480551345));
#53451=CARTESIAN_POINT('Ctrl Pts',(-4.4666195916167,2.45880976243686,2.09860305212333));
#53452=CARTESIAN_POINT('Ctrl Pts',(-4.93011266597958,1.22347167947137,2.13814129873321));
#53453=CARTESIAN_POINT('Ctrl Pts',(-4.94111085608669,-0.00445469630641156,
2.17767954534309));
#53454=CARTESIAN_POINT('Origin',(0.,0.,0.));
#53455=CARTESIAN_POINT('',(-4.94903399601206,0.00195803074323202,3.32232045465689));
#53456=CARTESIAN_POINT('',(-4.94919334226918,0.00181972978148383,3.17767954534309));
#53457=CARTESIAN_POINT('',(-4.942,-6.05220448138622E-16,0.));
#53458=CARTESIAN_POINT('Ctrl Pts',(-4.94903399601206,0.00195803074323202,
3.32232045465689));
#53459=CARTESIAN_POINT('Ctrl Pts',(-4.949593728633,0.112604296590692,3.31874289174351));
#53460=CARTESIAN_POINT('Ctrl Pts',(-4.94620248790589,0.223215646212416,
3.31516532883013));
#53461=CARTESIAN_POINT('Ctrl Pts',(-4.93875055399973,0.333552745210412,
3.31158776591675));
#53462=CARTESIAN_POINT('Ctrl Pts',(-4.82884621871006,1.96085186995656,3.25882432505653));
#53463=CARTESIAN_POINT('Ctrl Pts',(-3.83567522857514,3.52849703407851,3.20606088419632));
#53464=CARTESIAN_POINT('Ctrl Pts',(-2.41126381713223,4.32299910001284,3.15329744333611));
#53465=CARTESIAN_POINT('Ctrl Pts',(-0.986852405689299,5.11750116594718,
3.10053400247589));
#53466=CARTESIAN_POINT('Ctrl Pts',(0.868799427061646,5.13886013369387,3.04777056161567));
#53467=CARTESIAN_POINT('Ctrl Pts',(2.31112083361857,4.37735478907724,2.99500712075546));
#53468=CARTESIAN_POINT('Ctrl Pts',(3.75344224017549,3.61584944446061,2.94224367989524));
#53469=CARTESIAN_POINT('Ctrl Pts',(4.78243322053839,2.07147978748068,2.88948023903503));
#53470=CARTESIAN_POINT('Ctrl Pts',(4.92976460259391,0.447141508486386,2.83671679817481));
#53471=CARTESIAN_POINT('Ctrl Pts',(5.07709598464943,-1.17719677050791,2.7839533573146));
#53472=CARTESIAN_POINT('Ctrl Pts',(4.34276776839756,-2.88150367151656,2.73118991645438));
#53473=CARTESIAN_POINT('Ctrl Pts',(3.06099802257449,-3.89009065317052,2.67842647559417));
#53474=CARTESIAN_POINT('Ctrl Pts',(1.77922827675142,-4.89867763482448,2.62566303473395));
#53475=CARTESIAN_POINT('Ctrl Pts',(-0.0499829986428499,-5.21154469712375,
2.57289959387374));
#53476=CARTESIAN_POINT('Ctrl Pts',(-1.59409909536903,-4.68629519517074,
2.52013615301352));
#53477=CARTESIAN_POINT('Ctrl Pts',(-3.13821519209522,-4.16104569321773,
2.46737271215331));
#53478=CARTESIAN_POINT('Ctrl Pts',(-4.39723611015331,-2.79767962701243,
2.41460927129309));
#53479=CARTESIAN_POINT('Ctrl Pts',(-4.79813789831673,-1.21671190336476,
2.36184583043288));
#53480=CARTESIAN_POINT('Ctrl Pts',(-4.89824378961878,-0.821941443944892,
2.34867070517422));
#53481=CARTESIAN_POINT('Ctrl Pts',(-4.94484511185421,-0.413603307842339,
2.33549557991555));
#53482=CARTESIAN_POINT('Ctrl Pts',(-4.9411817412373,-0.00444225127051057,
2.32232045465689));
#53483=CARTESIAN_POINT('Ctrl Pts',(-4.94111085608669,-0.00445469630641156,
2.17767954534309));
#53484=CARTESIAN_POINT('Ctrl Pts',(-4.94479885876604,-0.416212969241057,
2.19093783220791));
#53485=CARTESIAN_POINT('Ctrl Pts',(-4.89760609031032,-0.8271378330251,2.20419611907274));
#53486=CARTESIAN_POINT('Ctrl Pts',(-4.79624701605789,-1.22423691020985,
2.21745440593756));
#53487=CARTESIAN_POINT('Ctrl Pts',(-4.39261962352267,-2.80554639122433,
2.27025093941227));
#53488=CARTESIAN_POINT('Ctrl Pts',(-3.13004751717586,-4.16761281810985,
2.32304747288697));
#53489=CARTESIAN_POINT('Ctrl Pts',(-1.58383298272376,-4.68979872834667,
2.37584400636168));
#53490=CARTESIAN_POINT('Ctrl Pts',(-0.0376184482716604,-5.21198463858349,
2.42864053983638));
#53491=CARTESIAN_POINT('Ctrl Pts',(1.79223851428572,-4.89429003217164,2.48143707331108));
#53492=CARTESIAN_POINT('Ctrl Pts',(3.07195081718679,-3.88147571791622,2.53423360678579));
#53493=CARTESIAN_POINT('Ctrl Pts',(4.35166312008787,-2.86866140366079,2.58703014026049));
#53494=CARTESIAN_POINT('Ctrl Pts',(5.08123076333263,-1.1607273815618,2.6398266737352));
#53495=CARTESIAN_POINT('Ctrl Pts',(4.92822027622649,0.464093861851888,2.6926232072099));
#53496=CARTESIAN_POINT('Ctrl Pts',(4.77520978912036,2.08891510526557,2.7454197406846));
#53497=CARTESIAN_POINT('Ctrl Pts',(3.73962117166333,3.63062356999396,2.79821627415931));
#53498=CARTESIAN_POINT('Ctrl Pts',(2.29332840687238,4.38672799125455,2.85101280763401));
#53499=CARTESIAN_POINT('Ctrl Pts',(0.847035642081437,5.14283241251514,2.90380934110872));
#53500=CARTESIAN_POINT('Ctrl Pts',(-1.00996127004341,5.11333279030795,2.95660587458342));
#53501=CARTESIAN_POINT('Ctrl Pts',(-2.4315078970232,4.31167097450304,3.00940240805812));
#53502=CARTESIAN_POINT('Ctrl Pts',(-3.853054524003,3.51000915869812,3.06219894153283));
#53503=CARTESIAN_POINT('Ctrl Pts',(-4.83915086583772,1.93618514929547,3.11499547500753));
#53504=CARTESIAN_POINT('Ctrl Pts',(-4.94047465700387,0.307323593631802,
3.16779200848224));
#53505=CARTESIAN_POINT('Ctrl Pts',(-4.94679983692322,0.205641231723391,
3.17108785410252));
#53506=CARTESIAN_POINT('Ctrl Pts',(-4.94967711776464,0.103744392201655,
3.17438369972281));
#53507=CARTESIAN_POINT('Ctrl Pts',(-4.94919334226918,0.00181972978148383,
3.17767954534309));
#53508=CARTESIAN_POINT('Origin',(0.,0.,0.));
#53509=CARTESIAN_POINT('',(-4.93570031758673,0.00282778719561921,4.32232045465689));
#53510=CARTESIAN_POINT('',(-4.93596067211196,0.00302686994969232,4.17767954534309));
#53511=CARTESIAN_POINT('',(-4.942,-6.05220448138622E-16,0.));
#53512=CARTESIAN_POINT('Ctrl Pts',(-4.93570031758673,0.00282778719561921,
4.32232045465689));
#53513=CARTESIAN_POINT('Ctrl Pts',(-4.93901975399819,0.635970529567334,
4.30199020357146));
#53514=CARTESIAN_POINT('Ctrl Pts',(-4.82594024125747,1.26797266957629,4.28165995248604));
#53515=CARTESIAN_POINT('Ctrl Pts',(-4.59096240198504,1.85083188703807,4.26132970140062));
#53516=CARTESIAN_POINT('Ctrl Pts',(-3.98112048346584,3.36353616802088,4.2085662605404));
#53517=CARTESIAN_POINT('Ctrl Pts',(-2.55021179152983,4.54522999135323,4.15580281968019));
#53518=CARTESIAN_POINT('Ctrl Pts',(-0.94949200772219,4.85808392031181,4.10303937881998));
#53519=CARTESIAN_POINT('Ctrl Pts',(0.651227776085471,5.17093784927039,4.05027593795976));
#53520=CARTESIAN_POINT('Ctrl Pts',(2.42175865176475,4.61495188385518,3.99751249709954));
#53521=CARTESIAN_POINT('Ctrl Pts',(3.55627122044722,3.44317432848828,3.94474905623933));
#53522=CARTESIAN_POINT('Ctrl Pts',(4.69078378912967,2.27139677312141,3.89198561537911));
#53523=CARTESIAN_POINT('Ctrl Pts',(5.18927805081532,0.483827627802874,3.8392221745189));
#53524=CARTESIAN_POINT('Ctrl Pts',(4.82487214846976,-1.10594900598695,3.78645873365868));
#53525=CARTESIAN_POINT('Ctrl Pts',(4.46046624612419,-2.6957256397768,3.73369529279847));
#53526=CARTESIAN_POINT('Ctrl Pts',(3.23316017974738,-4.08770976203793,3.68093185193825));
#53527=CARTESIAN_POINT('Ctrl Pts',(1.7015430859675,-4.6483616008314,3.62816841107804));
#53528=CARTESIAN_POINT('Ctrl Pts',(0.169925992187646,-5.20901343962485,
3.57540497021783));
#53529=CARTESIAN_POINT('Ctrl Pts',(-1.66600212899526,-4.93833299495065,
3.52264152935761));
#53530=CARTESIAN_POINT('Ctrl Pts',(-2.97064734936451,-3.95951622992839,
3.4698780884974));
#53531=CARTESIAN_POINT('Ctrl Pts',(-4.18683263839842,-3.04706698189228,
3.42069221055056));
#53532=CARTESIAN_POINT('Ctrl Pts',(-4.94133855052495,-1.51925455419597,
3.37150633260372));
#53533=CARTESIAN_POINT('Ctrl Pts',(-4.94903399601206,0.00195803074323202,
3.32232045465689));
#53534=CARTESIAN_POINT('Ctrl Pts',(-4.94919334226918,0.00181972978148383,
3.17767954534309));
#53535=CARTESIAN_POINT('Ctrl Pts',(-4.94192746196068,-1.52899860347891,
3.22718023319751));
#53536=CARTESIAN_POINT('Ctrl Pts',(-4.17649517400323,-3.06609305497157,
3.27668092105193));
#53537=CARTESIAN_POINT('Ctrl Pts',(-2.94711271903068,-3.97709242316291,
3.32618160890635));
#53538=CARTESIAN_POINT('Ctrl Pts',(-1.63587574939375,-4.94874778236929,
3.37897814238105));
#53539=CARTESIAN_POINT('Ctrl Pts',(0.203149430377691,-5.20815939885737,
3.43177467585576));
#53540=CARTESIAN_POINT('Ctrl Pts',(1.73199722462222,-4.63712444206039,3.48457120933046));
#53541=CARTESIAN_POINT('Ctrl Pts',(3.26084501886676,-4.06608948526341,3.53736774280516));
#53542=CARTESIAN_POINT('Ctrl Pts',(4.47951542758438,-2.66460795518137,3.59016427627987));
#53543=CARTESIAN_POINT('Ctrl Pts',(4.83271212906113,-1.07127541230128,3.64296080975457));
#53544=CARTESIAN_POINT('Ctrl Pts',(5.18590883053788,0.522057130578818,3.69575734322927));
#53545=CARTESIAN_POINT('Ctrl Pts',(4.67363182477377,2.30724068625696,3.74855387670398));
#53546=CARTESIAN_POINT('Ctrl Pts',(3.52930397676422,3.47084297428374,3.80135041017868));
#53547=CARTESIAN_POINT('Ctrl Pts',(2.38497612875467,4.63444526231052,3.85414694365339));
#53548=CARTESIAN_POINT('Ctrl Pts',(0.6085974384997,5.17646628268592,3.90694347712809));
#53549=CARTESIAN_POINT('Ctrl Pts',(-0.990411824257063,4.84993009504558,
3.95974001060279));
#53550=CARTESIAN_POINT('Ctrl Pts',(-2.58942108701383,4.52339390740524,4.0125365440775));
#53551=CARTESIAN_POINT('Ctrl Pts',(-4.01106092227238,3.32830051174915,4.0653330775522));
#53552=CARTESIAN_POINT('Ctrl Pts',(-4.60755047572122,1.80920317532792,4.11812961102691));
#53553=CARTESIAN_POINT('Ctrl Pts',(-4.831813392182,1.23806626759189,4.1379795891323));
#53554=CARTESIAN_POINT('Ctrl Pts',(-4.93943770829377,0.621129986103563,
4.1578295672377));
#53555=CARTESIAN_POINT('Ctrl Pts',(-4.93596067211196,0.00302686994969232,
4.17767954534309));
#53556=CARTESIAN_POINT('Origin',(0.,0.,0.));
#53557=CARTESIAN_POINT('',(-4.93897027655035,-0.00418490057281118,5.32232045465689));
#53558=CARTESIAN_POINT('',(-4.93838471541483,-0.00406162586984615,5.17767954534309));
#53559=CARTESIAN_POINT('',(-4.942,-6.05220448138622E-16,0.));
#53560=CARTESIAN_POINT('Ctrl Pts',(-4.93897027655035,-0.00418490057281118,
5.32232045465689));
#53561=CARTESIAN_POINT('Ctrl Pts',(-4.92960049919577,1.1487585810669,5.28523751539942));
#53562=CARTESIAN_POINT('Ctrl Pts',(-4.5267508630109,2.30760372029857,5.24815457614196));
#53563=CARTESIAN_POINT('Ctrl Pts',(-3.78916668346253,3.18507932319436,5.21107163688449));
#53564=CARTESIAN_POINT('Ctrl Pts',(-2.73969541672107,4.43359502898083,5.15830819602428));
#53565=CARTESIAN_POINT('Ctrl Pts',(-1.01255385125843,5.11247792715855,5.10554475516406));
#53566=CARTESIAN_POINT('Ctrl Pts',(0.606176578608286,4.91274509878472,5.05278131430385));
#53567=CARTESIAN_POINT('Ctrl Pts',(2.224907008475,4.71301227041089,5.00001787344363));
#53568=CARTESIAN_POINT('Ctrl Pts',(3.73522630274578,3.63466371548551,4.94725443258342));
#53569=CARTESIAN_POINT('Ctrl Pts',(4.44973628814144,2.16849289048282,4.8944909917232));
#53570=CARTESIAN_POINT('Ctrl Pts',(5.1642462735371,0.702322065480126,4.84172755086299));
#53571=CARTESIAN_POINT('Ctrl Pts',(5.08294695005765,-1.15167102959988,4.78896411000277));
#53572=CARTESIAN_POINT('Ctrl Pts',(4.24284043151724,-2.54967047338244,4.73620066914256));
#53573=CARTESIAN_POINT('Ctrl Pts',(3.40273391297681,-3.94766991716502,4.68343722828234));
#53574=CARTESIAN_POINT('Ctrl Pts',(1.80382019937538,-4.88967570965013,4.63067378742212));
#53575=CARTESIAN_POINT('Ctrl Pts',(0.173819826494171,-4.94694866740537,
4.57791034656191));
#53576=CARTESIAN_POINT('Ctrl Pts',(-1.45618054638702,-5.0042216251606,4.5251469057017));
#53577=CARTESIAN_POINT('Ctrl Pts',(-3.11726757854798,-4.17676174818597,
4.47238346484148));
#53578=CARTESIAN_POINT('Ctrl Pts',(-4.05342352207729,-2.84117444038203,
4.41962002398127));
#53579=CARTESIAN_POINT('Ctrl Pts',(-4.62886975682389,-2.02020151085742,
4.38718683420648));
#53580=CARTESIAN_POINT('Ctrl Pts',(-4.93040476513016,-1.00723542508793,
4.35475364443168));
#53581=CARTESIAN_POINT('Ctrl Pts',(-4.93570031758673,0.00282778719561921,
4.32232045465689));
#53582=CARTESIAN_POINT('Ctrl Pts',(-4.93596067211196,0.00302686994969232,
4.17767954534309));
#53583=CARTESIAN_POINT('Ctrl Pts',(-4.9301895642308,-1.0228870344476,4.2106261007124));
#53584=CARTESIAN_POINT('Ctrl Pts',(-4.61834948018582,-2.05201540819261,
4.24357265608171));
#53585=CARTESIAN_POINT('Ctrl Pts',(-4.02575926717865,-2.88027773583012,
4.27651921145102));
#53586=CARTESIAN_POINT('Ctrl Pts',(-3.07613923354808,-4.20756003338059,
4.32931574492572));
#53587=CARTESIAN_POINT('Ctrl Pts',(-1.40555989464781,-5.01902335129515,
4.38211227840043));
#53588=CARTESIAN_POINT('Ctrl Pts',(0.224766745275694,-4.94491834338594,
4.43490881187513));
#53589=CARTESIAN_POINT('Ctrl Pts',(1.85509338519918,-4.87081333547673,4.48770534534984));
#53590=CARTESIAN_POINT('Ctrl Pts',(3.44516732614589,-3.91114000174376,4.54050187882454));
#53591=CARTESIAN_POINT('Ctrl Pts',(4.270459451601,-2.50318069379225,4.59329841229924));
#53592=CARTESIAN_POINT('Ctrl Pts',(5.09575157705613,-1.09522138584072,4.64609494577394));
#53593=CARTESIAN_POINT('Ctrl Pts',(5.15626188701963,0.761023896329388,4.69889147924865));
#53594=CARTESIAN_POINT('Ctrl Pts',(4.42441840505647,2.21974306847382,4.75168801272335));
#53595=CARTESIAN_POINT('Ctrl Pts',(3.69257492309331,3.67846224061823,4.80448454619806));
#53596=CARTESIAN_POINT('Ctrl Pts',(2.16837764920352,4.73965530273698,4.85728107967276));
#53597=CARTESIAN_POINT('Ctrl Pts',(0.54633850223222,4.91978167747611,4.91007761314747));
#53598=CARTESIAN_POINT('Ctrl Pts',(-1.0757006447391,5.09990805221523,4.96287414662217));
#53599=CARTESIAN_POINT('Ctrl Pts',(-2.79558166479192,4.39896773957469,5.01567068009687));
#53600=CARTESIAN_POINT('Ctrl Pts',(-3.82962787248045,3.13634944983863,5.06846721357158));
#53601=CARTESIAN_POINT('Ctrl Pts',(-4.54262037450559,2.26575259758193,5.10487132416208));
#53602=CARTESIAN_POINT('Ctrl Pts',(-4.92954384104421,1.12811506301544,5.14127543475258));
#53603=CARTESIAN_POINT('Ctrl Pts',(-4.93838471541483,-0.00406162586984614,
5.17767954534309));
#53604=CARTESIAN_POINT('Origin',(0.,0.,0.));
#53605=CARTESIAN_POINT('',(-4.94990673126105,0.000609106175146774,6.32232045465689));
#53606=CARTESIAN_POINT('',(-4.95002176789587,9.24615926348992E-5,6.1776795453431));
#53607=CARTESIAN_POINT('',(-4.942,-6.05220448138622E-16,0.));
#53608=CARTESIAN_POINT('Ctrl Pts',(-4.94990673126105,0.000609106175146774,
6.32232045465689));
#53609=CARTESIAN_POINT('Ctrl Pts',(-4.94996465668772,0.0337538979231002,
6.3212482680876));
#53610=CARTESIAN_POINT('Ctrl Pts',(-4.94966035453883,0.0668975980773335,
6.3201760815183));
#53611=CARTESIAN_POINT('Ctrl Pts',(-4.94899057048952,0.100033910748547,
6.31910389494901));
#53612=CARTESIAN_POINT('Ctrl Pts',(-4.91602978541085,1.73070708277234,6.26634045408879));
#53613=CARTESIAN_POINT('Ctrl Pts',(-3.99797098316147,3.34348977495136,6.21357701322858));
#53614=CARTESIAN_POINT('Ctrl Pts',(-2.61265424963019,4.20434920314469,6.16081357236836));
#53615=CARTESIAN_POINT('Ctrl Pts',(-1.22733751609891,5.06520863133802,6.10805013150815));
#53616=CARTESIAN_POINT('Ctrl Pts',(0.625237148714281,5.17414479554567,6.05528669064793));
#53617=CARTESIAN_POINT('Ctrl Pts',(2.10189939976769,4.48157710670587,6.00252324978771));
#53618=CARTESIAN_POINT('Ctrl Pts',(3.57856165082109,3.78900941786606,5.9497598089275));
#53619=CARTESIAN_POINT('Ctrl Pts',(4.67931148811471,2.29493787597879,5.89699636806729));
#53620=CARTESIAN_POINT('Ctrl Pts',(4.90315986233076,0.679365744295384,5.84423292720707));
#53621=CARTESIAN_POINT('Ctrl Pts',(5.12700823654681,-0.936206387388013,
5.79146948634686));
#53622=CARTESIAN_POINT('Ctrl Pts',(4.4739551476853,-2.67327910886755,5.73870604548664));
#53623=CARTESIAN_POINT('Ctrl Pts',(3.24122748150885,-3.74125097570411,5.68594260462643));
#53624=CARTESIAN_POINT('Ctrl Pts',(2.00849981533238,-4.80922284254067,5.63317916376621));
#53625=CARTESIAN_POINT('Ctrl Pts',(0.196097571840956,-5.20809385473422,
5.580415722906));
#53626=CARTESIAN_POINT('Ctrl Pts',(-1.37109275233711,-4.7563241179068,5.52765228204578));
#53627=CARTESIAN_POINT('Ctrl Pts',(-2.93828307651517,-4.30455438107937,
5.47488884118557));
#53628=CARTESIAN_POINT('Ctrl Pts',(-4.26026148137987,-3.00214389523098,
5.42212540032535));
#53629=CARTESIAN_POINT('Ctrl Pts',(-4.73535019980207,-1.44186439560917,
5.36936195946513));
#53630=CARTESIAN_POINT('Ctrl Pts',(-4.87653942645625,-0.978172778920024,
5.35368145786239));
#53631=CARTESIAN_POINT('Ctrl Pts',(-4.94293228203772,-0.49170645290201,
5.33800095625964));
#53632=CARTESIAN_POINT('Ctrl Pts',(-4.93897027655035,-0.00418490057281118,
5.32232045465689));
#53633=CARTESIAN_POINT('Ctrl Pts',(-4.93838471541483,-0.00406162586984614,
5.17767954534309));
#53634=CARTESIAN_POINT('Ctrl Pts',(-4.94236567660296,-0.513869962422989,
5.19407196822729));
#53635=CARTESIAN_POINT('Ctrl Pts',(-4.86968605256145,-1.02257104983416,
5.21046439111149));
#53636=CARTESIAN_POINT('Ctrl Pts',(-4.71559692470099,-1.50528507494596,
5.22685681399569));
#53637=CARTESIAN_POINT('Ctrl Pts',(-4.21930837390877,-3.06000504316299,
5.27965334747039));
#53638=CARTESIAN_POINT('Ctrl Pts',(-2.8785198770001,-4.34514871276549,5.3324498809451));
#53639=CARTESIAN_POINT('Ctrl Pts',(-1.30417176812337,-4.7751307324871,5.3852464144198));
#53640=CARTESIAN_POINT('Ctrl Pts',(0.270176340753341,-5.2051127522087,5.4380429478945));
#53641=CARTESIAN_POINT('Ctrl Pts',(2.07808406159809,-4.77993312204945,5.49083948136921));
#53642=CARTESIAN_POINT('Ctrl Pts',(3.29576468259939,-3.69332812921623,5.54363601484391));
#53643=CARTESIAN_POINT('Ctrl Pts',(4.51344530360071,-2.606723136383,5.59643254831862));
#53644=CARTESIAN_POINT('Ctrl Pts',(5.14089882475856,-0.858692780875764,
5.64922908179332));
#53645=CARTESIAN_POINT('Ctrl Pts',(4.892221343433,0.754259796075777,5.70202561526803));
#53646=CARTESIAN_POINT('Ctrl Pts',(4.64354386210744,2.36721237302732,5.75482214874273));
#53647=CARTESIAN_POINT('Ctrl Pts',(3.51873537829851,3.84508717142316,5.80761868221743));
#53648=CARTESIAN_POINT('Ctrl Pts',(2.03032331340283,4.51447945572607,5.86041521569213));
#53649=CARTESIAN_POINT('Ctrl Pts',(0.54191124850715,5.18387174002898,5.91321174916684));
#53650=CARTESIAN_POINT('Ctrl Pts',(-1.31010439747531,5.04478151023892,5.96600828264154));
#53651=CARTESIAN_POINT('Ctrl Pts',(-2.68183880585053,4.16058627269715,6.01880481611625));
#53652=CARTESIAN_POINT('Ctrl Pts',(-4.05357321422575,3.27639103515538,6.07160134959095));
#53653=CARTESIAN_POINT('Ctrl Pts',(-4.94502638499377,1.6470907898619,6.12439788306566));
#53654=CARTESIAN_POINT('Ctrl Pts',(-4.95000099524402,0.0150884128829395,
6.17719441654037));
#53655=CARTESIAN_POINT('Ctrl Pts',(-4.95001623189281,0.0100897806679753,
6.17735612614128));
#53656=CARTESIAN_POINT('Ctrl Pts',(-4.950023152263,0.00509112310363388,
6.17751783574219));
#53657=CARTESIAN_POINT('Ctrl Pts',(-4.95002176789587,9.24615926348992E-5,
6.1776795453431));
#53658=CARTESIAN_POINT('Origin',(0.,0.,0.));
#53659=CARTESIAN_POINT('',(-4.93729272679059,0.00368592931905526,7.32232045465689));
#53660=CARTESIAN_POINT('',(-4.93812703863464,0.00398950918922817,7.17767954534309));
#53661=CARTESIAN_POINT('',(-4.942,-6.05220448138622E-16,0.));
#53662=CARTESIAN_POINT('Ctrl Pts',(-4.93729272679059,0.00368592931905526,
7.32232045465689));
#53663=CARTESIAN_POINT('Ctrl Pts',(-4.94116559210242,0.558353954818944,
7.30449557991555));
#53664=CARTESIAN_POINT('Ctrl Pts',(-4.85488370936681,1.1118525040865,7.28667070517422));
#53665=CARTESIAN_POINT('Ctrl Pts',(-4.67321739836765,1.63203970469098,7.26884583043288));
#53666=CARTESIAN_POINT('Ctrl Pts',(-4.13546665420853,3.17184668755196,7.21608238957266));
#53667=CARTESIAN_POINT('Ctrl Pts',(-2.76193831173125,4.41977291493536,7.16331894871245));
#53668=CARTESIAN_POINT('Ctrl Pts',(-1.17777228483381,4.80784430854112,7.11055550785224));
#53669=CARTESIAN_POINT('Ctrl Pts',(0.406393742063621,5.19591570214688,7.05779206699202));
#53670=CARTESIAN_POINT('Ctrl Pts',(2.2011974533812,4.72413226197502,7.0050286261318));
#53671=CARTESIAN_POINT('Ctrl Pts',(3.38976204879511,3.60721883209798,6.95226518527158));
#53672=CARTESIAN_POINT('Ctrl Pts',(4.57832664420902,2.49030540222094,6.89950174441137));
#53673=CARTESIAN_POINT('Ctrl Pts',(5.16065212371926,0.728261982638741,6.84673830355116));
#53674=CARTESIAN_POINT('Ctrl Pts',(4.8717021652758,-0.876944960040814,6.79397486269094));
#53675=CARTESIAN_POINT('Ctrl Pts',(4.58275220683234,-2.48215190272036,6.74121142183073));
#53676=CARTESIAN_POINT('Ctrl Pts',(3.4225268104352,-3.93052236849726,6.68844798097051));
#53677=CARTESIAN_POINT('Ctrl Pts',(1.91908439466629,-4.56285322317541,6.63568454011029));
#53678=CARTESIAN_POINT('Ctrl Pts',(0.415641978897348,-5.19518407785358,
6.58292109925008));
#53679=CARTESIAN_POINT('Ctrl Pts',(-1.43101745624338,-5.01147532143298,
6.53015765838987));
#53680=CARTESIAN_POINT('Ctrl Pts',(-2.78041578985976,-4.09533911728839,
6.47739421752966));
#53681=CARTESIAN_POINT('Ctrl Pts',(-4.10239349384425,-3.1978193816249,6.42570296323874));
#53682=CARTESIAN_POINT('Ctrl Pts',(-4.94711408486409,-1.59733653848074,
6.37401170894781));
#53683=CARTESIAN_POINT('Ctrl Pts',(-4.94990673126105,0.000609106175146774,
6.32232045465689));
#53684=CARTESIAN_POINT('Ctrl Pts',(-4.95002176789587,9.24615926348992E-5,
6.1776795453431));
#53685=CARTESIAN_POINT('Ctrl Pts',(-4.94957117052949,-1.62692081873173,
6.23031436921689));
#53686=CARTESIAN_POINT('Ctrl Pts',(-4.06928678123987,-3.25435222218023,
6.28294919309067));
#53687=CARTESIAN_POINT('Ctrl Pts',(-2.70715303041471,-4.14415974390912,
6.33558401696446));
#53688=CARTESIAN_POINT('Ctrl Pts',(-1.34083440560272,-5.03670101505779,
6.38838055043917));
#53689=CARTESIAN_POINT('Ctrl Pts',(0.510298893753757,-5.18707904869072,
6.44117708391388));
#53690=CARTESIAN_POINT('Ctrl Pts',(2.00276409681877,-4.52677296598962,6.49397361738859));
#53691=CARTESIAN_POINT('Ctrl Pts',(3.49522929988377,-3.86646688328851,6.54677015086329));
#53692=CARTESIAN_POINT('Ctrl Pts',(4.62902640665733,-2.39547668425338,6.59956668433799));
#53693=CARTESIAN_POINT('Ctrl Pts',(4.88753226227565,-0.784070085091338,
6.65236321781269));
#53694=CARTESIAN_POINT('Ctrl Pts',(5.14603811789397,0.827336514070738,6.7051597512874));
#53695=CARTESIAN_POINT('Ctrl Pts',(4.52925272235704,2.57915951335971,6.7579562847621));
#53696=CARTESIAN_POINT('Ctrl Pts',(3.31821896685987,3.67316762496513,6.81075281823681));
#53697=CARTESIAN_POINT('Ctrl Pts',(2.10718521136272,4.76717573657052,6.86354935171151));
#53698=CARTESIAN_POINT('Ctrl Pts',(0.301903095905328,5.20336896049236,6.91634588518622));
#53699=CARTESIAN_POINT('Ctrl Pts',(-1.27503704449112,4.78299258292295,6.96914241866092));
#53700=CARTESIAN_POINT('Ctrl Pts',(-2.85197718488759,4.36261620535354,7.02193895213562));
#53701=CARTESIAN_POINT('Ctrl Pts',(-4.20057535022311,3.0856702262929,7.07473548561032));
#53702=CARTESIAN_POINT('Ctrl Pts',(-4.70633267235205,1.53400465783913,7.12753201908503));
#53703=CARTESIAN_POINT('Ctrl Pts',(-4.86645984309908,1.04273383179117,7.14424786117105));
#53704=CARTESIAN_POINT('Ctrl Pts',(-4.94209974418837,0.523924819599999,
7.16096370325707));
#53705=CARTESIAN_POINT('Ctrl Pts',(-4.93812703863464,0.00398950918922817,
7.17767954534309));
#53706=CARTESIAN_POINT('Origin',(0.,0.,0.));
#53707=CARTESIAN_POINT('',(-4.9370364718937,-0.00357917755902493,8.32232045465689));
#53708=CARTESIAN_POINT('',(-4.93615302863258,-0.00314627141571121,8.17767954534309));
#53709=CARTESIAN_POINT('',(-4.942,-6.05220448138622E-16,0.));
#53710=CARTESIAN_POINT('Ctrl Pts',(-4.9370364718937,-0.00357917755902493,
8.32232045465689));
#53711=CARTESIAN_POINT('Ctrl Pts',(-4.92976643593387,1.07253365977557,8.28774289174351));
#53712=CARTESIAN_POINT('Ctrl Pts',(-4.58366254169201,2.15290343310709,8.25316532883013));
#53713=CARTESIAN_POINT('Ctrl Pts',(-3.93530233070663,3.00265049848112,8.21858776591675));
#53714=CARTESIAN_POINT('Ctrl Pts',(-2.94594065318929,4.29931733247173,8.16582432505654));
#53715=CARTESIAN_POINT('Ctrl Pts',(-1.25277317118212,5.05897768713911,8.11306088419632));
#53716=CARTESIAN_POINT('Ctrl Pts',(0.373581453010537,4.93588404929253,8.06029744333611));
#53717=CARTESIAN_POINT('Ctrl Pts',(1.99993607720318,4.81279041144596,8.00753400247589));
#53718=CARTESIAN_POINT('Ctrl Pts',(3.55947784358134,3.80694278108544,7.95477056161567));
#53719=CARTESIAN_POINT('Ctrl Pts',(4.34240574156256,2.37613695433122,7.90200712075546));
#53720=CARTESIAN_POINT('Ctrl Pts',(5.12533363954378,0.945331127576992,7.84924367989524));
#53721=CARTESIAN_POINT('Ctrl Pts',(5.13164766912806,-0.910432895570919,
7.79648023903503));
#53722=CARTESIAN_POINT('Ctrl Pts',(4.35847409863575,-2.34653318357428,7.74371679817482));
#53723=CARTESIAN_POINT('Ctrl Pts',(3.58530052814345,-3.78263347157761,7.6909533573146));
#53724=CARTESIAN_POINT('Ctrl Pts',(2.03263935757455,-4.7990700244364,7.63818991645438));
#53725=CARTESIAN_POINT('Ctrl Pts',(0.407160002087725,-4.93322766379111,
7.58542647559417));
#53726=CARTESIAN_POINT('Ctrl Pts',(-1.21831935339912,-5.06738530314582,
7.53266303473395));
#53727=CARTESIAN_POINT('Ctrl Pts',(-2.91661689380388,-4.31926402899647,
7.47989959387374));
#53728=CARTESIAN_POINT('Ctrl Pts',(-3.9147790910858,-3.02935952275251,7.42713615301352));
#53729=CARTESIAN_POINT('Ctrl Pts',(-4.57573590812677,-2.1752186035157,7.39219758689465));
#53730=CARTESIAN_POINT('Ctrl Pts',(-4.92970151716189,-1.08351977418085,
7.35725902077577));
#53731=CARTESIAN_POINT('Ctrl Pts',(-4.93729272679059,0.00368592931905526,
7.32232045465689));
#53732=CARTESIAN_POINT('Ctrl Pts',(-4.93812703863464,0.00398950918922817,
7.17767954534309));
#53733=CARTESIAN_POINT('Ctrl Pts',(-4.9295520615366,-1.11827674461206,7.21376023673177));
#53734=CARTESIAN_POINT('Ctrl Pts',(-4.55006154683992,-2.24579042752333,
7.24984092812046));
#53735=CARTESIAN_POINT('Ctrl Pts',(-3.84867674353058,-3.11294472114867,
7.28592161950915));
#53736=CARTESIAN_POINT('Ctrl Pts',(-2.82234701365785,-4.38184337383585,
7.33871815298385));
#53737=CARTESIAN_POINT('Ctrl Pts',(-1.10677107499002,-5.09325552136332,
7.39151468645855));
#53738=CARTESIAN_POINT('Ctrl Pts',(0.516336029677229,-4.92302088331724,
7.44431121993325));
#53739=CARTESIAN_POINT('Ctrl Pts',(2.13944313434447,-4.75278624527117,7.49710775340795));
#53740=CARTESIAN_POINT('Ctrl Pts',(3.67008140501115,-3.70090482165158,7.54990428688267));
#53741=CARTESIAN_POINT('Ctrl Pts',(4.41080403428737,-2.24667427194838,7.60270082035737));
#53742=CARTESIAN_POINT('Ctrl Pts',(5.15152666356361,-0.792443722245162,
7.65549735383208));
#53743=CARTESIAN_POINT('Ctrl Pts',(5.10233365144936,1.06413595354166,7.70829388730677));
#53744=CARTESIAN_POINT('Ctrl Pts',(4.28564016284837,2.47710030230944,7.76109042078147));
#53745=CARTESIAN_POINT('Ctrl Pts',(3.46894667424739,3.89006465107721,7.81388695425618));
#53746=CARTESIAN_POINT('Ctrl Pts',(1.88475270915971,4.85941367282593,7.86668348773089));
#53747=CARTESIAN_POINT('Ctrl Pts',(0.254908128790928,4.94345621594819,7.91948002120559));
#53748=CARTESIAN_POINT('Ctrl Pts',(-1.37493645157786,5.02749875907046,7.9722765546803));
#53749=CARTESIAN_POINT('Ctrl Pts',(-3.05043164722777,4.22623482356622,8.02507308815499));
#53750=CARTESIAN_POINT('Ctrl Pts',(-4.00812550651364,2.90476633090432,8.0778696216297));
#53751=CARTESIAN_POINT('Ctrl Pts',(-4.61162062728013,2.07203697816232,8.11113959620083));
#53752=CARTESIAN_POINT('Ctrl Pts',(-4.93008062183261,1.03273713844183,8.14440957077196));
#53753=CARTESIAN_POINT('Ctrl Pts',(-4.93615302863258,-0.00314627141571121,
8.17767954534309));
#53754=CARTESIAN_POINT('Origin',(0.,0.,0.));
#53755=CARTESIAN_POINT('',(-4.94983422880388,-0.000811751590238941,9.32232045465689));
#53756=CARTESIAN_POINT('',(-4.94934061074693,-0.00165165342605634,9.1776795453431));
#53757=CARTESIAN_POINT('',(-4.942,-6.05220448138622E-16,0.));
#53758=CARTESIAN_POINT('Ctrl Pts',(-4.94983422880388,-0.000811751590238941,
9.32232045465689));
#53759=CARTESIAN_POINT('Ctrl Pts',(-4.94619904315733,1.58603660082692,9.27099020357146));
#53760=CARTESIAN_POINT('Ctrl Pts',(-4.11486910012118,3.17616060693066,9.21965995248604));
#53761=CARTESIAN_POINT('Ctrl Pts',(-2.80821896129528,4.07632441244751,9.16832970140062));
#53762=CARTESIAN_POINT('Ctrl Pts',(-1.46508589907443,5.00162165359779,9.1155662605404));
#53763=CARTESIAN_POINT('Ctrl Pts',(0.38028069926283,5.19789211576897,9.06280281968019));
#53764=CARTESIAN_POINT('Ctrl Pts',(1.88799112724405,4.575806371946,9.01003937881998));
#53765=CARTESIAN_POINT('Ctrl Pts',(3.39570155522527,3.95372062812305,8.95727593795976));
#53766=CARTESIAN_POINT('Ctrl Pts',(4.56575581285046,2.51327867830594,8.90451249709954));
#53767=CARTESIAN_POINT('Ctrl Pts',(4.86562202928207,0.910075116822231,8.85174905623933));
#53768=CARTESIAN_POINT('Ctrl Pts',(5.16548824571368,-0.693128444661515,
8.79898561537912));
#53769=CARTESIAN_POINT('Ctrl Pts',(4.5951664209517,-2.45909361781186,8.7462221745189));
#53770=CARTESIAN_POINT('Ctrl Pts',(3.4142296015798,-3.58406901130408,8.69345873365869));
#53771=CARTESIAN_POINT('Ctrl Pts',(2.23329278220791,-4.70904440479628,8.64069529279847));
#53772=CARTESIAN_POINT('Ctrl Pts',(0.441740968226092,-5.19303001863033,
8.58793185193825));
#53773=CARTESIAN_POINT('Ctrl Pts',(-1.14502909018537,-4.81574738049279,
8.53516841107804));
#53774=CARTESIAN_POINT('Ctrl Pts',(-2.73179914859682,-4.43846474235526,
8.48240497021782));
#53775=CARTESIAN_POINT('Ctrl Pts',(-4.11378745143793,-3.19991385224615,
8.42964152935761));
#53776=CARTESIAN_POINT('Ctrl Pts',(-4.66200366634471,-1.66380175053471,
8.3768780884974));
#53777=CARTESIAN_POINT('Ctrl Pts',(-4.85095633907095,-1.1343528226608,8.35869221055056));
#53778=CARTESIAN_POINT('Ctrl Pts',(-4.94086010709221,-0.569554771785043,
8.34050633260373));
#53779=CARTESIAN_POINT('Ctrl Pts',(-4.9370364718937,-0.00357917755902493,
8.32232045465689));
#53780=CARTESIAN_POINT('Ctrl Pts',(-4.93615302863258,-0.00314627141571121,
8.17767954534309));
#53781=CARTESIAN_POINT('Ctrl Pts',(-4.93971699916741,-0.611119036064889,
8.19720610424667));
#53782=CARTESIAN_POINT('Ctrl Pts',(-4.83567403422615,-1.21791495642756,
8.21673266315024));
#53783=CARTESIAN_POINT('Ctrl Pts',(-4.61849424808279,-1.78108068136924,
8.23625922205381));
#53784=CARTESIAN_POINT('Ctrl Pts',(-4.03127660744421,-3.30378615116137,
8.28905575552852));
#53785=CARTESIAN_POINT('Ctrl Pts',(-2.61694880324517,-4.50752404092604,
8.34185228900322));
#53786=CARTESIAN_POINT('Ctrl Pts',(-1.01995990653351,-4.84380215349313,
8.39464882247793));
#53787=CARTESIAN_POINT('Ctrl Pts',(0.57702899017813,-5.18008026606022,8.44744535595263));
#53788=CARTESIAN_POINT('Ctrl Pts',(2.35667897940238,-4.64889860142975,8.50024188942734));
#53789=CARTESIAN_POINT('Ctrl Pts',(3.50807919667006,-3.4922940688051,8.55303842290204));
#53790=CARTESIAN_POINT('Ctrl Pts',(4.65947941393775,-2.33568953618045,8.60583495637674));
#53791=CARTESIAN_POINT('Ctrl Pts',(5.18262985924886,-0.553662135561577,
8.65863148985144));
#53792=CARTESIAN_POINT('Ctrl Pts',(4.83915310871477,1.04179398325038,8.71142802332615));
#53793=CARTESIAN_POINT('Ctrl Pts',(4.49567635818068,2.63725010206233,8.76422455680085));
#53794=CARTESIAN_POINT('Ctrl Pts',(3.28557241180142,4.04613493906739,8.81702109027556));
#53795=CARTESIAN_POINT('Ctrl Pts',(1.76023420818717,4.62647955204043,8.86981762375026));
#53796=CARTESIAN_POINT('Ctrl Pts',(0.234896004572933,5.20682416501346,8.92261415722497));
#53797=CARTESIAN_POINT('Ctrl Pts',(-1.60567645627628,4.95862855395447,8.97541069069966));
#53798=CARTESIAN_POINT('Ctrl Pts',(-2.9228125287938,3.99498491044041,9.02820722417436));
#53799=CARTESIAN_POINT('Ctrl Pts',(-4.16579429986394,3.0855940679239,9.07803133123061));
#53800=CARTESIAN_POINT('Ctrl Pts',(-4.9426191442377,1.53904642191653,9.12785543828685));
#53801=CARTESIAN_POINT('Ctrl Pts',(-4.94934061074693,-0.00165165342605634,
9.1776795453431));
#53802=CARTESIAN_POINT('Origin',(0.,0.,0.));
#53803=CARTESIAN_POINT('',(-4.93927523449924,0.00424456982664218,10.3223204546569));
#53804=CARTESIAN_POINT('',(-4.94081497674544,0.00444099958366976,10.1776795453431));
#53805=CARTESIAN_POINT('',(-4.942,-6.05220448138622E-16,0.));
#53806=CARTESIAN_POINT('Ctrl Pts',(-4.93927523449924,0.00424456982664218,
10.3223204546569));
#53807=CARTESIAN_POINT('Ctrl Pts',(-4.94321947186548,0.480467662900444,
10.3070009562597));
#53808=CARTESIAN_POINT('Ctrl Pts',(-4.8799048924926,0.955663934034991,10.2916814578624));
#53809=CARTESIAN_POINT('Ctrl Pts',(-4.7450520171049,1.40960838712838,10.2763619594652));
#53810=CARTESIAN_POINT('Ctrl Pts',(-4.28059152820107,2.97308459787111,10.2235985186049));
#53811=CARTESIAN_POINT('Ctrl Pts',(-2.96750623957443,4.28446059329433,10.1708350777447));
#53812=CARTESIAN_POINT('Ctrl Pts',(-1.40342635577711,4.74688412687777,10.1180716368845));
#53813=CARTESIAN_POINT('Ctrl Pts',(0.160653528020168,5.2093076604612,10.0653081960243));
#53814=CARTESIAN_POINT('Ctrl Pts',(1.9757280069881,4.82277873220489,10.0125447551641));
#53815=CARTESIAN_POINT('Ctrl Pts',(3.21569435837255,3.76321993027579,9.95978131430385));
#53816=CARTESIAN_POINT('Ctrl Pts',(4.455660709757,2.70366112834667,9.90701787344364));
#53817=CARTESIAN_POINT('Ctrl Pts',(5.12051893355795,0.971072452744719,9.85425443258342));
#53818=CARTESIAN_POINT('Ctrl Pts',(4.90766922172796,-0.64598549534651,9.8014909917232));
#53819=CARTESIAN_POINT('Ctrl Pts',(4.69481950989796,-2.26304344343773,9.74872755086298));
#53820=CARTESIAN_POINT('Ctrl Pts',(3.60426186243706,-3.76457066401824,9.69596411000277));
#53821=CARTESIAN_POINT('Ctrl Pts',(2.13234651308336,-4.4671705584447,9.64320066914255));
#53822=CARTESIAN_POINT('Ctrl Pts',(0.660431163729675,-5.16977045287116,
9.59043722828234));
#53823=CARTESIAN_POINT('Ctrl Pts',(-1.19284188751682,-5.07344302114356,
9.53767378742213));
#53824=CARTESIAN_POINT('Ctrl Pts',(-2.58398443596702,-4.22203018520405,
9.48491034656191));
#53825=CARTESIAN_POINT('Ctrl Pts',(-3.97512698441724,-3.37061734926452,
9.43214690570169));
#53826=CARTESIAN_POINT('Ctrl Pts',(-4.90413903007116,-1.76411910911306,
9.37938346484148));
#53827=CARTESIAN_POINT('Ctrl Pts',(-4.94819528984589,-0.133707978972622,
9.32662002398126));
#53828=CARTESIAN_POINT('Ctrl Pts',(-4.94939197035033,-0.089421849745139,
9.32518683420647));
#53829=CARTESIAN_POINT('Ctrl Pts',(-4.94993572666894,-0.0451180774845514,
9.32375364443168));
#53830=CARTESIAN_POINT('Ctrl Pts',(-4.94983422880388,-0.000811751590238941,
9.32232045465689));
#53831=CARTESIAN_POINT('Ctrl Pts',(-4.94934061074693,-0.00165165342605634,
9.1776795453431));
#53832=CARTESIAN_POINT('Ctrl Pts',(-4.94974160267239,-0.0935672327028531,
9.18065197176156));
#53833=CARTESIAN_POINT('Ctrl Pts',(-4.94740170081727,-0.185461992629528,
9.18362439818002));
#53834=CARTESIAN_POINT('Ctrl Pts',(-4.9422563677255,-0.277199402591944,
9.18659682459849));
#53835=CARTESIAN_POINT('Ctrl Pts',(-4.85086444995379,-1.90664839614095,
9.23939335807319));
#53836=CARTESIAN_POINT('Ctrl Pts',(-3.87438093022463,-3.48645470726985,
9.29218989154789));
#53837=CARTESIAN_POINT('Ctrl Pts',(-2.45774784765697,-4.29676774220554,
9.34498642502259));
#53838=CARTESIAN_POINT('Ctrl Pts',(-1.04111476508925,-5.10708077714125,
9.3977829584973));
#53839=CARTESIAN_POINT('Ctrl Pts',(0.815667880316977,-5.14790053588371,
9.450579491972));
#53840=CARTESIAN_POINT('Ctrl Pts',(2.2665431508298,-4.40062718922509,9.50337602544671));
#53841=CARTESIAN_POINT('Ctrl Pts',(3.71741842134259,-3.65335384256648,9.55617255892141));
#53842=CARTESIAN_POINT('Ctrl Pts',(4.76238631696197,-2.11798739050681,9.60896909239612));
#53843=CARTESIAN_POINT('Ctrl Pts',(4.92529937908085,-0.494129071747753,
9.66176562587082));
#53844=CARTESIAN_POINT('Ctrl Pts',(5.08821244119973,1.12972924701132,9.71456215934552));
#53845=CARTESIAN_POINT('Ctrl Pts',(4.36907066981809,2.8420794324698,9.76735869282023));
#53846=CARTESIAN_POINT('Ctrl Pts',(3.09555640642893,3.86267628047412,9.82015522629493));
#53847=CARTESIAN_POINT('Ctrl Pts',(1.82204214303977,4.88327312847843,9.87295175976963));
#53848=CARTESIAN_POINT('Ctrl Pts',(-0.00584461235687284,5.21211663902861,
9.92574829324434));
#53849=CARTESIAN_POINT('Ctrl Pts',(-1.55521355102309,4.69936680030775,9.97854482671904));
#53850=CARTESIAN_POINT('Ctrl Pts',(-3.10458248968932,4.18661696158688,10.0313413601937));
#53851=CARTESIAN_POINT('Ctrl Pts',(-4.37543361162511,2.83227377359494,10.0841378936684));
#53852=CARTESIAN_POINT('Ctrl Pts',(-4.78869407209101,1.25345386713711,10.1369344271432));
#53853=CARTESIAN_POINT('Ctrl Pts',(-4.89500374307923,0.847308491854974,
10.1505161332098));
#53854=CARTESIAN_POINT('Ctrl Pts',(-4.9445618440258,0.426308236753005,10.1640978392764));
#53855=CARTESIAN_POINT('Ctrl Pts',(-4.94081497674544,0.00444099958366976,
10.1776795453431));
#53856=CARTESIAN_POINT('Origin',(0.,0.,0.));
#53857=CARTESIAN_POINT('',(-4.93550942083981,-0.00268364051190351,11.3223204546569));
#53858=CARTESIAN_POINT('',(-4.93464332849729,-0.00183839903596135,11.1776795453431));
#53859=CARTESIAN_POINT('',(-4.942,-6.05220448138622E-16,0.));
#53860=CARTESIAN_POINT('Ctrl Pts',(-4.93550942083981,-0.00268364051190351,
11.3223204546569));
#53861=CARTESIAN_POINT('Ctrl Pts',(-4.93055147786098,0.996233778963576,
11.2902482680876));
#53862=CARTESIAN_POINT('Ctrl Pts',(-4.63616667462007,1.99783803363001,11.2581760815183));
#53863=CARTESIAN_POINT('Ctrl Pts',(-4.07266300921302,2.81352633957493,11.226103894949));
#53864=CARTESIAN_POINT('Ctrl Pts',(-3.14561700753245,4.15545298365024,11.1733404540888));
#53865=CARTESIAN_POINT('Ctrl Pts',(-1.49019904742592,4.99419689804637,11.1205770132286));
#53866=CARTESIAN_POINT('Ctrl Pts',(0.140153312490383,4.94801692591001,11.0678135723684));
#53867=CARTESIAN_POINT('Ctrl Pts',(1.77050567240668,4.90183695377364,11.0150501315081));
#53868=CARTESIAN_POINT('Ctrl Pts',(3.37579243213274,3.97073309510478,10.9622866906479));
#53869=CARTESIAN_POINT('Ctrl Pts',(4.22539246378791,2.57848268891964,10.9095232497877));
#53870=CARTESIAN_POINT('Ctrl Pts',(5.07499249544306,1.18623228273452,10.8567598089275));
#53871=CARTESIAN_POINT('Ctrl Pts',(5.16890579902736,-0.667164670966868,
10.8039963680673));
#53872=CARTESIAN_POINT('Ctrl Pts',(4.46438920521479,-2.13816357523356,10.7512329272071));
#53873=CARTESIAN_POINT('Ctrl Pts',(3.75987261140222,-3.60916247950026,10.6984694863469));
#53874=CARTESIAN_POINT('Ctrl Pts',(2.25692612019279,-4.69776333433226,10.6457060454866));
#53875=CARTESIAN_POINT('Ctrl Pts',(0.639592289029041,-4.90850650951066,
10.5929426046264));
#53876=CARTESIAN_POINT('Ctrl Pts',(-0.977741542134707,-5.11924968468906,
10.5401791637662));
#53877=CARTESIAN_POINT('Ctrl Pts',(-2.70946271325277,-4.45213518021386,
10.487415722906));
#53878=CARTESIAN_POINT('Ctrl Pts',(-3.76740545422127,-3.21078971494518,
10.4346522820458));
#53879=CARTESIAN_POINT('Ctrl Pts',(-4.51818187206105,-2.32986027932856,
10.3972083395828));
#53880=CARTESIAN_POINT('Ctrl Pts',(-4.92963472322582,-1.15974067526383,
10.3597643971199));
#53881=CARTESIAN_POINT('Ctrl Pts',(-4.93927523449924,0.00424456982664218,
10.3223204546569));
#53882=CARTESIAN_POINT('Ctrl Pts',(-4.94081497674544,0.00444099958366976,
10.1776795453431));
#53883=CARTESIAN_POINT('Ctrl Pts',(-4.92999654546744,-1.21362768880717,
10.2168943727512));
#53884=CARTESIAN_POINT('Ctrl Pts',(-4.47479284917987,-2.43892410978247,
10.2561092001592));
#53885=CARTESIAN_POINT('Ctrl Pts',(-3.65816585751927,-3.33475037626519,
10.2953240275673));
#53886=CARTESIAN_POINT('Ctrl Pts',(-2.5587073834856,-4.54083808828599,10.348120561042));
#53887=CARTESIAN_POINT('Ctrl Pts',(-0.804120636422241,-5.14971688740386,
10.4009170945167));
#53888=CARTESIAN_POINT('Ctrl Pts',(0.806103773459557,-4.88394658237934,
10.4537136279914));
#53889=CARTESIAN_POINT('Ctrl Pts',(2.41632818334133,-4.61817627735482,10.5065101614661));
#53890=CARTESIAN_POINT('Ctrl Pts',(3.88219025604155,-3.47775686818796,10.5593066949408));
#53891=CARTESIAN_POINT('Ctrl Pts',(4.53575894457716,-1.9823290114935,10.6121032284155));
#53892=CARTESIAN_POINT('Ctrl Pts',(5.18932763311279,-0.486901154799003,
10.6648997618902));
#53893=CARTESIAN_POINT('Ctrl Pts',(5.03060293748377,1.3635351494231,10.7176962953649));
#53894=CARTESIAN_POINT('Ctrl Pts',(4.13190895564446,2.72581472139719,10.7704928288396));
#53895=CARTESIAN_POINT('Ctrl Pts',(3.23321497380518,4.08809429337122,10.8232893623143));
#53896=CARTESIAN_POINT('Ctrl Pts',(1.5945517057557,4.96221713309726,10.876085895789));
#53897=CARTESIAN_POINT('Ctrl Pts',(-0.0374116408992591,4.94988261297637,
10.9288824292637));
#53898=CARTESIAN_POINT('Ctrl Pts',(-1.66937498755429,4.93754809285548,10.9816789627384));
#53899=CARTESIAN_POINT('Ctrl Pts',(-3.29463841281478,4.03875621288757,11.0344754962131));
#53900=CARTESIAN_POINT('Ctrl Pts',(-4.17263844793783,2.66304823386876,11.0872720296878));
#53901=CARTESIAN_POINT('Ctrl Pts',(-4.67379383761091,1.87780513509723,11.1174078682396));
#53902=CARTESIAN_POINT('Ctrl Pts',(-4.93148820012105,0.937181102537252,
11.1475437067913));
#53903=CARTESIAN_POINT('Ctrl Pts',(-4.93464332849729,-0.00183839903596135,
11.1776795453431));
#53904=CARTESIAN_POINT('Origin',(0.,0.,0.));
#53905=CARTESIAN_POINT('',(-4.9488440041135,-0.00213750530709822,12.3223204546569));
#53906=CARTESIAN_POINT('',(-4.94745353480859,-0.00311052193284108,12.1776795453431));
#53907=CARTESIAN_POINT('',(-4.942,-6.05220448138622E-16,0.));
#53908=CARTESIAN_POINT('Ctrl Pts',(-4.9488440041135,-0.00213750530709822,
12.3223204546569));
#53909=CARTESIAN_POINT('Ctrl Pts',(-4.94061448411462,1.50806390763245,12.2734955799156));
#53910=CARTESIAN_POINT('Ctrl Pts',(-4.19858957372796,3.0252638763299,12.2246707051742));
#53911=CARTESIAN_POINT('Ctrl Pts',(-2.99752188376984,3.93921020084163,12.1758458304329));
#53912=CARTESIAN_POINT('Ctrl Pts',(-1.69956742174719,4.92688201973019,12.1230823895727));
#53913=CARTESIAN_POINT('Ctrl Pts',(0.13447629685455,5.21004913441221,12.0703189487124));
#53914=CARTESIAN_POINT('Ctrl Pts',(1.669872996944,4.65983246739314,12.0175555078522));
#53915=CARTESIAN_POINT('Ctrl Pts',(3.20526969703341,4.10961580037408,11.964792066992));
#53916=CARTESIAN_POINT('Ctrl Pts',(4.44201937861055,2.72601535165399,11.9120286261318));
#53917=CARTESIAN_POINT('Ctrl Pts',(4.81723479316035,1.13875519654544,11.8592651852716));
#53918=CARTESIAN_POINT('Ctrl Pts',(5.19245020771016,-0.44850495856316,11.8065017444114));
#53919=CARTESIAN_POINT('Ctrl Pts',(4.70613135523258,-2.23942482006024,11.7537383035512));
#53920=CARTESIAN_POINT('Ctrl Pts',(3.57961864506819,-3.4188952610418,11.7009748626909));
#53921=CARTESIAN_POINT('Ctrl Pts',(2.45310593490382,-4.59836570202334,11.6482114218307));
#53922=CARTESIAN_POINT('Ctrl Pts',(0.686399367052665,-5.16638672248939,
11.5954479809705));
#53923=CARTESIAN_POINT('Ctrl Pts',(-0.916412232973623,-4.86443245089807,
11.5426845401103));
#53924=CARTESIAN_POINT('Ctrl Pts',(-2.51922383299994,-4.56247817930674,
11.4899210992501));
#53925=CARTESIAN_POINT('Ctrl Pts',(-3.95814046520138,-3.39054861565802,
11.4371576583899));
#53926=CARTESIAN_POINT('Ctrl Pts',(-4.57826175967478,-1.88202914695641,
11.3843942175297));
#53927=CARTESIAN_POINT('Ctrl Pts',(-4.82144315925703,-1.29046120861066,
11.3637029632387));
#53928=CARTESIAN_POINT('Ctrl Pts',(-4.93870801968536,-0.647131573531266,
11.3430117089478));
#53929=CARTESIAN_POINT('Ctrl Pts',(-4.93550942083981,-0.00268364051190351,
11.3223204546569));
#53930=CARTESIAN_POINT('Ctrl Pts',(-4.93464332849729,-0.00183839903596135,
11.1776795453431));
#53931=CARTESIAN_POINT('Ctrl Pts',(-4.93701583263233,-0.707935706243941,
11.200340240266));
#53932=CARTESIAN_POINT('Ctrl Pts',(-4.79546387301719,-1.41312576132387,
11.223000935189));
#53933=CARTESIAN_POINT('Ctrl Pts',(-4.50527725011862,-2.05066194500317,
11.2456616301119));
#53934=CARTESIAN_POINT('Ctrl Pts',(-3.82917937219074,-3.53604006678678,
11.2984581635866));
#53935=CARTESIAN_POINT('Ctrl Pts',(-2.34624697134931,-4.65417223228435,
11.3512546970613));
#53936=CARTESIAN_POINT('Ctrl Pts',(-0.732189317617651,-4.89557313460714,
11.404051230536));
#53937=CARTESIAN_POINT('Ctrl Pts',(0.881868336113988,-5.13697403692992,
11.4568477640108));
#53938=CARTESIAN_POINT('Ctrl Pts',(2.62705124273586,-4.50164367607793,11.5096442974855));
#53939=CARTESIAN_POINT('Ctrl Pts',(3.70815372246008,-3.27907509577412,11.5624408309602));
#53940=CARTESIAN_POINT('Ctrl Pts',(4.78925620218431,-2.05650651547028,11.6152373644349));
#53941=CARTESIAN_POINT('Ctrl Pts',(5.20627825501086,-0.246699715714593,
11.6680338979096));
#53942=CARTESIAN_POINT('Ctrl Pts',(4.76920065502008,1.32569326213742,11.7208304313843));
#53943=CARTESIAN_POINT('Ctrl Pts',(4.33212305502932,2.89808623998941,11.773626964859));
#53944=CARTESIAN_POINT('Ctrl Pts',(3.04094580222125,4.23306539593773,11.8264234983337));
#53945=CARTESIAN_POINT('Ctrl Pts',(1.48400349530759,4.72233746560275,11.8792200318084));
#53946=CARTESIAN_POINT('Ctrl Pts',(-0.0729388116060994,5.21160953526778,
11.9320165652831));
#53947=CARTESIAN_POINT('Ctrl Pts',(-1.89564617262539,4.85517451864949,11.9848130987578));
#53948=CARTESIAN_POINT('Ctrl Pts',(-3.15358830890438,3.81544470423333,12.0376096322325));
#53949=CARTESIAN_POINT('Ctrl Pts',(-4.26603410872305,2.89597231227191,12.0842996032694));
#53950=CARTESIAN_POINT('Ctrl Pts',(-4.93680336098554,1.44212692063929,12.1309895743062));
#53951=CARTESIAN_POINT('Ctrl Pts',(-4.94745353480859,-0.00311052193284108,
12.1776795453431));
#53952=CARTESIAN_POINT('Origin',(0.,0.,0.));
#53953=CARTESIAN_POINT('',(-4.94151427280004,0.00444821020356132,13.3223204546569));
#53954=CARTESIAN_POINT('',(-4.94372929093918,0.00429917225691094,13.1776795453431));
#53955=CARTESIAN_POINT('',(-4.942,-6.05220448138622E-16,0.));
#53956=CARTESIAN_POINT('Ctrl Pts',(-4.94151427280004,0.00444821020356132,
13.3223204546569));
#53957=CARTESIAN_POINT('Ctrl Pts',(-4.94510334294322,0.402329751972593,
13.3095063326037));
#53958=CARTESIAN_POINT('Ctrl Pts',(-4.90105411066494,0.799426659282486,
13.2966922105506));
#53959=CARTESIAN_POINT('Ctrl Pts',(-4.80630608075059,1.18403391346491,13.2838780884974));
#53960=CARTESIAN_POINT('Ctrl Pts',(-4.41617150483,2.76769310027955,13.2311146476372));
#53961=CARTESIAN_POINT('Ctrl Pts',(-3.16645719817481,4.13959474701713,13.178351206777));
#53962=CARTESIAN_POINT('Ctrl Pts',(-1.62595105536246,4.67533930486966,13.1255877659167));
#53963=CARTESIAN_POINT('Ctrl Pts',(-0.0854449125500667,5.21108386272221,
13.0728243250565));
#53964=CARTESIAN_POINT('Ctrl Pts',(1.74585306641946,4.91067133168968,13.0200608841963));
#53965=CARTESIAN_POINT('Ctrl Pts',(3.03445628684691,3.91082977043353,12.9672974433361));
#53966=CARTESIAN_POINT('Ctrl Pts',(4.3230595072743,2.91098820917742,12.9145340024759));
#53967=CARTESIAN_POINT('Ctrl Pts',(5.06896796915959,1.21171761769772,12.8617705616157));
#53968=CARTESIAN_POINT('Ctrl Pts',(4.9326931179398,-0.41358560700714,12.8090071207555));
#53969=CARTESIAN_POINT('Ctrl Pts',(4.79641826672,-2.03888883171205,12.7562436798952));
#53970=CARTESIAN_POINT('Ctrl Pts',(3.77796010239502,-3.59022468964221,12.703480239035));
#53971=CARTESIAN_POINT('Ctrl Pts',(2.34085390812233,-4.36152696093034,12.6507167981748));
#53972=CARTESIAN_POINT('Ctrl Pts',(0.903747713849633,-5.13282923221848,
12.5979533573146));
#53973=CARTESIAN_POINT('Ctrl Pts',(-0.952006510370724,-5.12409791686467,
12.5451899164544));
#53974=CARTESIAN_POINT('Ctrl Pts',(-2.38179129282902,-4.33930693630882,
12.4924264755942));
#53975=CARTESIAN_POINT('Ctrl Pts',(-3.81157607528729,-3.55451595575297,
12.4396630347339));
#53976=CARTESIAN_POINT('Ctrl Pts',(-4.81539141598345,-1.99366530999509,
12.3868995938737));
#53977=CARTESIAN_POINT('Ctrl Pts',(-4.93636648360977,-0.367151725568608,
12.3341361530135));
#53978=CARTESIAN_POINT('Ctrl Pts',(-4.94539675712518,-0.245739414485935,
12.3301975868946));
#53979=CARTESIAN_POINT('Ctrl Pts',(-4.94950785648002,-0.123961230389695,
12.3262590207758));
#53980=CARTESIAN_POINT('Ctrl Pts',(-4.9488440041135,-0.00213750530709822,
12.3223204546569));
#53981=CARTESIAN_POINT('Ctrl Pts',(-4.94745353480859,-0.00311052193284108,
12.1776795453431));
#53982=CARTESIAN_POINT('Ctrl Pts',(-4.94884646673765,-0.192132542820318,
12.1837861077809));
#53983=CARTESIAN_POINT('Ctrl Pts',(-4.93894745560412,-0.381007316833933,
12.1898926702188));
#53984=CARTESIAN_POINT('Ctrl Pts',(-4.91726778514412,-0.568520045648731,
12.1959992326566));
#53985=CARTESIAN_POINT('Ctrl Pts',(-4.72982821356618,-2.18973036890068,
12.2487957661313));
#53986=CARTESIAN_POINT('Ctrl Pts',(-3.6617721588716,-3.70912640319057,12.301592299606));
#53987=CARTESIAN_POINT('Ctrl Pts',(-2.19976737250484,-4.4343839504472,12.3543888330807));
#53988=CARTESIAN_POINT('Ctrl Pts',(-0.737762586138102,-5.15964149770382,
12.4071853665554));
#53989=CARTESIAN_POINT('Ctrl Pts',(1.1181909319008,-5.09076055792721,12.4599819000301));
#53990=CARTESIAN_POINT('Ctrl Pts',(2.52241404198307,-4.25912724791444,12.5127784335048));
#53991=CARTESIAN_POINT('Ctrl Pts',(3.92663715206537,-3.42749393790165,12.5655749669795));
#53992=CARTESIAN_POINT('Ctrl Pts',(4.87912985419102,-1.83310825765268,12.6183715004542));
#53993=CARTESIAN_POINT('Ctrl Pts',(4.94588170520655,-0.202463999821435,
12.6711680339289));
#53994=CARTESIAN_POINT('Ctrl Pts',(5.01263355622208,1.42818025800979,12.7239645674036));
#53995=CARTESIAN_POINT('Ctrl Pts',(4.1936445561275,3.09508309342328,12.7767611008784));
#53996=CARTESIAN_POINT('Ctrl Pts',(2.86209318500527,4.03870772815599,12.8295576343531));
#53997=CARTESIAN_POINT('Ctrl Pts',(1.53054181388302,4.98233236288871,12.8823541678278));
#53998=CARTESIAN_POINT('Ctrl Pts',(-0.313571928266912,5.20267879694063,
12.9351507013025));
#53999=CARTESIAN_POINT('Ctrl Pts',(-1.82996378449454,4.59934452509909,12.9879472347772));
#54000=CARTESIAN_POINT('Ctrl Pts',(-3.34635564072214,3.99601025325757,13.0407437682519));
#54001=CARTESIAN_POINT('Ctrl Pts',(-4.53502561102745,2.56899527552262,13.0935403017266));
#54002=CARTESIAN_POINT('Ctrl Pts',(-4.85434730874721,0.968529668713999,
13.1463368352013));
#54003=CARTESIAN_POINT('Ctrl Pts',(-4.917535847558,0.651823714081653,13.1567844052486));
#54004=CARTESIAN_POINT('Ctrl Pts',(-4.94668250438369,0.328325791222804,
13.1672319752958));
#54005=CARTESIAN_POINT('Ctrl Pts',(-4.94372929093918,0.00429917225691095,
13.1776795453431));
#54006=CARTESIAN_POINT('Origin',(0.,0.,0.));
#54007=CARTESIAN_POINT('',(-4.93448587773112,-0.00157506815688546,14.3223204546569));
#54008=CARTESIAN_POINT('',(-4.93400159721632,-0.000305393655117946,14.1776795453431));
#54009=CARTESIAN_POINT('',(-4.942,-6.05220448138622E-16,0.));
#54010=CARTESIAN_POINT('Ctrl Pts',(-4.93448587773112,-0.00157506815688546,
14.3223204546569));
#54011=CARTESIAN_POINT('Ctrl Pts',(-4.9318360603942,0.919788438910237,14.2927536444317));
#54012=CARTESIAN_POINT('Ctrl Pts',(-4.68434909382344,1.84247391790569,14.2631868342065));
#54013=CARTESIAN_POINT('Ctrl Pts',(-4.20094243104244,2.61812855704659,14.2336200239813));
#54014=CARTESIAN_POINT('Ctrl Pts',(-3.3382792398224,4.00232277240241,14.180856583121));
#54015=CARTESIAN_POINT('Ctrl Pts',(-1.72430206586684,4.91828000860559,14.1280931422608));
#54016=CARTESIAN_POINT('Ctrl Pts',(-0.0935873430086671,4.94911667465072,
14.0753297014006));
#54017=CARTESIAN_POINT('Ctrl Pts',(1.53712737984951,4.97995334069586,14.0225662605404));
#54018=CARTESIAN_POINT('Ctrl Pts',(3.18457965161027,4.12566943658293,13.9698028196802));
#54019=CARTESIAN_POINT('Ctrl Pts',(4.09895737196505,2.77507890210349,13.91703937882));
#54020=CARTESIAN_POINT('Ctrl Pts',(5.01333509231982,1.42448836762405,13.8642759379598));
#54021=CARTESIAN_POINT('Ctrl Pts',(5.19463826126858,-0.422408797221965,
13.8115124970995));
#54022=CARTESIAN_POINT('Ctrl Pts',(4.56034958089476,-1.92502627258323,13.7587490562393));
#54023=CARTESIAN_POINT('Ctrl Pts',(3.92606090052093,-3.42764374794451,13.7059856153791));
#54024=CARTESIAN_POINT('Ctrl Pts',(2.47618037082453,-4.58598153382108,13.6532221745189));
#54025=CARTESIAN_POINT('Ctrl Pts',(0.870598407947765,-4.87284032799863,
13.6004587336587));
#54026=CARTESIAN_POINT('Ctrl Pts',(-0.734983554928979,-5.15969912217617,
13.5476952927985));
#54027=CARTESIAN_POINT('Ctrl Pts',(-2.49626695098606,-4.57507892465472,
13.4949318519383));
#54028=CARTESIAN_POINT('Ctrl Pts',(-3.61163122642161,-3.38506046244813,
13.442168411078));
#54029=CARTESIAN_POINT('Ctrl Pts',(-4.45611828600162,-2.48404972171741,
13.402219092271));
#54030=CARTESIAN_POINT('Ctrl Pts',(-4.93032498439027,-1.23598765372993,
13.3622697734639));
#54031=CARTESIAN_POINT('Ctrl Pts',(-4.94151427280004,0.00444821020356132,
13.3223204546569));
#54032=CARTESIAN_POINT('Ctrl Pts',(-4.94372929093918,0.00429917225691095,
13.1776795453431));
#54033=CARTESIAN_POINT('Ctrl Pts',(-4.93175851423331,-1.30913460937943,
13.2200285087705));
#54034=CARTESIAN_POINT('Ctrl Pts',(-4.39236571089229,-2.63125521653574,
13.262377472198));
#54035=CARTESIAN_POINT('Ctrl Pts',(-3.45489131803353,-3.54492080217556,
13.3047264356254));
#54036=CARTESIAN_POINT('Ctrl Pts',(-2.28614020446586,-4.68398943037421,
13.3575229691001));
#54037=CARTESIAN_POINT('Ctrl Pts',(-0.498664552196314,-5.18821045088918,
13.4103195025748));
#54038=CARTESIAN_POINT('Ctrl Pts',(1.09305895224904,-4.82783177420557,13.4631160360495));
#54039=CARTESIAN_POINT('Ctrl Pts',(2.68478245669437,-4.46745309752197,13.5159125695242));
#54040=CARTESIAN_POINT('Ctrl Pts',(4.08075381331552,-3.2424747236398,13.5687091029989));
#54041=CARTESIAN_POINT('Ctrl Pts',(4.64488820407174,-1.71106723561516,13.6215056364736));
#54042=CARTESIAN_POINT('Ctrl Pts',(5.20902259482797,-0.179659747590474,
13.6743021699483));
#54043=CARTESIAN_POINT('Ctrl Pts',(4.94132001971923,1.6581768545767,13.727098703423));
#54044=CARTESIAN_POINT('Ctrl Pts',(3.9637611647886,2.96501853984655,13.7798952368977));
#54045=CARTESIAN_POINT('Ctrl Pts',(2.98620230985801,4.27186022511634,13.8326917703724));
#54046=CARTESIAN_POINT('Ctrl Pts',(1.29878717510559,5.04770699348884,13.8854883038471));
#54047=CARTESIAN_POINT('Ctrl Pts',(-0.32960087817538,4.93903844632007,13.9382848373218));
#54048=CARTESIAN_POINT('Ctrl Pts',(-1.95798893145639,4.8303698991513,13.9910813707965));
#54049=CARTESIAN_POINT('Ctrl Pts',(-3.52734990326595,3.8371860364412,14.0438779042712));
#54050=CARTESIAN_POINT('Ctrl Pts',(-4.32259269702876,2.41203853383676,14.0966744377459));
#54051=CARTESIAN_POINT('Ctrl Pts',(-4.72930328852039,1.68317611811527,14.1236761402783));
#54052=CARTESIAN_POINT('Ctrl Pts',(-4.93353545879958,0.841329253368597,
14.1506778428107));
#54053=CARTESIAN_POINT('Ctrl Pts',(-4.93400159721632,-0.000305393655117946,
14.1776795453431));
#54054=CARTESIAN_POINT('Origin',(0.,0.,0.));
#54055=CARTESIAN_POINT('',(-4.94718090754756,-0.00323194414963146,15.3223204546569));
#54056=CARTESIAN_POINT('',(-4.9448369857261,-0.0040807615555026,15.1776795453431));
#54057=CARTESIAN_POINT('',(-4.942,-6.05220448138622E-16,0.));
#54058=CARTESIAN_POINT('Ctrl Pts',(-4.94718090754756,-0.00323194414963146,
15.3223204546569));
#54059=CARTESIAN_POINT('Ctrl Pts',(-4.93629962156844,1.4307451373895,15.2760009562597));
#54060=CARTESIAN_POINT('Ctrl Pts',(-4.27737587184649,2.87344030248637,15.2296814578624));
#54061=CARTESIAN_POINT('Ctrl Pts',(-3.18014090814091,3.79331230684891,15.1833619594651));
#54062=CARTESIAN_POINT('Ctrl Pts',(-1.93025923583274,4.84115638505733,15.1305985186049));
#54063=CARTESIAN_POINT('Ctrl Pts',(-0.111627961864901,5.21058874364864,
15.0778350777447));
#54064=CARTESIAN_POINT('Ctrl Pts',(1.44803137056367,4.73346803090561,15.0250716368845));
#54065=CARTESIAN_POINT('Ctrl Pts',(3.00769070299228,4.25634731816257,14.9723081960243));
#54066=CARTESIAN_POINT('Ctrl Pts',(4.30837809388161,2.93267353408514,14.9195447551641));
#54067=CARTESIAN_POINT('Ctrl Pts',(4.75810604814116,1.36489607082845,14.8667813143038));
#54068=CARTESIAN_POINT('Ctrl Pts',(5.20783400240071,-0.202881392428214,
14.8140178734436));
#54069=CARTESIAN_POINT('Ctrl Pts',(4.80660252003052,-2.01476253486414,14.7612544325834));
#54070=CARTESIAN_POINT('Ctrl Pts',(3.73702582619445,-3.2460980306936,14.7084909917232));
#54071=CARTESIAN_POINT('Ctrl Pts',(2.66744913235836,-4.47743352652308,14.655727550863));
#54072=CARTESIAN_POINT('Ctrl Pts',(0.929527227056376,-5.12822337574609,
14.6029641100028));
#54073=CARTESIAN_POINT('Ctrl Pts',(-0.685751952425607,-4.90227077075043,
14.5502006691425));
#54074=CARTESIAN_POINT('Ctrl Pts',(-2.30103113190757,-4.67631816575478,
14.4974372282823));
#54075=CARTESIAN_POINT('Ctrl Pts',(-3.79366758556953,-3.57362310654048,
14.4446737874221));
#54076=CARTESIAN_POINT('Ctrl Pts',(-4.48431120815826,-2.09605997967911,
14.3919103465619));
#54077=CARTESIAN_POINT('Ctrl Pts',(-4.78794199402862,-1.44647220574097,
14.3687137159269));
#54078=CARTESIAN_POINT('Ctrl Pts',(-4.93656479099726,-0.724430485809702,
14.3455170852919));
#54079=CARTESIAN_POINT('Ctrl Pts',(-4.93448587773112,-0.00157506815688546,
14.3223204546569));
#54080=CARTESIAN_POINT('Ctrl Pts',(-4.93400159721632,-0.000305393655117946,
14.1776795453431));
#54081=CARTESIAN_POINT('Ctrl Pts',(-4.93444690105008,-0.804322229598714,
14.2034743762854));
#54082=CARTESIAN_POINT('Ctrl Pts',(-4.74893420650715,-1.60814539448429,
14.2292692072277));
#54083=CARTESIAN_POINT('Ctrl Pts',(-4.37634095459745,-2.31308827376533,
14.2550640381701));
#54084=CARTESIAN_POINT('Ctrl Pts',(-3.61372180268731,-3.75595643626419,
14.3078605716448));
#54085=CARTESIAN_POINT('Ctrl Pts',(-2.06735888315097,-4.78458161876317,
14.3606571051195));
#54086=CARTESIAN_POINT('Ctrl Pts',(-0.44186405756573,-4.93026304245127,
14.4134536385942));
#54087=CARTESIAN_POINT('Ctrl Pts',(1.18363076801951,-5.07594446613938,14.4662501720689));
#54088=CARTESIAN_POINT('Ctrl Pts',(2.88825749965368,-4.33868213101661,14.5190467055436));
#54089=CARTESIAN_POINT('Ctrl Pts',(3.89529018284092,-3.05441514934954,14.5718432390183));
#54090=CARTESIAN_POINT('Ctrl Pts',(4.90232286602818,-1.77014816768244,14.624639772493));
#54091=CARTESIAN_POINT('Ctrl Pts',(5.21176150076849,0.0611234605289337,
14.6774363059677));
#54092=CARTESIAN_POINT('Ctrl Pts',(4.682608052441,1.60496708387405,14.7302328394424));
#54093=CARTESIAN_POINT('Ctrl Pts',(4.15345460411353,3.1488107072191,14.7830293729171));
#54094=CARTESIAN_POINT('Ctrl Pts',(2.78570907271829,4.40522632569788,14.8358259063918));
#54095=CARTESIAN_POINT('Ctrl Pts',(1.20259496734194,4.80171873996239,14.8886224398665));
#54096=CARTESIAN_POINT('Ctrl Pts',(-0.380519138034476,5.19821115422692,
14.9414189733412));
#54097=CARTESIAN_POINT('Ctrl Pts',(-2.17900181739205,4.73478036427711,14.9942155068159));
#54098=CARTESIAN_POINT('Ctrl Pts',(-3.3733609497546,3.62259208519558,15.0470120402906));
#54099=CARTESIAN_POINT('Ctrl Pts',(-4.35867771010103,2.70506424759102,15.0905678753081));
#54100=CARTESIAN_POINT('Ctrl Pts',(-4.93283752130763,1.34600230443831,15.1341237103256));
#54101=CARTESIAN_POINT('Ctrl Pts',(-4.9448369857261,-0.0040807615555026,
15.1776795453431));
#54102=CARTESIAN_POINT('Origin',(0.,0.,0.));
#54103=CARTESIAN_POINT('',(-4.94384666289092,0.00426556420662083,16.3223204546569));
#54104=CARTESIAN_POINT('',(-4.94650740111161,0.00354971811832453,16.1776795453431));
#54105=CARTESIAN_POINT('',(-4.942,-6.05220448138622E-16,0.));
#54106=CARTESIAN_POINT('Ctrl Pts',(-4.94384666289092,0.00426556420662083,
16.3223204546569));
#54107=CARTESIAN_POINT('Ctrl Pts',(-4.94674943417405,0.323967179430384,
16.3120117089478));
#54108=CARTESIAN_POINT('Ctrl Pts',(-4.91837466800284,0.643155833620532,
16.3017029632387));
#54109=CARTESIAN_POINT('Ctrl Pts',(-4.85684297990262,0.955819257318147,
16.2913942175296));
#54110=CARTESIAN_POINT('Ctrl Pts',(-4.5419042203555,2.55613015167716,16.2386307766694));
#54111=CARTESIAN_POINT('Ctrl Pts',(-3.35834756654112,3.98549839996768,16.1858673358092));
#54112=CARTESIAN_POINT('Ctrl Pts',(-1.84485020909617,4.59336938114029,16.133103894949));
#54113=CARTESIAN_POINT('Ctrl Pts',(-0.331352851651252,5.20124036231289,
16.0803404540888));
#54114=CARTESIAN_POINT('Ctrl Pts',(1.51208520942422,4.98761407636759,16.0275770132286));
#54115=CARTESIAN_POINT('Ctrl Pts',(2.84645196705723,4.04971920709069,15.9748135723683));
#54116=CARTESIAN_POINT('Ctrl Pts',(4.18081872469025,3.11182433781378,15.9220501315081));
#54117=CARTESIAN_POINT('Ctrl Pts',(5.00611417888079,1.44966088520527,15.8692866906479));
#54118=CARTESIAN_POINT('Ctrl Pts',(4.94671805190497,-0.180263500133812,
15.8165232497877));
#54119=CARTESIAN_POINT('Ctrl Pts',(4.88732192492914,-1.81018788547292,15.7637598089275));
#54120=CARTESIAN_POINT('Ctrl Pts',(3.94323421678691,-3.40787320354259,15.7109963680673));
#54121=CARTESIAN_POINT('Ctrl Pts',(2.54414165016166,-4.24615799663446,15.6582329272071));
#54122=CARTESIAN_POINT('Ctrl Pts',(1.14504908353641,-5.08444278972633,15.6054694863468));
#54123=CARTESIAN_POINT('Ctrl Pts',(-0.709048341571857,-5.16332705784039,
15.5527060454866));
#54124=CARTESIAN_POINT('Ctrl Pts',(-2.17428721330366,-4.44690786540681,
15.4999426046264));
#54125=CARTESIAN_POINT('Ctrl Pts',(-3.63952608503543,-3.73048867297323,
15.4471791637662));
#54126=CARTESIAN_POINT('Ctrl Pts',(-4.71590640339076,-2.21876601999203,
15.394415722906));
#54127=CARTESIAN_POINT('Ctrl Pts',(-4.91353052724419,-0.59977679458864,
15.3416522820458));
#54128=CARTESIAN_POINT('Ctrl Pts',(-4.93766614961155,-0.402051376257967,
15.3352083395828));
#54129=CARTESIAN_POINT('Ctrl Pts',(-4.94869470590891,-0.202726026045579,
15.3287643971199));
#54130=CARTESIAN_POINT('Ctrl Pts',(-4.94718090754756,-0.00323194414963146,
15.3223204546569));
#54131=CARTESIAN_POINT('Ctrl Pts',(-4.9448369857261,-0.0040807615555026,
15.1776795453431));
#54132=CARTESIAN_POINT('Ctrl Pts',(-4.94738276248126,-0.290511052698514,
15.1869202438003));
#54133=CARTESIAN_POINT('Ctrl Pts',(-4.92462524198781,-0.576537197232804,
15.1961609422575));
#54134=CARTESIAN_POINT('Ctrl Pts',(-4.8751224347969,-0.857857073631679,
15.2054016407147));
#54135=CARTESIAN_POINT('Ctrl Pts',(-4.59228920210912,-2.46517218516427,
15.2581981741894));
#54136=CARTESIAN_POINT('Ctrl Pts',(-3.436387151366,-3.91885664001626,15.3109947076642));
#54137=CARTESIAN_POINT('Ctrl Pts',(-1.93411172090367,-4.55652821395913,
15.3637912411389));
#54138=CARTESIAN_POINT('Ctrl Pts',(-0.431836290441309,-5.19419978790203,
15.4165877746136));
#54139=CARTESIAN_POINT('Ctrl Pts',(1.41681251974025,-5.01585848093576,15.4693843080882));
#54140=CARTESIAN_POINT('Ctrl Pts',(2.76948401487652,-4.1027668473702,15.522180841563));
#54141=CARTESIAN_POINT('Ctrl Pts',(4.12215551001273,-3.18967521380468,15.5749773750377));
#54142=CARTESIAN_POINT('Ctrl Pts',(4.97884969010367,-1.54183325363995,15.6277739085124));
#54143=CARTESIAN_POINT('Ctrl Pts',(4.94920742712676,0.0899074861556964,
15.6805704419871));
#54144=CARTESIAN_POINT('Ctrl Pts',(4.91956516414985,1.72164822595137,15.7333669754618));
#54145=CARTESIAN_POINT('Ctrl Pts',(4.00358645810502,3.33728774537801,15.7861635089365));
#54146=CARTESIAN_POINT('Ctrl Pts',(2.61864387578884,4.200647779537,15.8389600424112));
#54147=CARTESIAN_POINT('Ctrl Pts',(1.23370129347265,5.06400781369599,15.8917565758859));
#54148=CARTESIAN_POINT('Ctrl Pts',(-0.620205165114908,5.17508836258739,
15.9445531093606));
#54149=CARTESIAN_POINT('Ctrl Pts',(-2.09832911795802,4.48327474299608,15.9973496428353));
#54150=CARTESIAN_POINT('Ctrl Pts',(-3.57645307080114,3.79146112340477,16.05014617631));
#54151=CARTESIAN_POINT('Ctrl Pts',(-4.67879451789979,2.29675333533074,16.1029427097847));
#54152=CARTESIAN_POINT('Ctrl Pts',(-4.90306331235317,0.680226188554136,
16.1557392432594));
#54153=CARTESIAN_POINT('Ctrl Pts',(-4.93412927302912,0.456303065875542,
16.1630526772873));
#54154=CARTESIAN_POINT('Ctrl Pts',(-4.94834669148062,0.23004246166547,16.1703661113152));
#54155=CARTESIAN_POINT('Ctrl Pts',(-4.94650740111161,0.00354971811832453,
16.1776795453431));
#54156=CARTESIAN_POINT('Origin',(0.,0.,0.));
#54157=CARTESIAN_POINT('',(-4.93403031428168,-0.000341981052076612,17.3223204546569));
#54158=CARTESIAN_POINT('',(-4.93428824426153,0.00126466874552048,17.1776795453431));
#54159=CARTESIAN_POINT('',(-4.942,-6.05220448138622E-16,0.));
#54160=CARTESIAN_POINT('Ctrl Pts',(-4.93403031428168,-0.000341981052076612,
17.3223204546569));
#54161=CARTESIAN_POINT('Ctrl Pts',(-4.93350394108414,0.843143514252388,
17.2952590207758));
#54162=CARTESIAN_POINT('Ctrl Pts',(-4.72829119907115,1.68686850434222,17.2681975868947));
#54163=CARTESIAN_POINT('Ctrl Pts',(-4.31985335744029,2.41689215977968,17.2411361530135));
#54164=CARTESIAN_POINT('Ctrl Pts',(-3.52349548532491,3.84026684640702,17.1883727121533));
#54165=CARTESIAN_POINT('Ctrl Pts',(-1.9545602926493,4.83139633972401,17.1356092712931));
#54166=CARTESIAN_POINT('Ctrl Pts',(-0.327119944589159,4.9391812045894,17.0828458304329));
#54167=CARTESIAN_POINT('Ctrl Pts',(1.30032040347096,5.04696606945479,17.0300823895727));
#54168=CARTESIAN_POINT('Ctrl Pts',(2.98626590691563,4.2714063058686,16.9773189487124));
#54169=CARTESIAN_POINT('Ctrl Pts',(3.96338272054503,2.96548703306019,16.9245555078522));
#54170=CARTESIAN_POINT('Ctrl Pts',(4.94049953417446,1.65956776025175,16.871792066992));
#54171=CARTESIAN_POINT('Ctrl Pts',(5.20878765798859,-0.176711021778891,
16.8190286261318));
#54172=CARTESIAN_POINT('Ctrl Pts',(4.64614108062899,-1.70759643201752,16.7662651852716));
#54173=CARTESIAN_POINT('Ctrl Pts',(4.0834945032694,-3.2384818422561,16.7135017444114));
#54174=CARTESIAN_POINT('Ctrl Pts',(2.68991322473609,-4.46397388070265,16.6607383035511));
#54175=CARTESIAN_POINT('Ctrl Pts',(1.09966334943406,-4.82630869971703,16.6079748626909));
#54176=CARTESIAN_POINT('Ctrl Pts',(-0.490586525867957,-5.18864351873141,
16.5552114218307));
#54177=CARTESIAN_POINT('Ctrl Pts',(-2.27750499793871,-4.68782111831362,
16.5024479809705));
#54178=CARTESIAN_POINT('Ctrl Pts',(-3.44780380133416,-3.551783147891,16.4496845401103));
#54179=CARTESIAN_POINT('Ctrl Pts',(-4.38945351416312,-2.63770050035899,
16.4072298449592));
#54180=CARTESIAN_POINT('Ctrl Pts',(-4.93189212706316,-1.31236741876541,
16.364775149808));
#54181=CARTESIAN_POINT('Ctrl Pts',(-4.94384666289092,0.00426556420662083,
16.3223204546569));
#54182=CARTESIAN_POINT('Ctrl Pts',(-4.94650740111161,0.00354971811832453,
16.1776795453431));
#54183=CARTESIAN_POINT('Ctrl Pts',(-4.93506863972457,-1.40503507794796,
16.2231626447899));
#54184=CARTESIAN_POINT('Ctrl Pts',(-4.30259793428105,-2.82259842281934,
16.2686457442367));
#54185=CARTESIAN_POINT('Ctrl Pts',(-3.23956236772638,-3.74272269838241,
16.3141288436835));
#54186=CARTESIAN_POINT('Ctrl Pts',(-2.00559648683807,-4.81079793306321,
16.3669253771582));
#54187=CARTESIAN_POINT('Ctrl Pts',(-0.191468583253334,-5.20860189694556,
16.4197219106329));
#54188=CARTESIAN_POINT('Ctrl Pts',(1.37620035566145,-4.75487224416495,16.4725184441076));
#54189=CARTESIAN_POINT('Ctrl Pts',(2.94386929457619,-4.30114259138436,16.5253149775823));
#54190=CARTESIAN_POINT('Ctrl Pts',(4.265079268821,-2.99587932194087,16.578111511057));
#54191=CARTESIAN_POINT('Ctrl Pts',(4.73781104997921,-1.43383540748133,16.6309080445317));
#54192=CARTESIAN_POINT('Ctrl Pts',(5.21054283113743,0.128208506978224,16.6837045780064));
#54193=CARTESIAN_POINT('Ctrl Pts',(4.83479641920902,1.94703306645383,16.7365011114811));
#54194=CARTESIAN_POINT('Ctrl Pts',(3.78178347511922,3.19387716968194,16.7892976449558));
#54195=CARTESIAN_POINT('Ctrl Pts',(2.72877053102942,4.44072127291004,16.8420941784306));
#54196=CARTESIAN_POINT('Ctrl Pts',(0.998491054778278,5.11558491989063,16.8948907119053));
#54197=CARTESIAN_POINT('Ctrl Pts',(-0.620640115192454,4.91096152429156,
16.94768724538));
#54198=CARTESIAN_POINT('Ctrl Pts',(-2.23977128516316,4.70633812869249,17.0004837788547));
#54199=CARTESIAN_POINT('Ctrl Pts',(-3.74775414885348,3.62222769051368,17.0532803123294));
#54200=CARTESIAN_POINT('Ctrl Pts',(-4.45746504028889,2.1526130784761,17.1060768458041));
#54201=CARTESIAN_POINT('Ctrl Pts',(-4.77830186027552,1.48824892058866,17.1299444123171));
#54202=CARTESIAN_POINT('Ctrl Pts',(-4.93600022440261,0.745101393327629,
17.1538119788301));
#54203=CARTESIAN_POINT('Ctrl Pts',(-4.93428824426153,0.00126466874552048,
17.1776795453431));
#54204=CARTESIAN_POINT('Origin',(0.,0.,0.));
#54205=CARTESIAN_POINT('',(-4.94522242777803,-0.0039236424385497,18.3223204546569));
#54206=CARTESIAN_POINT('',(-4.94192999916445,-0.00446510791632448,18.1776795453431));
#54207=CARTESIAN_POINT('',(-4.942,-6.05220448138622E-16,0.));
#54208=CARTESIAN_POINT('Ctrl Pts',(-4.94522242777803,-0.0039236424385497,
18.3223204546569));
#54209=CARTESIAN_POINT('Ctrl Pts',(-4.93329330491003,1.35399213993734,18.2785063326037));
#54210=CARTESIAN_POINT('Ctrl Pts',(-4.3513066594067,2.72080403156538,18.2346922105506));
#54211=CARTESIAN_POINT('Ctrl Pts',(-3.35561026819536,3.63892235657103,18.1908780884974));
#54212=CARTESIAN_POINT('Ctrl Pts',(-2.15653642646331,4.74457230855067,18.1381146476372));
#54213=CARTESIAN_POINT('Ctrl Pts',(-0.35748677154393,5.19951173147208,18.085351206777));
#54214=CARTESIAN_POINT('Ctrl Pts',(1.22293027595834,4.79656649826054,18.0325877659168));
#54215=CARTESIAN_POINT('Ctrl Pts',(2.80334732346066,4.39362126504898,17.9798243250565));
#54216=CARTESIAN_POINT('Ctrl Pts',(4.16513176354582,3.13279137570437,17.9270608841963));
#54217=CARTESIAN_POINT('Ctrl Pts',(4.68838366687364,1.58798426669984,17.8742974433361));
#54218=CARTESIAN_POINT('Ctrl Pts',(5.21163557020145,0.0431771576953521,
17.8215340024759));
#54219=CARTESIAN_POINT('Ctrl Pts',(4.89635493677199,-1.78560717096906,17.7687705616157));
#54220=CARTESIAN_POINT('Ctrl Pts',(3.88609177304056,-3.06605780050668,17.7160071207555));
#54221=CARTESIAN_POINT('Ctrl Pts',(2.87582860930912,-4.34650843004432,17.6632436798953));
#54222=CARTESIAN_POINT('Ctrl Pts',(1.17058291527568,-5.07862536045516,17.610480239035));
#54223=CARTESIAN_POINT('Ctrl Pts',(-0.453558190725748,-4.92918049163674,
17.5577167981748));
#54224=CARTESIAN_POINT('Ctrl Pts',(-2.0776992967272,-4.77973562281832,17.5049533573146));
#54225=CARTESIAN_POINT('Ctrl Pts',(-3.62073581469659,-3.74872895477065,
17.4521899164544));
#54226=CARTESIAN_POINT('Ctrl Pts',(-4.38036379790372,-2.30541568077795,
17.3994264755942));
#54227=CARTESIAN_POINT('Ctrl Pts',(-4.75039204866972,-1.6023522103828,17.3737244686151));
#54228=CARTESIAN_POINT('Ctrl Pts',(-4.93453024520391,-0.801455114314277,
17.348022461636));
#54229=CARTESIAN_POINT('Ctrl Pts',(-4.93403031428168,-0.000341981052076612,
17.3223204546569));
#54230=CARTESIAN_POINT('Ctrl Pts',(-4.93428824426153,0.00126466874552048,
17.1776795453431));
#54231=CARTESIAN_POINT('Ctrl Pts',(-4.93221321843459,-0.900311452079429,
17.2066085123048));
#54232=CARTESIAN_POINT('Ctrl Pts',(-4.69594942149747,-1.80290006851385,
17.2355374792665));
#54233=CARTESIAN_POINT('Ctrl Pts',(-4.23213525097133,-2.56744414176908,
17.2644664462282));
#54234=CARTESIAN_POINT('Ctrl Pts',(-3.38565565103777,-3.96276796408032,
17.3172629797029));
#54235=CARTESIAN_POINT('Ctrl Pts',(-1.78125753199004,-4.89829682280636,
17.3700595131776));
#54236=CARTESIAN_POINT('Ctrl Pts',(-0.149997058388728,-4.94775064594635,
17.4228560466523));
#54237=CARTESIAN_POINT('Ctrl Pts',(1.48126341521252,-4.99720446908635,17.475652580127));
#54238=CARTESIAN_POINT('Ctrl Pts',(3.13938624336737,-4.16058325664038,17.5284491136017));
#54239=CARTESIAN_POINT('Ctrl Pts',(4.06883557073125,-2.81909846013186,17.5812456470764));
#54240=CARTESIAN_POINT('Ctrl Pts',(4.99828489809513,-1.47761366362332,17.6340421805511));
#54241=CARTESIAN_POINT('Ctrl Pts',(5.19906072466804,0.368734716947733,17.6868387140258));
#54242=CARTESIAN_POINT('Ctrl Pts',(4.57967756755998,1.87864175098721,17.7396352475005));
#54243=CARTESIAN_POINT('Ctrl Pts',(3.9602944104519,3.38854878502672,17.7924317809752));
#54244=CARTESIAN_POINT('Ctrl Pts',(2.52075226966277,4.56201447253459,17.8452283144499));
#54245=CARTESIAN_POINT('Ctrl Pts',(0.916990219673444,4.86434504442812,17.8980248479246));
#54246=CARTESIAN_POINT('Ctrl Pts',(-0.68677183031584,5.16667561632164,17.9508213813993));
#54247=CARTESIAN_POINT('Ctrl Pts',(-2.45475378950534,4.59787107260088,18.003617914874));
#54248=CARTESIAN_POINT('Ctrl Pts',(-3.58136314295608,3.4171025376229,18.0564144483487));
#54249=CARTESIAN_POINT('Ctrl Pts',(-4.44390962426003,2.51309109660283,18.0968361473469));
#54250=CARTESIAN_POINT('Ctrl Pts',(-4.93050729338922,1.25036908149785,18.137257846345));
#54251=CARTESIAN_POINT('Ctrl Pts',(-4.94192999916445,-0.00446510791632448,
18.1776795453431));
#54252=CARTESIAN_POINT('Origin',(0.,0.,-1.84858989190501));
#54253=CARTESIAN_POINT('',(-4.37485075966118,-0.00347109768167049,18.651410108095));
#54254=CARTESIAN_POINT('',(-4.37798451307649,0.0018411544964702,18.848589891905));
#54255=CARTESIAN_POINT('',(-4.372,-4.40683631492666E-13,-1.84858989190501));
#54256=CARTESIAN_POINT('',(-4.32479004603203,0.640761311052912,19.628));
#54257=CARTESIAN_POINT('Ctrl Pts',(-4.37485075966118,-0.00347109768167011,
18.651410108095));
#54258=CARTESIAN_POINT('Ctrl Pts',(-4.37700632796887,-0.248843725443851,
18.660359426902));
#54259=CARTESIAN_POINT('Ctrl Pts',(-4.24678226663423,-1.93862138449445,
18.7220721865693));
#54260=CARTESIAN_POINT('Ctrl Pts',(-2.04533412033072,-4.73987705500777,
18.8365483870968));
#54261=CARTESIAN_POINT('Ctrl Pts',(2.85792925831606,-4.29723869811459,18.9948387096774));
#54262=CARTESIAN_POINT('Ctrl Pts',(5.16462833680317,0.0542185969503185,
19.1531290322581));
#54263=CARTESIAN_POINT('Ctrl Pts',(2.76051461044002,4.36178489183685,19.3114193548387));
#54264=CARTESIAN_POINT('Ctrl Pts',(-1.32005059452733,4.63359119197125,19.4433279569892));
#54265=CARTESIAN_POINT('Ctrl Pts',(-3.63987183575178,2.72812739966123,19.5488548387097));
#54266=CARTESIAN_POINT('Ctrl Pts',(-4.21857665773145,1.35764386397051,19.6016182795699));
#54267=CARTESIAN_POINT('Ctrl Pts',(-4.32479004603219,0.640761311051878,
19.628));
#54268=CARTESIAN_POINT('',(-0.803308159453264,4.29756675351946,19.628));
#54269=CARTESIAN_POINT('Origin',(0.,0.,19.628));
#54270=CARTESIAN_POINT('Ctrl Pts',(-4.37798451307649,0.00184115449647014,
18.848589891905));
#54271=CARTESIAN_POINT('Ctrl Pts',(-4.37034287302321,-1.32832166361097,
18.8972071273712));
#54272=CARTESIAN_POINT('Ctrl Pts',(-3.01402217294637,-4.11556359956004,
18.9986208963121));
#54273=CARTESIAN_POINT('Ctrl Pts',(1.72525842040716,-4.86940713488401,19.1528311987277));
#54274=CARTESIAN_POINT('Ctrl Pts',(5.02276837180745,-1.19521866677756,19.3112207991518));
#54275=CARTESIAN_POINT('Ctrl Pts',(3.95306672650205,2.75529758855723,19.4432121328385));
#54276=CARTESIAN_POINT('Ctrl Pts',(1.3947178009747,4.32991044428859,19.548805199788));
#54277=CARTESIAN_POINT('Ctrl Pts',(-0.0904913830656236,4.43080762341373,
19.6016017332627));
#54278=CARTESIAN_POINT('Ctrl Pts',(-0.803308159453631,4.29756675351939,
19.628));
#54279=CARTESIAN_POINT('Origin',(0.,0.,-1.84858989190501));
#54280=CARTESIAN_POINT('',(-4.36494952125445,-0.000302537669007011,17.651410108095));
#54281=CARTESIAN_POINT('',(-4.37193807291522,-0.0039501116577445,17.848589891905));
#54282=CARTESIAN_POINT('',(-4.372,-4.40683631492666E-13,-1.84858989190501));
#54283=CARTESIAN_POINT('Ctrl Pts',(-4.36494952125446,-0.000302537669007175,
17.651410108095));
#54284=CARTESIAN_POINT('Ctrl Pts',(-4.36539179118401,-0.709016948559791,
17.6771121150741));
#54285=CARTESIAN_POINT('Ctrl Pts',(-3.86807546336294,-2.87206193474975,
17.7555775629134));
#54286=CARTESIAN_POINT('Ctrl Pts',(-0.472995886023615,-5.14054336213398,
17.8868064516129));
#54287=CARTESIAN_POINT('Ctrl Pts',(4.05270272242283,-3.19751510246813,18.0450967741935));
#54288=CARTESIAN_POINT('Ctrl Pts',(4.88945318540557,1.65605334244537,18.2033870967742));
#54289=CARTESIAN_POINT('Ctrl Pts',(1.27529601904452,5.00227852023644,18.3616774193548));
#54290=CARTESIAN_POINT('Ctrl Pts',(-3.22941067771149,3.86313894204385,18.5110184231284));
#54291=CARTESIAN_POINT('Ctrl Pts',(-4.36429751701074,1.19782550299575,18.6075959860418));
#54292=CARTESIAN_POINT('Ctrl Pts',(-4.37485075966118,-0.00347109768167011,
18.651410108095));
#54293=CARTESIAN_POINT('Ctrl Pts',(-4.37193807291522,-0.00395011165774454,
17.848589891905));
#54294=CARTESIAN_POINT('Ctrl Pts',(-4.37503172333717,-0.34380114135277,
17.8609647263816));
#54295=CARTESIAN_POINT('Ctrl Pts',(-4.18383382909851,-2.13016311819971,
17.9261360943329));
#54296=CARTESIAN_POINT('Ctrl Pts',(-1.7333097832156,-4.86367572142824,18.0441039957589));
#54297=CARTESIAN_POINT('Ctrl Pts',(3.13645552043595,-4.10159948955856,18.202493596183));
#54298=CARTESIAN_POINT('Ctrl Pts',(5.14796384574126,0.398543369117654,18.3608831966071));
#54299=CARTESIAN_POINT('Ctrl Pts',(2.46797524199195,4.53507188733415,18.5192727970312));
#54300=CARTESIAN_POINT('Ctrl Pts',(-2.46096278237594,4.53951629179981,18.6776623974553));
#54301=CARTESIAN_POINT('Ctrl Pts',(-4.32286248336998,1.67443240118537,18.7874347624133));
#54302=CARTESIAN_POINT('Ctrl Pts',(-4.37864141367461,0.116186340178791,
18.8444105938965));
#54303=CARTESIAN_POINT('Ctrl Pts',(-4.37798451307649,0.00184115449647014,
18.848589891905));
#54304=CARTESIAN_POINT('Origin',(0.,0.,-1.84858989190501));
#54305=CARTESIAN_POINT('',(-4.37363367263438,0.00377358290378073,16.651410108095));
#54306=CARTESIAN_POINT('',(-4.36517770212695,0.0011188044825361,16.848589891905));
#54307=CARTESIAN_POINT('',(-4.372,-4.40683631492666E-13,-1.84858989190501));
#54308=CARTESIAN_POINT('Ctrl Pts',(-4.37363367263438,0.00377358290378063,
16.651410108095));
#54309=CARTESIAN_POINT('Ctrl Pts',(-4.36305794810196,-1.16100169057931,
16.6938648032461));
#54310=CARTESIAN_POINT('Ctrl Pts',(-3.28678615689719,-3.7906423093463,16.7890829392575));
#54311=CARTESIAN_POINT('Ctrl Pts',(1.14681571606612,-5.03325475486043,16.937064516129));
#54312=CARTESIAN_POINT('Ctrl Pts',(4.84536125415653,-1.78081574711759,17.0953548387097));
#54313=CARTESIAN_POINT('Ctrl Pts',(4.13332826509411,3.09264287390914,17.2536451612903));
#54314=CARTESIAN_POINT('Ctrl Pts',(-0.341147903092961,5.15096781506579,
17.411935483871));
#54315=CARTESIAN_POINT('Ctrl Pts',(-3.82897189620604,2.94763574423766,17.5445237994725));
#54316=CARTESIAN_POINT('Ctrl Pts',(-4.36448385884661,0.745897095166127,
17.6243486742139));
#54317=CARTESIAN_POINT('Ctrl Pts',(-4.36494952125446,-0.000302537669007175,
17.651410108095));
#54318=CARTESIAN_POINT('Ctrl Pts',(-4.36517770212695,0.0011188044825361,
16.848589891905));
#54319=CARTESIAN_POINT('Ctrl Pts',(-4.36334200546248,-0.796471401961387,
16.8775188588667));
#54320=CARTESIAN_POINT('Ctrl Pts',(-3.77287007871479,-3.05222639411641,
16.9592443593031));
#54321=CARTESIAN_POINT('Ctrl Pts',(-0.156460816144074,-5.16096436253732,
17.0937663932142));
#54322=CARTESIAN_POINT('Ctrl Pts',(4.24417435465306,-2.94058317628852,17.2521559936383));
#54323=CARTESIAN_POINT('Ctrl Pts',(4.7770306357801,1.95960002071087,17.4105455940624));
#54324=CARTESIAN_POINT('Ctrl Pts',(0.956505601666415,5.07396180892462,17.5689351944865));
#54325=CARTESIAN_POINT('Ctrl Pts',(-3.36909691713057,3.68230599805327,17.7149499604341));
#54326=CARTESIAN_POINT('Ctrl Pts',(-4.36183283826352,1.10615411256716,17.8081681929069));
#54327=CARTESIAN_POINT('Ctrl Pts',(-4.37193807291522,-0.00395011165774454,
17.848589891905));
#54328=CARTESIAN_POINT('Origin',(0.,0.,-1.84858989190501));
#54329=CARTESIAN_POINT('',(-4.37658335244799,-0.00285917843438755,15.651410108095));
#54330=CARTESIAN_POINT('',(-4.37598752684337,0.00314030101388529,15.848589891905));
#54331=CARTESIAN_POINT('',(-4.372,-4.40683631492666E-13,-1.84858989190501));
#54332=CARTESIAN_POINT('Ctrl Pts',(-4.37658335244799,-0.00285917843438723,
15.651410108095));
#54333=CARTESIAN_POINT('Ctrl Pts',(-4.37792255245523,-0.179344027897961,
15.657854050558));
#54334=CARTESIAN_POINT('Ctrl Pts',(-4.28827874574891,-1.79952736688815,
15.7170614338811));
#54335=CARTESIAN_POINT('Ctrl Pts',(-2.26751786562628,-4.63758557609733,
15.8290322580645));
#54336=CARTESIAN_POINT('Ctrl Pts',(2.65323118895075,-4.42822781393943,15.9873225806452));
#54337=CARTESIAN_POINT('Ctrl Pts',(5.15882697608013,-0.187992963311806,
16.1456129032258));
#54338=CARTESIAN_POINT('Ctrl Pts',(2.96850419640318,4.22336596918787,16.3039032258064));
#54339=CARTESIAN_POINT('Ctrl Pts',(-1.92395505269964,4.79032719267193,16.4621935483871));
#54340=CARTESIAN_POINT('Ctrl Pts',(-4.22261913325801,2.01425606870238,16.5780291758166));
#54341=CARTESIAN_POINT('Ctrl Pts',(-4.37620164431587,0.286601478848438,
16.6411013623859));
#54342=CARTESIAN_POINT('Ctrl Pts',(-4.37363367263438,0.00377358290378063,
16.651410108095));
#54343=CARTESIAN_POINT('Ctrl Pts',(-4.37598752684337,0.00314030101388495,
15.848589891905));
#54344=CARTESIAN_POINT('Ctrl Pts',(-4.36586808840044,-1.24298125471277,
15.8940729913518));
#54345=CARTESIAN_POINT('Ctrl Pts',(-3.15685416964687,-3.95275705920985,
15.9923526242733));
#54346=CARTESIAN_POINT('Ctrl Pts',(1.43550516966593,-4.9597746708902,16.1434287906695));
#54347=CARTESIAN_POINT('Ctrl Pts',(4.94197826197569,-1.49562391370258,16.3018183910937));
#54348=CARTESIAN_POINT('Ctrl Pts',(3.94475245484231,3.3315114408263,16.4602079915177));
#54349=CARTESIAN_POINT('Ctrl Pts',(-0.647385467154988,5.12259027405121,
16.6185975919419));
#54350=CARTESIAN_POINT('Ctrl Pts',(-3.91857823830144,2.77088302731469,16.7480582254043));
#54351=CARTESIAN_POINT('Ctrl Pts',(-4.36669222603978,0.659162948528226,
16.824722325392));
#54352=CARTESIAN_POINT('Ctrl Pts',(-4.36517770212695,0.0011188044825361,
16.848589891905));
#54353=CARTESIAN_POINT('Origin',(0.,0.,-1.84858989190501));
#54354=CARTESIAN_POINT('',(-4.36535254096326,-0.00139340307212889,14.651410108095));
#54355=CARTESIAN_POINT('',(-4.37450977369375,-0.00361009500681242,14.848589891905));
#54356=CARTESIAN_POINT('',(-4.372,-4.40683631492666E-13,-1.84858989190501));
#54357=CARTESIAN_POINT('Ctrl Pts',(-4.36535254096326,-0.00139340307212868,
14.651410108095));
#54358=CARTESIAN_POINT('Ctrl Pts',(-4.36719167669768,-0.640876180485729,
14.67460673873));
#54359=CARTESIAN_POINT('Ctrl Pts',(-3.93664196772952,-2.73257986740296,
14.7505668102252));
#54360=CARTESIAN_POINT('Ctrl Pts',(-0.715156117622299,-5.11247386069707,
14.8792903225806));
#54361=CARTESIAN_POINT('Ctrl Pts',(3.89726470591888,-3.38528655547465,15.0375806451613));
#54362=CARTESIAN_POINT('Ctrl Pts',(4.96212753934002,1.42342106576975,15.1958709677419));
#54363=CARTESIAN_POINT('Ctrl Pts',(1.5101211008729,4.93643307547415,15.3541612903226));
#54364=CARTESIAN_POINT('Ctrl Pts',(-3.1200112045152,3.99587919704142,15.5060076704403));
#54365=CARTESIAN_POINT('Ctrl Pts',(-4.36695709135924,1.26572596937806,15.6050906096977));
#54366=CARTESIAN_POINT('Ctrl Pts',(-4.37658335244799,-0.00285917843438723,
15.651410108095));
#54367=CARTESIAN_POINT('Ctrl Pts',(-4.37450977369375,-0.00361009500681263,
14.848589891905));
#54368=CARTESIAN_POINT('Ctrl Pts',(-4.37676192585348,-0.2570041121813,14.8578305903622));
#54369=CARTESIAN_POINT('Ctrl Pts',(-4.24160137044629,-1.95575914866763,
14.9198678222941));
#54370=CARTESIAN_POINT('Ctrl Pts',(-2.01745869282129,-4.75288338056742,
15.0347015877008));
#54371=CARTESIAN_POINT('Ctrl Pts',(2.88882981271105,-4.27956800578602,15.1930911881249));
#54372=CARTESIAN_POINT('Ctrl Pts',(5.16248437889336,0.0937818828261288,
15.351480788549));
#54373=CARTESIAN_POINT('Ctrl Pts',(2.73148949656154,4.38166693681219,15.5098703889731));
#54374=CARTESIAN_POINT('Ctrl Pts',(-2.18875273549729,4.67647318514471,15.6682599893972));
#54375=CARTESIAN_POINT('Ctrl Pts',(-4.27423782525496,1.84868256384714,15.7811664903745));
#54376=CARTESIAN_POINT('Ctrl Pts',(-4.37761467728721,0.203509842654685,
15.8412764578771));
#54377=CARTESIAN_POINT('Ctrl Pts',(-4.37598752684337,0.00314030101388495,
15.848589891905));
#54378=CARTESIAN_POINT('Origin',(0.,0.,-1.84858989190501));
#54379=CARTESIAN_POINT('',(-4.3715702955649,0.00393516289142377,13.651410108095));
#54380=CARTESIAN_POINT('',(-4.36492411635568,-0.000270170186619789,13.848589891905));
#54381=CARTESIAN_POINT('',(-4.372,-4.40683631492666E-13,-1.84858989190501));
#54382=CARTESIAN_POINT('Ctrl Pts',(-4.3715702955649,0.00393516289142415,
13.651410108095));
#54383=CARTESIAN_POINT('Ctrl Pts',(-4.36167155640512,-1.09343140876319,
13.691359426902));
#54384=CARTESIAN_POINT('Ctrl Pts',(-3.38808352462445,-3.65581253168041,
13.7840721865693));
#54385=CARTESIAN_POINT('Ctrl Pts',(0.907928552289056,-5.08178147829179,
13.9295483870968));
#54386=CARTESIAN_POINT('Ctrl Pts',(4.75589152831045,-2.00756893285326,14.0878387096774));
#54387=CARTESIAN_POINT('Ctrl Pts',(4.2747154125816,2.89407073006048,14.2461290322581));
#54388=CARTESIAN_POINT('Ctrl Pts',(-0.0976002483683332,5.16132845696157,
14.4044193548387));
#54389=CARTESIAN_POINT('Ctrl Pts',(-3.75335254656528,3.08663197095523,14.5395130467844));
#54390=CARTESIAN_POINT('Ctrl Pts',(-4.36300834804604,0.813701953645304,
14.6218432978698));
#54391=CARTESIAN_POINT('Ctrl Pts',(-4.36535254096326,-0.00139340307212868,
14.651410108095));
#54392=CARTESIAN_POINT('Ctrl Pts',(-4.36492411635568,-0.000270170186619789,
13.848589891905));
#54393=CARTESIAN_POINT('Ctrl Pts',(-4.36531805977148,-0.711553376731479,
13.8743847228474));
#54394=CARTESIAN_POINT('Ctrl Pts',(-3.86529136737144,-2.8781600308068,13.9529760872644));
#54395=CARTESIAN_POINT('Ctrl Pts',(-0.460905372910369,-5.14272362102755,
14.0843639851561));
#54396=CARTESIAN_POINT('Ctrl Pts',(4.06315051784514,-3.18603952805496,14.2427535855802));
#54397=CARTESIAN_POINT('Ctrl Pts',(4.88439639669049,1.67413017563193,14.4011431860043));
#54398=CARTESIAN_POINT('Ctrl Pts',(1.25441857601452,5.00863993928383,14.5595327864284));
#54399=CARTESIAN_POINT('Ctrl Pts',(-3.24025672884045,3.85045757200017,14.7086816883953));
#54400=CARTESIAN_POINT('Ctrl Pts',(-4.36389430254103,1.19075719850307,14.8050340568875));
#54401=CARTESIAN_POINT('Ctrl Pts',(-4.37450977369375,-0.00361009500681263,
14.848589891905));
#54402=CARTESIAN_POINT('Origin',(0.,0.,-1.84858989190501));
#54403=CARTESIAN_POINT('',(-4.37805463091546,-0.00189096989131645,12.651410108095));
#54404=CARTESIAN_POINT('',(-4.3735298381194,0.00380331467108683,12.848589891905));
#54405=CARTESIAN_POINT('',(-4.372,-4.40683631492666E-13,-1.84858989190501));
#54406=CARTESIAN_POINT('Ctrl Pts',(-4.37805463091546,-0.00189096989131629,
12.651410108095));
#54407=CARTESIAN_POINT('Ctrl Pts',(-4.37864191593093,-0.109663799931991,
12.6553486742139));
#54408=CARTESIAN_POINT('Ctrl Pts',(-4.32628239365674,-1.66064736718339,
12.7120506811929));
#54409=CARTESIAN_POINT('Ctrl Pts',(-2.4839194519693,-4.5253708583176,12.8215161290323));
#54410=CARTESIAN_POINT('Ctrl Pts',(2.44122672465452,-4.54854364912704,12.9798064516129));
#54411=CARTESIAN_POINT('Ctrl Pts',(5.14420067918421,-0.431319627959304,
13.1380967741936));
#54412=CARTESIAN_POINT('Ctrl Pts',(3.16456988475122,4.07852114052473,13.2963870967742));
#54413=CARTESIAN_POINT('Ctrl Pts',(-1.69566975348524,4.87581186432528,13.4546774193548));
#54414=CARTESIAN_POINT('Ctrl Pts',(-4.17531922896613,2.15372155886245,13.5730184231284));
#54415=CARTESIAN_POINT('Ctrl Pts',(-4.37474540982351,0.355925875277971,
13.6385959860418));
#54416=CARTESIAN_POINT('Ctrl Pts',(-4.3715702955649,0.00393516289142415,
13.651410108095));
#54417=CARTESIAN_POINT('Ctrl Pts',(-4.3735298381194,0.00380331467108686,
12.848589891905));
#54418=CARTESIAN_POINT('Ctrl Pts',(-4.36293974589787,-1.15814174670351,
12.8909388553325));
#54419=CARTESIAN_POINT('Ctrl Pts',(-3.29085772231164,-3.78595162322649,
12.9860843522346));
#54420=CARTESIAN_POINT('Ctrl Pts',(1.14016230868481,-5.03587826648703,13.1340263826114));
#54421=CARTESIAN_POINT('Ctrl Pts',(4.84505108113381,-1.78480251743019,13.2924159830355));
#54422=CARTESIAN_POINT('Ctrl Pts',(4.13457213027864,3.09279053680373,13.4508055834596));
#54423=CARTESIAN_POINT('Ctrl Pts',(-0.343804419177731,5.15187718471428,
13.6091951838838));
#54424=CARTESIAN_POINT('Ctrl Pts',(-3.8305579098897,2.94525464061577,13.7417899533655));
#54425=CARTESIAN_POINT('Ctrl Pts',(-4.36451174137436,0.744292087358565,
13.8215881893726));
#54426=CARTESIAN_POINT('Ctrl Pts',(-4.36492411635568,-0.000270170186619789,
13.848589891905));
#54427=CARTESIAN_POINT('Origin',(0.,0.,-1.84858989190501));
#54428=CARTESIAN_POINT('',(-4.3662580307389,-0.00237411499775451,11.651410108095));
#54429=CARTESIAN_POINT('',(-4.37682453544783,-0.00275176080394124,11.848589891905));
#54430=CARTESIAN_POINT('',(-4.372,-4.40683631492666E-13,-1.84858989190501));
#54431=CARTESIAN_POINT('Ctrl Pts',(-4.3662580307389,-0.00237411499775443,
11.651410108095));
#54432=CARTESIAN_POINT('Ctrl Pts',(-4.36908770984708,-0.57249276395778,
11.6721013623859));
#54433=CARTESIAN_POINT('Ctrl Pts',(-4.00080778508103,-2.59292231754593,
11.745556057537));
#54434=CARTESIAN_POINT('Ctrl Pts',(-0.955706815437237,-5.07301308219371,
11.8717741935484));
#54435=CARTESIAN_POINT('Ctrl Pts',(3.73310810644377,-3.5654931096253,12.030064516129));
#54436=CARTESIAN_POINT('Ctrl Pts',(5.02379164936073,1.1875835604264,12.1883548387097));
#54437=CARTESIAN_POINT('Ctrl Pts',(1.74147501164997,4.85964011352491,12.3466451612903));
#54438=CARTESIAN_POINT('Ctrl Pts',(-3.00493840101716,4.12681778354368,12.5009969177521));
#54439=CARTESIAN_POINT('Ctrl Pts',(-4.3707742866348,1.33412695349428,12.6025852333536));
#54440=CARTESIAN_POINT('Ctrl Pts',(-4.37805463091546,-0.00189096989131629,
12.651410108095));
#54441=CARTESIAN_POINT('Ctrl Pts',(-4.37682453544783,-0.0027517608039412,
11.848589891905));
#54442=CARTESIAN_POINT('Ctrl Pts',(-4.37805680950565,-0.169972374992373,
11.8546964543429));
#54443=CARTESIAN_POINT('Ctrl Pts',(-4.29358524369388,-1.7817038588778,11.9135995502554));
#54444=CARTESIAN_POINT('Ctrl Pts',(-2.29456228398659,-4.62547553554524,
12.0252991796426));
#54445=CARTESIAN_POINT('Ctrl Pts',(2.63111281568934,-4.44266646915302,12.1836887800668));
#54446=CARTESIAN_POINT('Ctrl Pts',(5.15901534120123,-0.211188811899807,
12.3420783804909));
#54447=CARTESIAN_POINT('Ctrl Pts',(2.98542980392062,4.2127483773522,12.500467980915));
#54448=CARTESIAN_POINT('Ctrl Pts',(-1.90882269345658,4.79754478144462,12.6588575813391));
#54449=CARTESIAN_POINT('Ctrl Pts',(-4.22005393336117,2.0228792487521,12.7748982183358));
#54450=CARTESIAN_POINT('Ctrl Pts',(-4.37614243406833,0.290457377422949,
12.8381423218578));
#54451=CARTESIAN_POINT('Ctrl Pts',(-4.3735298381194,0.00380331467108686,
12.848589891905));
#54452=CARTESIAN_POINT('Origin',(0.,0.,-1.84858989190501));
#54453=CARTESIAN_POINT('',(-4.36958950328423,0.00375500997191766,10.651410108095));
#54454=CARTESIAN_POINT('',(-4.36549183168559,-0.00162636191587406,10.848589891905));
#54455=CARTESIAN_POINT('',(-4.372,-4.40683631492666E-13,-1.84858989190501));
#54456=CARTESIAN_POINT('Ctrl Pts',(-4.36958950328423,0.00375500997191747,
10.651410108095));
#54457=CARTESIAN_POINT('Ctrl Pts',(-4.36106090852754,-1.0259785981898,10.688854050558));
#54458=CARTESIAN_POINT('Ctrl Pts',(-3.48414488794968,-3.51981628552574,
10.7790614338811));
#54459=CARTESIAN_POINT('Ctrl Pts',(0.667017186951725,-5.11897697997292,
10.9220322580645));
#54460=CARTESIAN_POINT('Ctrl Pts',(4.65581649466175,-2.22984528997355,11.0803225806452));
#54461=CARTESIAN_POINT('Ctrl Pts',(4.40657187915952,2.68904472312794,11.2386129032258));
#54462=CARTESIAN_POINT('Ctrl Pts',(0.14616290696869,5.16018155240764,11.3969032258064));
#54463=CARTESIAN_POINT('Ctrl Pts',(-3.67299362448513,3.22514497791193,11.5345022940962));
#54464=CARTESIAN_POINT('Ctrl Pts',(-4.36187192659012,0.881330247193059,
11.6193379215257));
#54465=CARTESIAN_POINT('Ctrl Pts',(-4.3662580307389,-0.00237411499775443,
11.651410108095));
#54466=CARTESIAN_POINT('Ctrl Pts',(-4.36549183168559,-0.00162636191587386,
10.848589891905));
#54467=CARTESIAN_POINT('Ctrl Pts',(-4.36759069612872,-0.626283874484138,
10.871250586828));
#54468=CARTESIAN_POINT('Ctrl Pts',(-3.95060522485931,-2.70364125089475,
10.9467078152256));
#54469=CARTESIAN_POINT('Ctrl Pts',(-0.763741663751577,-5.10653881568242,
11.074961577098));
#54470=CARTESIAN_POINT('Ctrl Pts',(3.86794975738412,-3.42038077988013,11.2333511775221));
#54471=CARTESIAN_POINT('Ctrl Pts',(4.97472054752429,1.38282156443299,11.3917407779462));
#54472=CARTESIAN_POINT('Ctrl Pts',(1.54795388466898,4.92583787552529,11.5501303783703));
#54473=CARTESIAN_POINT('Ctrl Pts',(-3.10298340129681,4.01633537157594,11.7024134163566));
#54474=CARTESIAN_POINT('Ctrl Pts',(-4.36740273051995,1.27579500142313,11.8018999208682));
#54475=CARTESIAN_POINT('Ctrl Pts',(-4.37682453544783,-0.0027517608039412,
11.848589891905));
#54476=CARTESIAN_POINT('Origin',(0.,0.,-1.84858989190501));
#54477=CARTESIAN_POINT('',(-4.37893064514985,-0.000718125850480163,9.65141010809499));
#54478=CARTESIAN_POINT('',(-4.37095165486262,0.00392878392899476,9.84858989190502));
#54479=CARTESIAN_POINT('',(-4.372,-4.40683631492666E-13,-1.84858989190501));
#54480=CARTESIAN_POINT('Ctrl Pts',(-4.37893064514985,-0.000718125850479884,
9.65141010809498));
#54481=CARTESIAN_POINT('Ctrl Pts',(-4.37902043646228,-0.0399142522790172,
9.65284329786977));
#54482=CARTESIAN_POINT('Ctrl Pts',(-4.36082969860212,-1.52204564057694,
9.70703992850478));
#54483=CARTESIAN_POINT('Ctrl Pts',(-2.69478237803987,-4.40306543037773,
9.81399999999999));
#54484=CARTESIAN_POINT('Ctrl Pts',(2.22377879965116,-4.65871710875468,9.97229032258064));
#54485=CARTESIAN_POINT('Ctrl Pts',(5.11810379036282,-0.67368452576514,10.1305806451613));
#54486=CARTESIAN_POINT('Ctrl Pts',(3.35357921258595,3.92458197953528,10.2888709677419));
#54487=CARTESIAN_POINT('Ctrl Pts',(-1.46360347987537,4.95042443663959,10.4471612903226));
#54488=CARTESIAN_POINT('Ctrl Pts',(-4.12415016732119,2.29334108429437,10.5680076704403));
#54489=CARTESIAN_POINT('Ctrl Pts',(-4.37307882051719,0.425051522096353,
10.6360906096977));
#54490=CARTESIAN_POINT('Ctrl Pts',(-4.36958950328423,0.00375500997191747,
10.651410108095));
#54491=CARTESIAN_POINT('Ctrl Pts',(-4.37095165486262,0.00392878392899445,
9.84858989190502));
#54492=CARTESIAN_POINT('Ctrl Pts',(-4.36138099894435,-1.0736503956833,9.88780471931308));
#54493=CARTESIAN_POINT('Ctrl Pts',(-3.41650604254828,-3.61702144425598,
9.97981608019584));
#54494=CARTESIAN_POINT('Ctrl Pts',(0.840841326532404,-5.09441123866306,
10.1246239745533));
#54495=CARTESIAN_POINT('Ctrl Pts',(4.73121909778617,-2.06775381846214,10.2830135749774));
#54496=CARTESIAN_POINT('Ctrl Pts',(4.30996593957687,2.84327867165857,10.4414031754015));
#54497=CARTESIAN_POINT('Ctrl Pts',(-0.0390238264566685,5.16318866070086,
10.5997927758256));
#54498=CARTESIAN_POINT('Ctrl Pts',(-3.7353314916358,3.11908229388608,10.7355216813268));
#54499=CARTESIAN_POINT('Ctrl Pts',(-4.36270060925329,0.829088583628261,
10.8184540533533));
#54500=CARTESIAN_POINT('Ctrl Pts',(-4.36549183168559,-0.00162636191587386,
10.848589891905));
#54501=CARTESIAN_POINT('Origin',(0.,0.,-1.84858989190501));
#54502=CARTESIAN_POINT('',(-4.3676089549007,-0.00316636266463396,8.65141010809498));
#54503=CARTESIAN_POINT('',(-4.3784939599728,-0.00146115515596901,8.84858989190502));
#54504=CARTESIAN_POINT('',(-4.372,-4.40683631492666E-13,-1.84858989190501));
#54505=CARTESIAN_POINT('Ctrl Pts',(-4.3676089549007,-0.0031663626646336,
8.65141010809498));
#54506=CARTESIAN_POINT('Ctrl Pts',(-4.37099157996906,-0.503863509155134,
8.66959598604181));
#54507=CARTESIAN_POINT('Ctrl Pts',(-4.0607005189635,-2.45318988687306,8.74054530484886));
#54508=CARTESIAN_POINT('Ctrl Pts',(-1.19412647058753,-5.02224045834365,
8.86425806451613));
#54509=CARTESIAN_POINT('Ctrl Pts',(3.56062739266322,-3.73774929868204,9.02254838709676));
#54510=CARTESIAN_POINT('Ctrl Pts',(5.07425366817473,0.949097971864315,9.18083870967742));
#54511=CARTESIAN_POINT('Ctrl Pts',(1.96894576792944,4.77201108675727,9.33912903225805));
#54512=CARTESIAN_POINT('Ctrl Pts',(-2.88428822201713,4.2558282973375,9.49598616506391));
#54513=CARTESIAN_POINT('Ctrl Pts',(-4.37571473425415,1.40310643844898,9.60007985700956));
#54514=CARTESIAN_POINT('Ctrl Pts',(-4.37893064514985,-0.000718125850479884,
9.65141010809498));
#54515=CARTESIAN_POINT('Ctrl Pts',(-4.3784939599728,-0.00146115515596968,
8.84858989190502));
#54516=CARTESIAN_POINT('Ctrl Pts',(-4.37884870232368,-0.0827753827151446,
8.85156231832348));
#54517=CARTESIAN_POINT('Ctrl Pts',(-4.34001073551865,-1.6080554399903,8.90733127821665));
#54518=CARTESIAN_POINT('Ctrl Pts',(-2.56365995117077,-4.48192901101572,
9.01589677158451));
#54519=CARTESIAN_POINT('Ctrl Pts',(2.36421564112952,-4.59026408905411,9.17428637200862));
#54520=CARTESIAN_POINT('Ctrl Pts',(5.13754605775107,-0.515422651333577,
9.33267597243274));
#54521=CARTESIAN_POINT('Ctrl Pts',(3.22895369161553,4.02913117959985,9.49106557285684));
#54522=CARTESIAN_POINT('Ctrl Pts',(-1.62223260619563,4.90187733184103,9.64945517328097));
#54523=CARTESIAN_POINT('Ctrl Pts',(-4.15999532952882,2.19738929405191,9.76862994629701));
#54524=CARTESIAN_POINT('Ctrl Pts',(-4.37426636626487,0.377138731501872,
9.83500818583837));
#54525=CARTESIAN_POINT('Ctrl Pts',(-4.37095165486262,0.00392878392899445,
9.84858989190502));
#54526=CARTESIAN_POINT('Origin',(0.,0.,-1.84858989190501));
#54527=CARTESIAN_POINT('',(-4.36783565389082,0.00326080189849165,7.65141010809498));
#54528=CARTESIAN_POINT('',(-4.36682740614764,-0.00278338701585445,7.84858989190503));
#54529=CARTESIAN_POINT('',(-4.372,-4.40683631492666E-13,-1.84858989190501));
#54530=CARTESIAN_POINT('Ctrl Pts',(-4.36783565389082,0.0032608018984915,
7.65141010809498));
#54531=CARTESIAN_POINT('Ctrl Pts',(-4.36111999858997,-0.958548857288375,
7.68634867421386));
#54532=CARTESIAN_POINT('Ctrl Pts',(-3.57508309710888,-3.38283964502905,
7.77405068119295));
#54533=CARTESIAN_POINT('Ctrl Pts',(0.424618501333285,-5.14475814567673,
7.91451612903225));
#54534=CARTESIAN_POINT('Ctrl Pts',(4.54535988400859,-2.44714952016159,8.0728064516129));
#54535=CARTESIAN_POINT('Ctrl Pts',(4.52860253637045,2.47802266268103,8.23109677419354));
#54536=CARTESIAN_POINT('Ctrl Pts',(0.389600147091602,5.14752843358518,8.38938709677419));
#54537=CARTESIAN_POINT('Ctrl Pts',(-3.58777114537366,3.36303202741965,8.52949154140801));
#54538=CARTESIAN_POINT('Ctrl Pts',(-4.36117742976588,0.948829858465871,
8.6168325451816));
#54539=CARTESIAN_POINT('Ctrl Pts',(-4.3676089549007,-0.0031663626646336,
8.65141010809498));
#54540=CARTESIAN_POINT('Ctrl Pts',(-4.36682740614764,-0.00278338701585466,
7.84858989190503));
#54541=CARTESIAN_POINT('Ctrl Pts',(-4.36998031573444,-0.540633837652302,
7.8681164508086));
#54542=CARTESIAN_POINT('Ctrl Pts',(-4.02906901036793,-2.52888541639766,
7.94043954318687));
#54543=CARTESIAN_POINT('Ctrl Pts',(-1.06391319462353,-5.05253685976928,
8.06555916903983));
#54544=CARTESIAN_POINT('Ctrl Pts',(3.65925338948522,-3.64278803069328,8.22394876946396));
#54545=CARTESIAN_POINT('Ctrl Pts',(5.04768747299395,1.08668817054443,8.38233836988805));
#54546=CARTESIAN_POINT('Ctrl Pts',(1.83608824986349,4.82584914224785,8.54072797031219));
#54547=CARTESIAN_POINT('Ctrl Pts',(-2.95709387717496,4.17950307750852,8.69614514431782));
#54548=CARTESIAN_POINT('Ctrl Pts',(-4.37254773342937,1.36153600902825,8.79876578484878));
#54549=CARTESIAN_POINT('Ctrl Pts',(-4.3784939599728,-0.00146115515596968,
8.84858989190502));
#54550=CARTESIAN_POINT('Origin',(0.,0.,-1.84858989190501));
#54551=CARTESIAN_POINT('',(-4.37899478532443,0.000538853135781114,6.65141010809498));
#54552=CARTESIAN_POINT('',(-4.36857373794226,0.00352936749739713,6.84858989190502));
#54553=CARTESIAN_POINT('',(-4.372,-4.40683631492666E-13,-1.84858989190501));
#54554=CARTESIAN_POINT('Ctrl Pts',(-4.37899478532443,0.00053885313578114,
6.65141010809498));
#54555=CARTESIAN_POINT('Ctrl Pts',(-4.37652423695377,-1.41310306479934,
6.7031013623859));
#54556=CARTESIAN_POINT('Ctrl Pts',(-2.86643925520047,-4.27424452468468,
6.80755605753705));
#54557=CARTESIAN_POINT('Ctrl Pts',(2.00137227482285,-4.75850252356265,6.96477419354837));
#54558=CARTESIAN_POINT('Ctrl Pts',(5.08059451261016,-0.914547236405604,
7.12306451612904));
#54559=CARTESIAN_POINT('Ctrl Pts',(3.53511070256229,3.76189175413264,7.28135483870967));
#54560=CARTESIAN_POINT('Ctrl Pts',(-1.22827365147281,5.01399851279189,7.43964516129032));
#54561=CARTESIAN_POINT('Ctrl Pts',(-4.06898604612617,2.43305468214084,7.56299691775209));
#54562=CARTESIAN_POINT('Ctrl Pts',(-4.37126183097366,0.493954571118568,
7.63358523335364));
#54563=CARTESIAN_POINT('Ctrl Pts',(-4.36783565389082,0.0032608018984915,
7.65141010809498));
#54564=CARTESIAN_POINT('Ctrl Pts',(-4.36857373794226,0.00352936749739713,
6.84858989190502));
#54565=CARTESIAN_POINT('Ctrl Pts',(-4.3609877808655,-0.989297031049394,
6.8846705832937));
#54566=CARTESIAN_POINT('Ctrl Pts',(-3.53400975081915,-3.4463519724339,6.97354780815709));
#54567=CARTESIAN_POINT('Ctrl Pts',(0.538586577094185,-5.13516937442138,
7.11522156649516));
#54568=CARTESIAN_POINT('Ctrl Pts',(4.60087948645563,-2.34349054961462,7.27361116691928));
#54569=CARTESIAN_POINT('Ctrl Pts',(4.47032190918109,2.58384636410851,7.43200076734339));
#54570=CARTESIAN_POINT('Ctrl Pts',(0.26589292373178,5.15648532996368,7.59039036776751));
#54571=CARTESIAN_POINT('Ctrl Pts',(-3.63264590427038,3.29210602756316,7.72925340928804));
#54572=CARTESIAN_POINT('Ctrl Pts',(-4.3614553781167,0.913623385120531,7.81531991733389));
#54573=CARTESIAN_POINT('Ctrl Pts',(-4.36682740614764,-0.00278338701585466,
7.84858989190503));
#54574=CARTESIAN_POINT('Origin',(0.,0.,-1.84858989190501));
#54575=CARTESIAN_POINT('',(-4.36931971855082,-0.00370222284602327,5.65141010809498));
#54576=CARTESIAN_POINT('',(-4.37909655387308,8.17972643269707E-5,5.84858989190502));
#54577=CARTESIAN_POINT('',(-4.372,-4.40683631492666E-13,-1.84858989190501));
#54578=CARTESIAN_POINT('Ctrl Pts',(-4.36931971855082,-0.00370222284602335,
5.65141010809498));
#54579=CARTESIAN_POINT('Ctrl Pts',(-4.37282475456675,-0.434994053437505,
5.66709060969773));
#54580=CARTESIAN_POINT('Ctrl Pts',(-4.11645084466375,-2.3134683703663,5.73553455216068));
#54581=CARTESIAN_POINT('Ctrl Pts',(-1.42988345294528,-4.96026920238937,
5.85674193548387));
#54582=CARTESIAN_POINT('Ctrl Pts',(3.38020716333018,-3.90167102433782,6.01503225806451));
#54583=CARTESIAN_POINT('Ctrl Pts',(5.11340107541181,0.708496077023162,6.17332258064516));
#54584=CARTESIAN_POINT('Ctrl Pts',(2.19202615312461,4.67374139134797,6.3316129032258));
#54585=CARTESIAN_POINT('Ctrl Pts',(-2.72468151658193,4.38462631046011,6.48990322580645));
#54586=CARTESIAN_POINT('Ctrl Pts',(-4.36552898201431,1.50209810391025,6.59650229409617));
#54587=CARTESIAN_POINT('Ctrl Pts',(-4.37904602975287,0.0298607935490157,
6.65033792152568));
#54588=CARTESIAN_POINT('Ctrl Pts',(-4.37899478532443,0.00053885313578114,
6.65141010809498));
#54589=CARTESIAN_POINT('Ctrl Pts',(-4.37909655387308,8.17972643267733E-5,
5.84858989190502));
#54590=CARTESIAN_POINT('Ctrl Pts',(-4.37869792746944,-1.43927515570558,
5.90122471577881));
#54591=CARTESIAN_POINT('Ctrl Pts',(-2.8187969284654,-4.3231521197151,6.0066560731273));
#54592=CARTESIAN_POINT('Ctrl Pts',(2.08906951604171,-4.72184588505036,6.16488396395049));
#54593=CARTESIAN_POINT('Ctrl Pts',(5.098151436811,-0.817858137064712,6.32327356437462));
#54594=CARTESIAN_POINT('Ctrl Pts',(3.46121148378334,3.83145599864432,6.48166316479871));
#54595=CARTESIAN_POINT('Ctrl Pts',(-1.32998241066,4.98910681308353,6.64005276522284));
#54596=CARTESIAN_POINT('Ctrl Pts',(-4.09382090065572,2.37211345116906,6.76236167425826));
#54597=CARTESIAN_POINT('Ctrl Pts',(-4.37208823990123,0.463496420738366,
6.831874049819));
#54598=CARTESIAN_POINT('Ctrl Pts',(-4.36857373794226,0.00352936749739713,
6.84858989190502));
#54599=CARTESIAN_POINT('Origin',(0.,0.,-1.84858989190501));
#54600=CARTESIAN_POINT('',(-4.36642690985212,0.00250163610255838,4.65141010809498));
#54601=CARTESIAN_POINT('',(-4.36880169481863,-0.00359316639133633,4.84858989190502));
#54602=CARTESIAN_POINT('',(-4.372,-4.40683631492666E-13,-1.84858989190501));
#54603=CARTESIAN_POINT('Ctrl Pts',(-4.36642690985212,0.00250163610255878,
4.65141010809498));
#54604=CARTESIAN_POINT('Ctrl Pts',(-4.36174213540044,-0.891062986338486,
4.68384329786977));
#54605=CARTESIAN_POINT('Ctrl Pts',(-3.66101665548786,-3.24505548151499,
4.76903992850477));
#54606=CARTESIAN_POINT('Ctrl Pts',(0.181272997936893,-5.15906748833169,
4.907));
#54607=CARTESIAN_POINT('Ctrl Pts',(4.4247679934035,-2.65899707670991,5.06529032258064));
#54608=CARTESIAN_POINT('Ctrl Pts',(4.64053527927078,2.26147508740778,5.22358064516129));
#54609=CARTESIAN_POINT('Ctrl Pts',(0.63216865368283,5.12339731452249,5.38187096774192));
#54610=CARTESIAN_POINT('Ctrl Pts',(-3.49756148837773,3.50013537491244,5.52448078871984));
#54611=CARTESIAN_POINT('Ctrl Pts',(-4.361030631826,1.01626315589314,5.61432716883751));
#54612=CARTESIAN_POINT('Ctrl Pts',(-4.36931971855082,-0.00370222284602335,
5.65141010809498));
#54613=CARTESIAN_POINT('Ctrl Pts',(-4.36880169481863,-0.00359316639133644,
4.84858989190502));
#54614=CARTESIAN_POINT('Ctrl Pts',(-4.37232350022417,-0.454601269873613,
4.86498231478922));
#54615=CARTESIAN_POINT('Ctrl Pts',(-4.10093982798236,-2.35407682434418,
4.93417127114812));
#54616=CARTESIAN_POINT('Ctrl Pts',(-1.36037264139205,-4.98090617072295,
5.05615676098171));
#54617=CARTESIAN_POINT('Ctrl Pts',(3.43778957362211,-3.85248528258675,5.21454636140584));
#54618=CARTESIAN_POINT('Ctrl Pts',(5.10304258525828,0.786763228710822,5.37293596182993));
#54619=CARTESIAN_POINT('Ctrl Pts',(2.11781634615703,4.70902260867037,5.53132556225406));
#54620=CARTESIAN_POINT('Ctrl Pts',(-2.79740769526454,4.33987905263503,5.68971516267816));
#54621=CARTESIAN_POINT('Ctrl Pts',(-4.37709282415761,1.45270398568835,5.79546993922849));
#54622=CARTESIAN_POINT('Ctrl Pts',(-4.37909777857019,0.00450392355468565,
5.84842818230411));
#54623=CARTESIAN_POINT('Ctrl Pts',(-4.37909655387308,8.17972643267733E-5,
5.84858989190502));
#54624=CARTESIAN_POINT('Origin',(0.,0.,-1.84858989190501));
#54625=CARTESIAN_POINT('',(-4.37822270954365,0.00173219555018226,3.65141010809498));
#54626=CARTESIAN_POINT('',(-4.36665723562798,0.00267775706545931,3.84858989190502));
#54627=CARTESIAN_POINT('',(-4.372,-4.40683631492666E-13,-1.84858989190501));
#54628=CARTESIAN_POINT('Ctrl Pts',(-4.37822270954365,0.00173219555018251,
3.65141010809498));
#54629=CARTESIAN_POINT('Ctrl Pts',(-4.37141484073147,-1.3440268941613,3.70059598604181));
#54630=CARTESIAN_POINT('Ctrl Pts',(-2.98789956101879,-4.1455315666631,3.80254530484886));
#54631=CARTESIAN_POINT('Ctrl Pts',(1.77450307237079,-4.84767739015689,3.95725806451612));
#54632=CARTESIAN_POINT('Ctrl Pts',(5.03175648528012,-1.15337068283656,4.11554838709677));
#54633=CARTESIAN_POINT('Ctrl Pts',(3.7087595738537,3.5908132325819,4.27383870967742));
#54634=CARTESIAN_POINT('Ctrl Pts',(-0.990205008382098,5.06639233464293,
4.43212903225806));
#54635=CARTESIAN_POINT('Ctrl Pts',(-4.00969822487022,2.57279053906618,4.55798616506392));
#54636=CARTESIAN_POINT('Ctrl Pts',(-4.36936348937275,0.562619011588028,
4.63107985700956));
#54637=CARTESIAN_POINT('Ctrl Pts',(-4.36642690985212,0.00250163610255878,
4.65141010809498));
#54638=CARTESIAN_POINT('Ctrl Pts',(-4.36665723562798,0.00267775706545938,
3.84858989190502));
#54639=CARTESIAN_POINT('Ctrl Pts',(-4.36155175532508,-0.904909371632279,
3.88153644727432));
#54640=CARTESIAN_POINT('Ctrl Pts',(-3.64359471136329,-3.27429676880991,
3.96727953611833));
#54641=CARTESIAN_POINT('Ctrl Pts',(0.234452652827207,-5.15801046495039,
4.10581915843705));
#54642=CARTESIAN_POINT('Ctrl Pts',(4.4544870133001,-2.61105064195526,4.26420875886115));
#54643=CARTESIAN_POINT('Ctrl Pts',(4.61508054334482,2.31539879571022,4.42259835928526));
#54644=CARTESIAN_POINT('Ctrl Pts',(0.56988195080356,5.13179058096912,4.58098795970938));
#54645=CARTESIAN_POINT('Ctrl Pts',(-3.52225462180705,3.46403365178023,4.72298513724929));
#54646=CARTESIAN_POINT('Ctrl Pts',(-4.36098050850789,0.998000618272236,
4.81218578131451));
#54647=CARTESIAN_POINT('Ctrl Pts',(-4.36880169481863,-0.00359316639133644,
4.84858989190502));
#54648=CARTESIAN_POINT('Origin',(0.,0.,-1.84858989190501));
#54649=CARTESIAN_POINT('',(-4.3712761175009,-0.0039298912494793,2.65141010809498));
#54650=CARTESIAN_POINT('',(-4.37836367713493,0.00160984593324705,2.84858989190502));
#54651=CARTESIAN_POINT('',(-4.372,-4.40683631492666E-13,-1.84858989190501));
#54652=CARTESIAN_POINT('Ctrl Pts',(-4.3712761175009,-0.00392989124947909,
2.65141010809498));
#54653=CARTESIAN_POINT('Ctrl Pts',(-4.37451696257115,-0.365899162664298,
2.66458523335364));
#54654=CARTESIAN_POINT('Ctrl Pts',(-4.16818790357475,-2.17383119834201,
2.73052379947252));
#54655=CARTESIAN_POINT('Ctrl Pts',(-1.66245191543707,-4.88723759858308,
2.84922580645161));
#54656=CARTESIAN_POINT('Ctrl Pts',(3.19224964022283,-4.05689272016998,3.00751612903226));
#54657=CARTESIAN_POINT('Ctrl Pts',(5.14114662208426,0.466314344506177,3.1658064516129));
#54658=CARTESIAN_POINT('Ctrl Pts',(2.41021871871718,4.56505016420442,3.32409677419355));
#54659=CARTESIAN_POINT('Ctrl Pts',(-2.5146557123555,4.50836375769575,3.48238709677419));
#54660=CARTESIAN_POINT('Ctrl Pts',(-4.33147098232467,1.64065849811777,3.591491541408));
#54661=CARTESIAN_POINT('Ctrl Pts',(-4.37871788376841,0.0996167512533684,
3.6478325451816));
#54662=CARTESIAN_POINT('Ctrl Pts',(-4.37822270954365,0.00173219555018251,
3.65141010809498));
#54663=CARTESIAN_POINT('Ctrl Pts',(-4.37836367713493,0.00160984593324717,
2.84858989190502));
#54664=CARTESIAN_POINT('Ctrl Pts',(-4.37193582834707,-1.35264708506912,
2.89809057975943));
#54665=CARTESIAN_POINT('Ctrl Pts',(-2.9725521843832,-4.16280399703585,3.00038780108855));
#54666=CARTESIAN_POINT('Ctrl Pts',(1.80663443860224,-4.83695274769126,3.15548155589238));
#54667=CARTESIAN_POINT('Ctrl Pts',(5.04096893490742,-1.11744005069485,3.31387115631648));
#54668=CARTESIAN_POINT('Ctrl Pts',(3.68139281034196,3.62041254264275,3.4722607567406));
#54669=CARTESIAN_POINT('Ctrl Pts',(-1.03309179131411,5.05892887272037,3.63065035716471));
#54670=CARTESIAN_POINT('Ctrl Pts',(-4.0212815682019,2.54692422938098,3.75609340221952));
#54671=CARTESIAN_POINT('Ctrl Pts',(-4.36973323768933,0.549490145536826,
3.82873991379962));
#54672=CARTESIAN_POINT('Ctrl Pts',(-4.36665723562798,0.00267775706545938,
3.84858989190502));
#54673=CARTESIAN_POINT('Origin',(0.,0.,-1.84858989190501));
#54674=CARTESIAN_POINT('',(-4.36544656918105,0.00153916655095219,1.65141010809498));
#54675=CARTESIAN_POINT('',(-4.37121340809612,-0.00394090090135357,1.84858989190502));
#54676=CARTESIAN_POINT('',(-4.372,-4.40683631492666E-13,-1.84858989190501));
#54677=CARTESIAN_POINT('Ctrl Pts',(-4.36544656918105,0.00153916655095176,
1.65141010809498));
#54678=CARTESIAN_POINT('Ctrl Pts',(-4.36281788561468,-0.823458774996837,
1.68133792152568));
#54679=CARTESIAN_POINT('Ctrl Pts',(-3.74207983653693,-3.10661615213039,
1.76402917581661));
#54680=CARTESIAN_POINT('Ctrl Pts',(-0.0624691826164238,-5.16187799225891,
1.89948387096774));
#54681=CARTESIAN_POINT('Ctrl Pts',(4.29430578210828,-2.8649130214088,2.05777419354839));
#54682=CARTESIAN_POINT('Ctrl Pts',(4.74212257914569,2.03988351823947,2.21606451612903));
#54683=CARTESIAN_POINT('Ctrl Pts',(0.873326467994359,5.08784270323556,2.37435483870968));
#54684=CARTESIAN_POINT('Ctrl Pts',(-3.40224500791429,3.63628377215307,2.51947003603166));
#54685=CARTESIAN_POINT('Ctrl Pts',(-4.36153810021927,1.08370711208091,2.61182179249343));
#54686=CARTESIAN_POINT('Ctrl Pts',(-4.3712761175009,-0.00392989124947909,
2.65141010809498));
#54687=CARTESIAN_POINT('Ctrl Pts',(-4.37121340809612,-0.00394090090135399,
1.84858989190502));
#54688=CARTESIAN_POINT('Ctrl Pts',(-4.37447604421791,-0.368207831146071,
1.86184817876984));
#54689=CARTESIAN_POINT('Ctrl Pts',(-4.16647286574876,-2.17936832407669,
1.92790299910937));
#54690=CARTESIAN_POINT('Ctrl Pts',(-1.65208468153467,-4.89189754332655,
2.04675435292359));
#54691=CARTESIAN_POINT('Ctrl Pts',(3.20433051897175,-4.04874042926377,2.20514395334771));
#54692=CARTESIAN_POINT('Ctrl Pts',(5.14059300557593,0.484092964878372,2.36353355377181));
#54693=CARTESIAN_POINT('Ctrl Pts',(2.392155064142,4.57576601695794,2.52192315419593));
#54694=CARTESIAN_POINT('Ctrl Pts',(-2.53628918908134,4.49747442552335,2.68031275462004));
#54695=CARTESIAN_POINT('Ctrl Pts',(-4.33547083524805,1.62595452236117,2.78920166718974));
#54696=CARTESIAN_POINT('Ctrl Pts',(-4.37879165497107,0.0917787298065273,
2.84529404628473));
#54697=CARTESIAN_POINT('Ctrl Pts',(-4.37836367713493,0.00160984593324717,
2.84858989190502));
#54698=CARTESIAN_POINT('Origin',(0.,0.,-1.84858989190501));
#54699=CARTESIAN_POINT('',(-4.37640441740291,0.00246357316762604,0.651410108094979));
#54700=CARTESIAN_POINT('',(-4.36535621882271,0.00145633068789036,0.848589891905021));
#54701=CARTESIAN_POINT('',(-4.372,-4.40683631492666E-13,-1.84858989190501));
#54702=CARTESIAN_POINT('Ctrl Pts',(-4.37640441740291,0.00246357316762608,
0.651410108094978));
#54703=CARTESIAN_POINT('Ctrl Pts',(-4.3669296163584,-1.27588513251927,0.698090609697727));
#54704=CARTESIAN_POINT('Ctrl Pts',(-3.10443214653608,-4.01442651751147,
0.79753455216069));
#54705=CARTESIAN_POINT('Ctrl Pts',(1.54404435335689,-4.92628156041988,0.949741935483869));
#54706=CARTESIAN_POINT('Ctrl Pts',(4.97150648183897,-1.38949747849925,1.10803225806451));
#54707=CARTESIAN_POINT('Ctrl Pts',(3.87423912778238,3.41166257284768,1.26632258064516));
#54708=CARTESIAN_POINT('Ctrl Pts',(-0.749980974679123,5.10752324154442,
1.42461290322581));
#54709=CARTESIAN_POINT('Ctrl Pts',(-3.94614385852298,2.71245661069425,1.55297541237574));
#54710=CARTESIAN_POINT('Ctrl Pts',(-4.36745231673392,0.631032051720065,
1.62857448066547));
#54711=CARTESIAN_POINT('Ctrl Pts',(-4.36544656918105,0.00153916655095176,
1.65141010809498));
#54712=CARTESIAN_POINT('Ctrl Pts',(-4.36535621882271,0.0014563306878905,
0.848589891905021));
#54713=CARTESIAN_POINT('Ctrl Pts',(-4.36284379533113,-0.820370961494963,
0.87840231125495));
#54714=CARTESIAN_POINT('Ctrl Pts',(-3.74556810328531,-3.1011139180804,0.961011264079584));
#54715=CARTESIAN_POINT('Ctrl Pts',(-0.0704529116473286,-5.16289724783097,
1.09641675037892));
#54716=CARTESIAN_POINT('Ctrl Pts',(4.29252819085395,-2.86947836000301,1.25480635080303));
#54717=CARTESIAN_POINT('Ctrl Pts',(4.74374945851672,2.03886099295457,1.41319595122714));
#54718=CARTESIAN_POINT('Ctrl Pts',(0.87187597225223,5.08919664880298,1.57158555165126));
#54719=CARTESIAN_POINT('Ctrl Pts',(-3.4039180408651,3.63453814591924,1.71671686521054));
#54720=CARTESIAN_POINT('Ctrl Pts',(-4.36148372635845,1.08235900094027,1.80905164529514));
#54721=CARTESIAN_POINT('Ctrl Pts',(-4.37121340809612,-0.00394090090135399,
1.84858989190502));
#54722=CARTESIAN_POINT('Origin',(0.,0.,19.5));
#54723=CARTESIAN_POINT('',(-4.87237116524908,0.00192128708900893,19.1338737912933));
#54724=CARTESIAN_POINT('Ctrl Pts',(-0.803308159453631,4.29756675351939,
19.628));
#54725=CARTESIAN_POINT('Ctrl Pts',(-0.673853669232168,4.32487002581643,
19.6249474412138));
#54726=CARTESIAN_POINT('Ctrl Pts',(-0.543485635434045,4.34604385579072,
19.621903094994));
#54727=CARTESIAN_POINT('Ctrl Pts',(-0.412569255997991,4.3612238307311,19.6188638308603));
#54728=CARTESIAN_POINT('Ctrl Pts',(-0.27984336996821,4.37661362101213,19.6157825584728));
#54729=CARTESIAN_POINT('Ctrl Pts',(-0.146553204834455,4.38584275860783,
19.6127065096298));
#54730=CARTESIAN_POINT('Ctrl Pts',(-0.0130667331008604,4.38900056457998,
19.6096324222416));
#54731=CARTESIAN_POINT('Ctrl Pts',(0.102479072721167,4.39173395943972,19.6069714941353));
#54732=CARTESIAN_POINT('Ctrl Pts',(0.218172435996331,4.38991749290017,19.6043120356729));
#54733=CARTESIAN_POINT('Ctrl Pts',(0.333776183320261,4.38357806344137,19.6016519311904));
#54734=CARTESIAN_POINT('Ctrl Pts',(0.379031782704649,4.38109635600062,19.6006105754768));
#54735=CARTESIAN_POINT('Ctrl Pts',(0.424273632554427,4.37792119522461,19.5995691207606));
#54736=CARTESIAN_POINT('Ctrl Pts',(0.469487373095433,4.37405300814147,19.5985274401165));
#54737=CARTESIAN_POINT('Ctrl Pts',(0.491900142232015,4.37213552060263,19.598011071696));
#54738=CARTESIAN_POINT('Ctrl Pts',(0.514298864495916,4.37004829843513,19.5974948121273));
#54739=CARTESIAN_POINT('Ctrl Pts',(0.536673783628106,4.36779258854753,19.5969788310225));
#54740=CARTESIAN_POINT('Ctrl Pts',(0.67587029099505,4.35375960205351,19.5937688633242));
#54741=CARTESIAN_POINT('Ctrl Pts',(0.814241659431173,4.33320254529649,19.5905674515573));
#54742=CARTESIAN_POINT('Ctrl Pts',(0.951373424482021,4.30622334317185,19.5873709472848));
#54743=CARTESIAN_POINT('Ctrl Pts',(1.08850518953287,4.2792441410472,19.5841744430122));
#54744=CARTESIAN_POINT('Ctrl Pts',(1.22439822554137,4.24584269855803,19.580982846234));
#54745=CARTESIAN_POINT('Ctrl Pts',(1.35863436321977,4.20606161338018,19.5777925085132));
#54746=CARTESIAN_POINT('Ctrl Pts',(1.44718365537814,4.1798198949077,19.57568799216));
#54747=CARTESIAN_POINT('Ctrl Pts',(1.53501187237287,4.15080088353343,19.573584023676));
#54748=CARTESIAN_POINT('Ctrl Pts',(1.62197697724057,4.11905814350536,19.5714795558027));
#54749=CARTESIAN_POINT('Ctrl Pts',(1.66029004733011,4.10507366288661,19.5705524181278));
#54750=CARTESIAN_POINT('Ctrl Pts',(1.69843554242665,4.09056039562537,19.5696251835263));
#54751=CARTESIAN_POINT('Ctrl Pts',(1.73640102301099,4.07552228846135,19.5686977624494));
#54752=CARTESIAN_POINT('Ctrl Pts',(1.75436952443725,4.06840497436797,19.5682588277464));
#54753=CARTESIAN_POINT('Ctrl Pts',(1.77228816141992,4.061173866115,19.5678200842298));
#54754=CARTESIAN_POINT('Ctrl Pts',(1.79015508413385,4.05383000141309,19.5673815385189));
#54755=CARTESIAN_POINT('Ctrl Pts',(1.91574464850677,4.00220875787305,19.5642989279495));
#54756=CARTESIAN_POINT('Ctrl Pts',(2.03879019285953,3.94501636210332,19.561225830935));
#54757=CARTESIAN_POINT('Ctrl Pts',(2.15887237555029,3.88249361470115,19.5581590360687));
#54758=CARTESIAN_POINT('Ctrl Pts',(2.27969637656572,3.81958462748645,19.5550732958053));
#54759=CARTESIAN_POINT('Ctrl Pts',(2.39752111769151,3.75127894449634,19.5519939357949));
#54760=CARTESIAN_POINT('Ctrl Pts',(2.51190593036526,3.67777150955579,19.5489176847461));
#54761=CARTESIAN_POINT('Ctrl Pts',(2.62522809247125,3.60494696874821,19.5458700124906));
#54762=CARTESIAN_POINT('Ctrl Pts',(2.73517470696147,3.52701649641376,19.5428253916997));
#54763=CARTESIAN_POINT('Ctrl Pts',(2.84129224832913,3.44412553804493,19.5397806414099));
#54764=CARTESIAN_POINT('Ctrl Pts',(2.91209516263097,3.38881968242346,19.5377491469835));
#54765=CARTESIAN_POINT('Ctrl Pts',(2.98119295340959,3.33130466078434,19.5357175949077));
#54766=CARTESIAN_POINT('Ctrl Pts',(3.04844206982076,3.27161381566964,19.5336850403595));
#54767=CARTESIAN_POINT('Ctrl Pts',(3.08425226424725,3.23982840519718,19.5326027038555));
#54768=CARTESIAN_POINT('Ctrl Pts',(3.1195381208217,3.20742589648737,19.5315200830935));
#54769=CARTESIAN_POINT('Ctrl Pts',(3.15427695670459,3.17441047942531,19.5304370354107));
#54770=CARTESIAN_POINT('Ctrl Pts',(3.16725486117647,3.16207641819842,19.5300324251523));
#54771=CARTESIAN_POINT('Ctrl Pts',(3.18015812731145,3.14965513440157,19.5296277011351));
#54772=CARTESIAN_POINT('Ctrl Pts',(3.19297991753168,3.13715232569191,19.5292230337074));
#54773=CARTESIAN_POINT('Ctrl Pts',(3.21028959746143,3.12027327734767,19.5286767243753));
#54774=CARTESIAN_POINT('Ctrl Pts',(3.22744427955767,3.10325207454711,19.5281307247594));
#54775=CARTESIAN_POINT('Ctrl Pts',(3.24444163127926,3.08608990264034,19.5275850170264));
#54776=CARTESIAN_POINT('Ctrl Pts',(3.33717764080849,2.99245464912803,19.5246076851246));
#54777=CARTESIAN_POINT('Ctrl Pts',(3.42523294755332,2.89462674101026,19.5216390416869));
#54778=CARTESIAN_POINT('Ctrl Pts',(3.50859096128539,2.79305369138356,19.5186761904996));
#54779=CARTESIAN_POINT('Ctrl Pts',(3.59397640033088,2.68901019215335,19.5156412771407));
#54780=CARTESIAN_POINT('Ctrl Pts',(3.67443362705331,2.58103662340854,19.5126124412155));
#54781=CARTESIAN_POINT('Ctrl Pts',(3.74990902226373,2.46957232453757,19.5095865700048));
#54782=CARTESIAN_POINT('Ctrl Pts',(3.82667993619766,2.35619476524857,19.5065087603736));
#54783=CARTESIAN_POINT('Ctrl Pts',(3.89829689144343,2.23920494837555,19.5034340181076));
#54784=CARTESIAN_POINT('Ctrl Pts',(3.96466142958627,2.11903192999767,19.5003590674328));
#54785=CARTESIAN_POINT('Ctrl Pts',(4.0309620923612,1.99897457724446,19.4972870763748));
#54786=CARTESIAN_POINT('Ctrl Pts',(4.09202070623594,1.87573937136613,19.4942148773091));
#54787=CARTESIAN_POINT('Ctrl Pts',(4.14769296331372,1.74973219296001,19.4911392039111));
#54788=CARTESIAN_POINT('Ctrl Pts',(4.15491534612853,1.73338523439156,19.4907401956463));
#54789=CARTESIAN_POINT('Ctrl Pts',(4.16204794028702,1.71698942368025,19.490341076027));
#54790=CARTESIAN_POINT('Ctrl Pts',(4.1690873140012,1.70055278577387,19.4899420115644));
#54791=CARTESIAN_POINT('Ctrl Pts',(4.2235955422653,1.57327839358026,19.4868519217777));
#54792=CARTESIAN_POINT('Ctrl Pts',(4.27240340036226,1.44383040880503,19.4837717143479));
#54793=CARTESIAN_POINT('Ctrl Pts',(4.31545919855678,1.31266698606642,19.4806981622917));
#54794=CARTESIAN_POINT('Ctrl Pts',(4.35892069590576,1.18026765801579,19.4775956492703));
#54795=CARTESIAN_POINT('Ctrl Pts',(4.39652153701043,1.04611964222381,19.4744999176358));
#54796=CARTESIAN_POINT('Ctrl Pts',(4.42816288898243,0.910666566444117,19.4714076483225));
#54797=CARTESIAN_POINT('Ctrl Pts',(4.45971763719553,0.775584231634271,19.4683238426851));
#54798=CARTESIAN_POINT('Ctrl Pts',(4.48534571134421,0.639203155572113,19.4652434804418));
#54799=CARTESIAN_POINT('Ctrl Pts',(4.50489988856683,0.501947997482608,19.4621632697058));
#54800=CARTESIAN_POINT('Ctrl Pts',(4.5234656283834,0.371630903362032,19.4592387594872));
#54801=CARTESIAN_POINT('Ctrl Pts',(4.53655584516878,0.240525160569636,19.456314385846));
#54802=CARTESIAN_POINT('Ctrl Pts',(4.5440002395032,0.108991400598333,19.453387331288));
#54803=CARTESIAN_POINT('Ctrl Pts',(4.54553145652646,0.0819365827912304,
19.4527852734757));
#54804=CARTESIAN_POINT('Ctrl Pts',(4.54682366211308,0.0548636663001908,
19.4521831022411));
#54805=CARTESIAN_POINT('Ctrl Pts',(4.54787513450369,0.0277758132908992,
19.4515807930663));
#54806=CARTESIAN_POINT('Ctrl Pts',(4.54880630338109,0.00378719894119923,
19.4510473966946));
#54807=CARTESIAN_POINT('Ctrl Pts',(4.54954867988174,-0.0202170615304457,
19.450513804788));
#54808=CARTESIAN_POINT('Ctrl Pts',(4.5501006277934,-0.0442070954676754,
19.4499806150988));
#54809=CARTESIAN_POINT('Ctrl Pts',(4.55331420062987,-0.183882814458235,
19.4468762571225));
#54810=CARTESIAN_POINT('Ctrl Pts',(4.55008558494902,-0.323251293541528,
19.443781616557));
#54811=CARTESIAN_POINT('Ctrl Pts',(4.54031186270851,-0.461877411739,19.4406934171861));
#54812=CARTESIAN_POINT('Ctrl Pts',(4.53067866021077,-0.598510460562132,
19.4376496177859));
#54813=CARTESIAN_POINT('Ctrl Pts',(4.51468731171393,-0.734423134579881,
19.4346120756979));
#54814=CARTESIAN_POINT('Ctrl Pts',(4.49218947310497,-0.869204596926774,
19.4315776539935));
#54815=CARTESIAN_POINT('Ctrl Pts',(4.48129191999887,-0.934490341445224,
19.430107834059));
#54816=CARTESIAN_POINT('Ctrl Pts',(4.46886701290829,-0.999510687886201,
19.4286387462481));
#54817=CARTESIAN_POINT('Ctrl Pts',(4.45489347098868,-1.06421861098155,19.4271700340528));
#54818=CARTESIAN_POINT('Ctrl Pts',(4.42601008140308,-1.19797025124501,19.4241341977007));
#54819=CARTESIAN_POINT('Ctrl Pts',(4.39051333916906,-1.33038812058978,19.421099966171));
#54820=CARTESIAN_POINT('Ctrl Pts',(4.34872071354063,-1.46115895479143,19.4180641910325));
#54821=CARTESIAN_POINT('Ctrl Pts',(4.32227027711835,-1.54392345173146,19.416142857398));
#54822=CARTESIAN_POINT('Ctrl Pts',(4.29329690956391,-1.62602796166861,19.4142209054574));
#54823=CARTESIAN_POINT('Ctrl Pts',(4.26187123440312,-1.70738903830258,19.4122975370436));
#54824=CARTESIAN_POINT('Ctrl Pts',(4.25321767430855,-1.72979310639049,19.4117679069221));
#54825=CARTESIAN_POINT('Ctrl Pts',(4.24437655206198,-1.75214443843245,19.4112380817814));
#54826=CARTESIAN_POINT('Ctrl Pts',(4.23535981723739,-1.7744158038722,19.4107086515302));
#54827=CARTESIAN_POINT('Ctrl Pts',(4.18439432237877,-1.90030074813356,19.4077161409069));
#54828=CARTESIAN_POINT('Ctrl Pts',(4.12776551664013,-2.02378469411099,19.4047326389142));
#54829=CARTESIAN_POINT('Ctrl Pts',(4.06584469055636,-2.14458841387499,19.4017552111055));
#54830=CARTESIAN_POINT('Ctrl Pts',(4.00036068062891,-2.2723436859638,19.3986064496223));
#54831=CARTESIAN_POINT('Ctrl Pts',(3.92895803265593,-2.39710220266129,19.3954644815049));
#54832=CARTESIAN_POINT('Ctrl Pts',(3.85201703329039,-2.51851897272141,19.392325836016));
#54833=CARTESIAN_POINT('Ctrl Pts',(3.77655716323104,-2.63759844617919,19.3892476100675));
#54834=CARTESIAN_POINT('Ctrl Pts',(3.69576939240684,-2.75346420580146,19.3861725800561));
#54835=CARTESIAN_POINT('Ctrl Pts',(3.60996439826952,-2.86576656284731,19.3830974718481));
#54836=CARTESIAN_POINT('Ctrl Pts',(3.54413699183306,-2.95192207133902,19.3807383271401));
#54837=CARTESIAN_POINT('Ctrl Pts',(3.47535563877055,-3.03597991726489,19.3783791364089));
#54838=CARTESIAN_POINT('Ctrl Pts',(3.40374469167589,-3.11776882943693,19.3760184212987));
#54839=CARTESIAN_POINT('Ctrl Pts',(3.38306291872267,-3.14139007423622,19.3753366292557));
#54840=CARTESIAN_POINT('Ctrl Pts',(3.36214505086869,-3.16482198260282,19.3746547100648));
#54841=CARTESIAN_POINT('Ctrl Pts',(3.34099389843024,-3.18806021076517,19.3739726281131));
#54842=CARTESIAN_POINT('Ctrl Pts',(3.32373515295353,-3.20702195132993,19.3734160684253));
#54843=CARTESIAN_POINT('Ctrl Pts',(3.30632108269655,-3.22585473586077,19.3728594003699));
#54844=CARTESIAN_POINT('Ctrl Pts',(3.28875317708965,-3.24455615157313,19.372302604599));
#54845=CARTESIAN_POINT('Ctrl Pts',(3.27637002727884,-3.25773828253526,19.3719101340564));
#54846=CARTESIAN_POINT('Ctrl Pts',(3.26391669904378,-3.27084847479794,19.3715177984306));
#54847=CARTESIAN_POINT('Ctrl Pts',(3.25139510554647,-3.28388487669204,19.3711256274074));
#54848=CARTESIAN_POINT('Ctrl Pts',(3.15282448543269,-3.38650809465787,19.3680384371903));
#54849=CARTESIAN_POINT('Ctrl Pts',(3.05000398947139,-3.48458548857025,19.3649607083322));
#54850=CARTESIAN_POINT('Ctrl Pts',(2.94328170324704,-3.57779502158214,19.3618892172301));
#54851=CARTESIAN_POINT('Ctrl Pts',(2.83673480189425,-3.67085137626031,19.3588227737435));
#54852=CARTESIAN_POINT('Ctrl Pts',(2.72629835158367,-3.75905650319765,19.3557625475278));
#54853=CARTESIAN_POINT('Ctrl Pts',(2.61227793614804,-3.84205888933313,19.3527053308466));
#54854=CARTESIAN_POINT('Ctrl Pts',(2.49975879118773,-3.92396840950061,19.3496883675631));
#54855=CARTESIAN_POINT('Ctrl Pts',(2.38374884571102,-4.0008118415243,19.3466743350847));
#54856=CARTESIAN_POINT('Ctrl Pts',(2.26451075890163,-4.07221233820177,19.3436601507197));
#54857=CARTESIAN_POINT('Ctrl Pts',(2.15307182587664,-4.13894265382576,19.3408431188587));
#54858=CARTESIAN_POINT('Ctrl Pts',(2.03881261846325,-4.20091883876065,19.3380259543306));
#54859=CARTESIAN_POINT('Ctrl Pts',(1.92192917555825,-4.2577952663979,19.3352061406412));
#54860=CARTESIAN_POINT('Ctrl Pts',(1.89885610409831,-4.26902280938128,19.334649502668));
#54861=CARTESIAN_POINT('Ctrl Pts',(1.87568072700257,-4.28005149894805,19.3340927614631));
#54862=CARTESIAN_POINT('Ctrl Pts',(1.85240449004643,-4.29087848232892,19.3335358976687));
#54863=CARTESIAN_POINT('Ctrl Pts',(1.83464431921192,-4.29913965765674,19.3331110009753));
#54864=CARTESIAN_POINT('Ctrl Pts',(1.81682357432143,-4.30728417370212,19.3326859893584));
#54865=CARTESIAN_POINT('Ctrl Pts',(1.79895912167073,-4.315303623104,19.3322612385723));
#54866=CARTESIAN_POINT('Ctrl Pts',(1.72163150021165,-4.35001641054753,19.3304226729781));
#54867=CARTESIAN_POINT('Ctrl Pts',(1.64342321773675,-4.38241577414544,19.3285875039126));
#54868=CARTESIAN_POINT('Ctrl Pts',(1.56440032675076,-4.41242911636972,19.3267550510791));
#54869=CARTESIAN_POINT('Ctrl Pts',(1.43711047143297,-4.46077452542352,19.3238033410982));
#54870=CARTESIAN_POINT('Ctrl Pts',(1.30770822291801,-4.50293181836922,19.3208586788369));
#54871=CARTESIAN_POINT('Ctrl Pts',(1.17662145504096,-4.53906398417229,19.3179182210069));
#54872=CARTESIAN_POINT('Ctrl Pts',(1.04250946942332,-4.57603000735673,19.3149099033514));
#54873=CARTESIAN_POINT('Ctrl Pts',(0.906633655370345,-4.60668969161992,
19.3119059864259));
#54874=CARTESIAN_POINT('Ctrl Pts',(0.769431097467203,-4.63116704578967,
19.308903425512));
#54875=CARTESIAN_POINT('Ctrl Pts',(0.630182204159468,-4.65600947242755,
19.3058560822937));
#54876=CARTESIAN_POINT('Ctrl Pts',(0.489565915681568,-4.67448381748104,
19.3028101358377));
#54877=CARTESIAN_POINT('Ctrl Pts',(0.348028745832047,-4.68666735853543,
19.2997624031501));
#54878=CARTESIAN_POINT('Ctrl Pts',(0.276401735269172,-4.69283302247179,
19.2982200522494));
#54879=CARTESIAN_POINT('Ctrl Pts',(0.204538794597775,-4.69738677129886,
19.2966772438915));
#54880=CARTESIAN_POINT('Ctrl Pts',(0.132497794988,-4.70033357743951,19.2951335655473));
#54881=CARTESIAN_POINT('Ctrl Pts',(0.112510249077041,-4.70115115941847,
19.2947052769069));
#54882=CARTESIAN_POINT('Ctrl Pts',(0.092508998863809,-4.70184502431764,
19.2942769212978));
#54883=CARTESIAN_POINT('Ctrl Pts',(0.0724952864131179,-4.70241523264229,
19.2938484899096));
#54884=CARTESIAN_POINT('Ctrl Pts',(0.0524053747538238,-4.70298761194961,
19.2934184273332));
#54885=CARTESIAN_POINT('Ctrl Pts',(0.0323102430098365,-4.70343515128597,
19.2929884454936));
#54886=CARTESIAN_POINT('Ctrl Pts',(0.0122186816347883,-4.70375813703399,
19.2925586960882));
#54887=CARTESIAN_POINT('Ctrl Pts',(-0.130279647047385,-4.70604889624492,
19.2895107213251));
#54888=CARTESIAN_POINT('Ctrl Pts',(-0.272714799094277,-4.70208198168319,
19.2864719199788));
#54889=CARTESIAN_POINT('Ctrl Pts',(-0.414633190928799,-4.69200784465072,
19.2834391901245));
#54890=CARTESIAN_POINT('Ctrl Pts',(-0.558078433367512,-4.68182532348272,
19.2803738321848));
#54891=CARTESIAN_POINT('Ctrl Pts',(-0.70099656213896,-4.66540343587715,
19.277314677082));
#54892=CARTESIAN_POINT('Ctrl Pts',(-0.842927293052888,-4.64284438111864,
19.2742585216926));
#54893=CARTESIAN_POINT('Ctrl Pts',(-0.984668741071393,-4.62031541176288,
19.2712064420796));
#54894=CARTESIAN_POINT('Ctrl Pts',(-1.12542627120009,-4.59166551790643,
19.2681573541844));
#54895=CARTESIAN_POINT('Ctrl Pts',(-1.26473685825812,-4.5569449834536,19.2651080676816));
#54896=CARTESIAN_POINT('Ctrl Pts',(-1.40219852797764,-4.52268525675062,
19.2620992510297));
#54897=CARTESIAN_POINT('Ctrl Pts',(-1.53825218997399,-4.48251476703442,
19.259090241007));
#54898=CARTESIAN_POINT('Ctrl Pts',(-1.6724364842164,-4.43643407027143,19.2560779726351));
#54899=CARTESIAN_POINT('Ctrl Pts',(-1.69577574030498,-4.42841905488856,
19.2555540357366));
#54900=CARTESIAN_POINT('Ctrl Pts',(-1.71905838453956,-4.42022512285657,
19.2550300002629));
#54901=CARTESIAN_POINT('Ctrl Pts',(-1.74228191014027,-4.41185213332152,
19.2545058500857));
#54902=CARTESIAN_POINT('Ctrl Pts',(-1.76035515482698,-4.40533602154642,
19.2540979406852));
#54903=CARTESIAN_POINT('Ctrl Pts',(-1.77838477372036,-4.39871426481839,
19.2536901381687));
#54904=CARTESIAN_POINT('Ctrl Pts',(-1.79636551936284,-4.3919886694264,19.2532825296376));
#54905=CARTESIAN_POINT('Ctrl Pts',(-1.93187451941972,-4.34130230054732,
19.2502106534458));
#54906=CARTESIAN_POINT('Ctrl Pts',(-2.06468449537211,-4.28469503542289,
19.2471480732848));
#54907=CARTESIAN_POINT('Ctrl Pts',(-2.19433977491624,-4.22226508755719,
19.2440916139197));
#54908=CARTESIAN_POINT('Ctrl Pts',(-2.32196725551768,-4.1608115394395,19.2410829573521));
#54909=CARTESIAN_POINT('Ctrl Pts',(-2.44653872111971,-4.09371577322205,
19.23808023162));
#54910=CARTESIAN_POINT('Ctrl Pts',(-2.56760656005401,-4.02102358517923,
19.235080408152));
#54911=CARTESIAN_POINT('Ctrl Pts',(-2.68526160349352,-3.95038052574101,
19.2321651470591));
#54912=CARTESIAN_POINT('Ctrl Pts',(-2.79960837675168,-3.87445182317372,
19.229252626912));
#54913=CARTESIAN_POINT('Ctrl Pts',(-2.91021369160128,-3.79323796763903,
19.2263400681055));
#54914=CARTESIAN_POINT('Ctrl Pts',(-2.98399388261748,-3.73906359290253,
19.2243972216394));
#54915=CARTESIAN_POINT('Ctrl Pts',(-3.05610871619606,-3.68253657740801,
19.2224543579711));
#54916=CARTESIAN_POINT('Ctrl Pts',(-3.12651483591522,-3.62376762555295,
19.2205106520618));
#54917=CARTESIAN_POINT('Ctrl Pts',(-3.16741234664924,-3.58962991353437,
19.2193815920652));
#54918=CARTESIAN_POINT('Ctrl Pts',(-3.20773318569702,-3.55473559432281,
19.2182522478782));
#54919=CARTESIAN_POINT('Ctrl Pts',(-3.24746784403176,-3.51910539807467,
19.217122457792));
#54920=CARTESIAN_POINT('Ctrl Pts',(-3.26700401396051,-3.50158725150764,
19.2165669787208));
#54921=CARTESIAN_POINT('Ctrl Pts',(-3.28639847163628,-3.48389120743249,
19.21601139186));
#54922=CARTESIAN_POINT('Ctrl Pts',(-3.30565001708697,-3.46601967389373,
19.2154556779901));
#54923=CARTESIAN_POINT('Ctrl Pts',(-3.31923733798883,-3.45340633530117,
19.2150634672609));
#54924=CARTESIAN_POINT('Ctrl Pts',(-3.33275239972697,-3.44070650564925,
19.2146712232022));
#54925=CARTESIAN_POINT('Ctrl Pts',(-3.34618584616149,-3.42792978435657,
19.2142792032619));
#54926=CARTESIAN_POINT('Ctrl Pts',(-3.44713342315095,-3.33191726347047,
19.2113333126973));
#54927=CARTESIAN_POINT('Ctrl Pts',(-3.54361479719668,-3.23143681477532,
19.2083960349772));
#54928=CARTESIAN_POINT('Ctrl Pts',(-3.63553433126932,-3.126940879262,19.2054645714511));
#54929=CARTESIAN_POINT('Ctrl Pts',(-3.73049026986206,-3.01899309932707,
19.2024362720435));
#54930=CARTESIAN_POINT('Ctrl Pts',(-3.82057851236323,-2.90675969406161,
19.1994141772984));
#54931=CARTESIAN_POINT('Ctrl Pts',(-3.90566064499467,-2.79069444962541,
19.1963952019566));
#54932=CARTESIAN_POINT('Ctrl Pts',(-3.99147592842286,-2.67362907362455,
19.1933502121733));
#54933=CARTESIAN_POINT('Ctrl Pts',(-4.07219888206677,-2.55266483623709,
19.1903083957846));
#54934=CARTESIAN_POINT('Ctrl Pts',(-4.14764752468129,-2.42823151976782,
19.1872665870857));
#54935=CARTESIAN_POINT('Ctrl Pts',(-4.20306739838779,-2.33683055555379,
19.1850322638681));
#54936=CARTESIAN_POINT('Ctrl Pts',(-4.25564073821494,-2.24355706942676,
19.1827979447995));
#54937=CARTESIAN_POINT('Ctrl Pts',(-4.30527982057198,-2.14857260904585,
19.1805623752584));
#54938=CARTESIAN_POINT('Ctrl Pts',(-4.32699691910319,-2.10701690762921,
19.1795843135842));
#54939=CARTESIAN_POINT('Ctrl Pts',(-4.3481522027174,-2.06513363702578,19.1786060125617));
#54940=CARTESIAN_POINT('Ctrl Pts',(-4.36873745807105,-2.02293601505909,
19.1776273671286));
#54941=CARTESIAN_POINT('Ctrl Pts',(-4.38086243818899,-1.99808107308335,
19.1770509323837));
#54942=CARTESIAN_POINT('Ctrl Pts',(-4.39278964467502,-1.97311706816874,
19.1764743781503));
#54943=CARTESIAN_POINT('Ctrl Pts',(-4.40451730909724,-1.9480466787424,19.175897682959));
#54944=CARTESIAN_POINT('Ctrl Pts',(-4.4127985002692,-1.93034386255322,19.1754904643556));
#54945=CARTESIAN_POINT('Ctrl Pts',(-4.42097601800018,-1.91259691029446,
19.1750833804788));
#54946=CARTESIAN_POINT('Ctrl Pts',(-4.42904852534276,-1.89480918199437,
19.1746764755087));
#54947=CARTESIAN_POINT('Ctrl Pts',(-4.48950921559979,-1.76158436280397,
19.1716288777402));
#54948=CARTESIAN_POINT('Ctrl Pts',(-4.54410184606152,-1.62603381239176,
19.1685903704127));
#54949=CARTESIAN_POINT('Ctrl Pts',(-4.59268280744846,-1.48860776987399,
19.1655578531078));
#54950=CARTESIAN_POINT('Ctrl Pts',(-4.64144650306992,-1.35066480793007,
19.1625139291796));
#54951=CARTESIAN_POINT('Ctrl Pts',(-4.68415360775462,-1.21083146528599,
19.1594760404209));
#54952=CARTESIAN_POINT('Ctrl Pts',(-4.72061445405524,-1.06953622768658,
19.1564410512956));
#54953=CARTESIAN_POINT('Ctrl Pts',(-4.75671346962216,-0.929643178041525,
19.1534361808442));
#54954=CARTESIAN_POINT('Ctrl Pts',(-4.78668986944038,-0.78831633896503,
19.1504341527609));
#54955=CARTESIAN_POINT('Ctrl Pts',(-4.81031125214298,-0.645956691618861,
19.1474319239356));
#54956=CARTESIAN_POINT('Ctrl Pts',(-4.82807965738957,-0.538871347096197,
19.1451735964244));
#54957=CARTESIAN_POINT('Ctrl Pts',(-4.84225125518576,-0.431201234879474,
19.1429151553273));
#54958=CARTESIAN_POINT('Ctrl Pts',(-4.85270728658022,-0.32311529964396,
19.1406553054137));
#54959=CARTESIAN_POINT('Ctrl Pts',(-4.85885127437678,-0.259603758599947,
19.1393274124716));
#54960=CARTESIAN_POINT('Ctrl Pts',(-4.86371203457958,-0.195948633814534,
19.1379990330984));
#54961=CARTESIAN_POINT('Ctrl Pts',(-4.86726251019289,-0.132184380886881,
19.136669904511));
#54962=CARTESIAN_POINT('Ctrl Pts',(-4.86838059639054,-0.112104273637358,
19.1362513464105));
#54963=CARTESIAN_POINT('Ctrl Pts',(-4.86936819801155,-0.0920224658990377,
19.1358329041084));
#54964=CARTESIAN_POINT('Ctrl Pts',(-4.87022464687506,-0.0719445408679467,
19.1354146627671));
#54965=CARTESIAN_POINT('Ctrl Pts',(-4.87127693233824,-0.0472755739962392,
19.1349007858712));
#54966=CARTESIAN_POINT('Ctrl Pts',(-4.87213135174695,-0.0226102934020704,
19.134387167001));
#54967=CARTESIAN_POINT('Ctrl Pts',(-4.8727870952798,0.00204924970852941,
19.1338737912933));
#54968=CARTESIAN_POINT('',(0.446113671359645,4.91412736825422,19.058));
#54969=CARTESIAN_POINT('Ctrl Pts',(0.44649414690178,4.91265885279919,19.058));
#54970=CARTESIAN_POINT('Ctrl Pts',(0.299727560449543,4.91447193481392,19.0691244126311));
#54971=CARTESIAN_POINT('Ctrl Pts',(0.153167317909177,4.91005959431981,19.0802626720314));
#54972=CARTESIAN_POINT('Ctrl Pts',(0.00725046426545532,4.89944030839442,
19.0914270753353));
#54973=CARTESIAN_POINT('Ctrl Pts',(-0.137909608980915,4.88887609813179,
19.10253357579));
#54974=CARTESIAN_POINT('Ctrl Pts',(-0.282433758712205,4.87216902002991,
19.1136659496671));
#54975=CARTESIAN_POINT('Ctrl Pts',(-0.425882683147369,4.84928678485378,
19.1248363037588));
#54976=CARTESIAN_POINT('Ctrl Pts',(-0.565675808016648,4.82698770403557,
19.1357219810862));
#54977=CARTESIAN_POINT('Ctrl Pts',(-0.704448457143253,4.79882393308609,
19.1466437274425));
#54978=CARTESIAN_POINT('Ctrl Pts',(-0.841774914873059,4.76472078486696,
19.1576127473831));
#54979=CARTESIAN_POINT('Ctrl Pts',(-0.940805834192305,4.74012781002693,
19.1655228919155));
#54980=CARTESIAN_POINT('Ctrl Pts',(-1.0390843184423,4.71244522520194,19.1734576204009));
#54981=CARTESIAN_POINT('Ctrl Pts',(-1.13644149966956,4.68163105513636,19.181421134727));
#54982=CARTESIAN_POINT('Ctrl Pts',(-1.16730557623662,4.6718623776514,19.1839457201022));
#54983=CARTESIAN_POINT('Ctrl Pts',(-1.198076992637,4.66177888532038,19.1864731984846));
#54984=CARTESIAN_POINT('Ctrl Pts',(-1.22875016771071,4.65137899873876,19.1890037037495));
#54985=CARTESIAN_POINT('Ctrl Pts',(-1.24841289336978,4.644712257645,19.190625858309));
#54986=CARTESIAN_POINT('Ctrl Pts',(-1.26802854233492,4.6379177328912,19.1922487049096));
#54987=CARTESIAN_POINT('Ctrl Pts',(-1.28758810772402,4.63099805128267,19.1938716419773));
#54988=CARTESIAN_POINT('Ctrl Pts',(-1.41973360557623,4.58424830235176,19.204836293928));
#54989=CARTESIAN_POINT('Ctrl Pts',(-1.54943066798541,4.53175252800649,19.2158141351685));
#54990=CARTESIAN_POINT('Ctrl Pts',(-1.67628513679076,4.47348474855613,19.2268170475339));
#54991=CARTESIAN_POINT('Ctrl Pts',(-1.77854477370016,4.42651405823497,19.2356866903145));
#54992=CARTESIAN_POINT('Ctrl Pts',(-1.87895707987582,4.37579165399884,19.2445726249588));
#54993=CARTESIAN_POINT('Ctrl Pts',(-1.97730366067652,4.32128226154577,19.2534810756009));
#54994=CARTESIAN_POINT('Ctrl Pts',(-2.10058309475894,4.25295363233385,19.2646479991967));
#54995=CARTESIAN_POINT('Ctrl Pts',(-2.22061803115919,4.17867506623871,19.275850302475));
#54996=CARTESIAN_POINT('Ctrl Pts',(-2.3371003873209,4.09882401061829,19.2871002449437));
#54997=CARTESIAN_POINT('Ctrl Pts',(-2.45349352336119,4.01903411722977,19.2983415704744));
#54998=CARTESIAN_POINT('Ctrl Pts',(-2.56634003134295,3.93367951832198,19.3096304622446));
#54999=CARTESIAN_POINT('Ctrl Pts',(-2.67529062823455,3.84310647943015,19.3209791516131));
#55000=CARTESIAN_POINT('Ctrl Pts',(-2.71693531724479,3.80848632915125,19.3253170134781));
#55001=CARTESIAN_POINT('Ctrl Pts',(-2.75801032451888,3.77310349110297,19.3296636119694));
#55002=CARTESIAN_POINT('Ctrl Pts',(-2.79849428295858,3.73697648238141,19.3340196301562));
#55003=CARTESIAN_POINT('Ctrl Pts',(-2.81294818526249,3.72407813264686,19.335574850143));
#55004=CARTESIAN_POINT('Ctrl Pts',(-2.82732736116309,3.71108427106867,19.3371313434063));
#55005=CARTESIAN_POINT('Ctrl Pts',(-2.84161861583708,3.69800711896962,19.3386877998622));
#55006=CARTESIAN_POINT('Ctrl Pts',(-2.94391515755751,3.60440110145739,19.34982888694));
#55007=CARTESIAN_POINT('Ctrl Pts',(-3.04186033803071,3.50639786607989,19.3609841912936));
#55008=CARTESIAN_POINT('Ctrl Pts',(-3.13519298587128,3.40438402939327,19.3721662582028));
#55009=CARTESIAN_POINT('Ctrl Pts',(-3.22998005288867,3.30078049302696,19.3835225772406));
#55010=CARTESIAN_POINT('Ctrl Pts',(-3.32001032606879,3.19303967930977,19.3949064994243));
#55011=CARTESIAN_POINT('Ctrl Pts',(-3.4049668301135,3.08153340439932,19.4063311657064));
#55012=CARTESIAN_POINT('Ctrl Pts',(-3.48992333415822,2.97002712948888,19.4177558319884));
#55013=CARTESIAN_POINT('Ctrl Pts',(-3.56980658085615,2.85475460919877,19.4292212423689));
#55014=CARTESIAN_POINT('Ctrl Pts',(-3.64424819284547,2.73606613269444,19.4407405378004));
#55015=CARTESIAN_POINT('Ctrl Pts',(-3.69362849951562,2.65733498741996,19.4483817793834));
#55016=CARTESIAN_POINT('Ctrl Pts',(-3.74061319511361,2.57710031760525,19.4560467316635));
#55017=CARTESIAN_POINT('Ctrl Pts',(-3.78513614038734,2.49546231597417,19.463739230308));
#55018=CARTESIAN_POINT('Ctrl Pts',(-3.80567440292713,2.4578030214146,19.4672877501953));
#55019=CARTESIAN_POINT('Ctrl Pts',(-3.82568866999261,2.41984508871949,19.470842131787));
#55020=CARTESIAN_POINT('Ctrl Pts',(-3.84517166765662,2.38159830576804,19.4744027515965));
#55021=CARTESIAN_POINT('Ctrl Pts',(-3.85722034167954,2.35794573298872,19.4766047098446));
#55022=CARTESIAN_POINT('Ctrl Pts',(-3.86906582550741,2.33418269113951,19.4788090538567));
#55023=CARTESIAN_POINT('Ctrl Pts',(-3.88070630194933,2.310311496771,19.4810158726822));
#55024=CARTESIAN_POINT('Ctrl Pts',(-3.8885082527386,2.29431198982011,19.4824949781091));
#55025=CARTESIAN_POINT('Ctrl Pts',(-3.8962165975453,2.27826690602767,19.4839749160027));
#55026=CARTESIAN_POINT('Ctrl Pts',(-3.90382674774023,2.26218599112426,19.4854548878754));
#55027=CARTESIAN_POINT('Ctrl Pts',(-3.96414789534232,2.13472211503535,19.4971857472531));
#55028=CARTESIAN_POINT('Ctrl Pts',(-4.01838481417725,2.00484470453858,19.5089339279855));
#55029=CARTESIAN_POINT('Ctrl Pts',(-4.06640211675339,1.87293521419554,19.5207141703003));
#55030=CARTESIAN_POINT('Ctrl Pts',(-4.11224826252183,1.74699016109889,19.5319617555951));
#55031=CARTESIAN_POINT('Ctrl Pts',(-4.15242432683241,1.61919178653392,19.5432385686204));
#55032=CARTESIAN_POINT('Ctrl Pts',(-4.18676153681696,1.4898597689249,19.554557439162));
#55033=CARTESIAN_POINT('Ctrl Pts',(-4.2207524598163,1.36183205048544,19.5657621601394));
#55034=CARTESIAN_POINT('Ctrl Pts',(-4.24902179998014,1.23230080216518,19.5770080946197));
#55035=CARTESIAN_POINT('Ctrl Pts',(-4.27135507448881,1.1015746586975,19.588307688129));
#55036=CARTESIAN_POINT('Ctrl Pts',(-4.29323252438759,0.973516650317833,
19.5993766556815));
#55037=CARTESIAN_POINT('Ctrl Pts',(-4.30941374767392,0.844311453337346,
19.6104971142425));
#55038=CARTESIAN_POINT('Ctrl Pts',(-4.31964759244882,0.714256825545012,
19.621680762742));
#55039=CARTESIAN_POINT('Ctrl Pts',(-4.32157304106312,0.689787673591424,
19.6237849123534));
#55040=CARTESIAN_POINT('Ctrl Pts',(-4.32328781702124,0.665288489028016,
19.6258912988008));
#55041=CARTESIAN_POINT('Ctrl Pts',(-4.32479004603219,0.640761311051878,
19.628));
#55042=CARTESIAN_POINT('',(-3.60367707498796,3.37571982724537,19.058));
#55043=CARTESIAN_POINT('Origin',(0.,0.,19.058));
#55044=CARTESIAN_POINT('Ctrl Pts',(-4.8727870952798,0.00204924970852941,
19.1338737912933));
#55045=CARTESIAN_POINT('Ctrl Pts',(-4.87617886814195,0.129598459003725,
19.1312184028586));
#55046=CARTESIAN_POINT('Ctrl Pts',(-4.87425769241846,0.256993603559053,
19.1285695196845));
#55047=CARTESIAN_POINT('Ctrl Pts',(-4.86689403436298,0.383955746440246,
19.1259250851319));
#55048=CARTESIAN_POINT('Ctrl Pts',(-4.85865401760772,0.526027822131655,
19.1229659329201));
#55049=CARTESIAN_POINT('Ctrl Pts',(-4.84360044272571,0.667558209996482,
19.1200123512114));
#55050=CARTESIAN_POINT('Ctrl Pts',(-4.82205180462592,0.808202442374607,
19.117061458221));
#55051=CARTESIAN_POINT('Ctrl Pts',(-4.80012826355871,0.951293601552751,
19.1140592256271));
#55052=CARTESIAN_POINT('Ctrl Pts',(-4.77148144982624,1.09346818380839,19.1110597761218));
#55053=CARTESIAN_POINT('Ctrl Pts',(-4.73639180273002,1.23435901743,19.1080600748768));
#55054=CARTESIAN_POINT('Ctrl Pts',(-4.71189105823817,1.33273362650888,19.1059655849107));
#55055=CARTESIAN_POINT('Ctrl Pts',(-4.68424808585656,1.43048229055225,19.1038709722142));
#55056=CARTESIAN_POINT('Ctrl Pts',(-4.6535439006576,1.52747603119476,19.1017752037047));
#55057=CARTESIAN_POINT('Ctrl Pts',(-4.64011081963306,1.56991079272586,19.1008583049818));
#55058=CARTESIAN_POINT('Ctrl Pts',(-4.62609165763282,1.61220100164168,19.099941185029));
#55059=CARTESIAN_POINT('Ctrl Pts',(-4.61149254035212,1.65433555918283,19.0990237573359));
#55060=CARTESIAN_POINT('Ctrl Pts',(-4.60425406248102,1.6752265525563,19.098568881885));
#55061=CARTESIAN_POINT('Ctrl Pts',(-4.59687300609065,1.69607927843875,19.0981139307812));
#55062=CARTESIAN_POINT('Ctrl Pts',(-4.58935008303519,1.71689236429986,19.0976588934799));
#55063=CARTESIAN_POINT('Ctrl Pts',(-4.58288926961042,1.73476699408821,19.0972680997573));
#55064=CARTESIAN_POINT('Ctrl Pts',(-4.57632388063936,1.75261206193917,19.0968772491973));
#55065=CARTESIAN_POINT('Ctrl Pts',(-4.56965942251531,1.77041363655401,19.0964866227106));
#55066=CARTESIAN_POINT('Ctrl Pts',(-4.51879838731399,1.90626962008207,19.0935054849917));
#55067=CARTESIAN_POINT('Ctrl Pts',(-4.4621015938381,2.03978869153619,19.090533120728));
#55068=CARTESIAN_POINT('Ctrl Pts',(-4.39988991481362,2.17062521779186,19.0875666304161));
#55069=CARTESIAN_POINT('Ctrl Pts',(-4.33631291127845,2.304333139242,19.0845350362203));
#55070=CARTESIAN_POINT('Ctrl Pts',(-4.26697605411688,2.4352402172723,19.08150957663));
#55071=CARTESIAN_POINT('Ctrl Pts',(-4.19216902199247,2.5629660482269,19.0784871570202));
#55072=CARTESIAN_POINT('Ctrl Pts',(-4.11721282278043,2.69094656767373,19.0754587106304));
#55073=CARTESIAN_POINT('Ctrl Pts',(-4.03676418963347,2.81573387820879,19.0724333163567));
#55074=CARTESIAN_POINT('Ctrl Pts',(-3.95106744680097,2.93692273562437,19.0694078610249));
#55075=CARTESIAN_POINT('Ctrl Pts',(-3.86644065662709,3.05659850939287,19.0664201795206));
#55076=CARTESIAN_POINT('Ctrl Pts',(-3.77669549591118,3.17276577294219,19.0634324384734));
#55077=CARTESIAN_POINT('Ctrl Pts',(-3.68202832948565,3.28500209019142,19.0604416398662));
#55078=CARTESIAN_POINT('Ctrl Pts',(-3.65627454507218,3.31553548447098,19.0596280063176));
#55079=CARTESIAN_POINT('Ctrl Pts',(-3.63015628737134,3.34577773744076,19.0588141464826));
#55080=CARTESIAN_POINT('Ctrl Pts',(-3.60367707498796,3.37571982724537,19.058));
#55081=CARTESIAN_POINT('',(-4.,-4.89858719658941E-16,20.));
#55082=CARTESIAN_POINT('',(-4.5,-5.51091059616309E-16,19.5));
#55083=CARTESIAN_POINT('Origin',(0.,0.,20.));
#55084=CARTESIAN_POINT('Ctrl Pts',(2.86929757049748,-4.02374147429196,-0.329089653438089));
#55085=CARTESIAN_POINT('Ctrl Pts',(3.53627793941073,-3.54812315628632,-0.302707933007981));
#55086=CARTESIAN_POINT('Ctrl Pts',(4.61815699384527,-2.26074102389229,-0.249944492147766));
#55087=CARTESIAN_POINT('Ctrl Pts',(5.34305681190694,1.0543831002385,-0.144417610427336));
#55088=CARTESIAN_POINT('Ctrl Pts',(2.97075510791326,5.02204979956487,-0.0125090082767979));
#55089=CARTESIAN_POINT('Ctrl Pts',(-2.60167993603097,5.22655530852652,0.145781314303847));
#55090=CARTESIAN_POINT('Ctrl Pts',(-5.79544439621568,0.666623916928201,
0.304071636884492));
#55091=CARTESIAN_POINT('Ctrl Pts',(-3.71916882578288,-4.49661457488776,
0.462361959465137));
#55092=CARTESIAN_POINT('Ctrl Pts',(1.74534931250902,-5.56854608224957,0.620652282045782));
#55093=CARTESIAN_POINT('Ctrl Pts',(5.61966720797076,-1.57065337116734,0.778942604626428));
#55094=CARTESIAN_POINT('Ctrl Pts',(4.37934349714106,3.85645847095449,0.937232927207072));
#55095=CARTESIAN_POINT('Ctrl Pts',(-0.84775983002377,5.77341716827827,1.09552324978772));
#55096=CARTESIAN_POINT('Ctrl Pts',(-5.30296447800194,2.43487893547456,1.25381357236836));
#55097=CARTESIAN_POINT('Ctrl Pts',(-4.93115623773879,-3.11998211803485,
1.41210389494901));
#55098=CARTESIAN_POINT('Ctrl Pts',(-0.0706136094443395,-5.83485842583339,
1.57039421752965));
#55099=CARTESIAN_POINT('Ctrl Pts',(4.85417638956518,-3.23842638421833,1.7286845401103));
#55100=CARTESIAN_POINT('Ctrl Pts',(5.36037735273058,2.3058335652194,1.88697486269095));
#55101=CARTESIAN_POINT('Ctrl Pts',(0.98718650613642,5.75117077753662,2.04526518527159));
#55102=CARTESIAN_POINT('Ctrl Pts',(-4.28460500301765,3.96139458246299,2.20355550785224));
#55103=CARTESIAN_POINT('Ctrl Pts',(-5.65625702821141,-1.43431356080714,
2.36184583043288));
#55104=CARTESIAN_POINT('Ctrl Pts',(-1.87919427403712,-5.52441175942303,
2.52013615301353));
#55105=CARTESIAN_POINT('Ctrl Pts',(3.60843955214569,-4.58581057252521,2.67842647559417));
#55106=CARTESIAN_POINT('Ctrl Pts',(5.81142420090129,0.527110130500736,2.83671679817481));
#55107=CARTESIAN_POINT('Ctrl Pts',(2.72445125981257,5.16021910144056,2.99500712075546));
#55108=CARTESIAN_POINT('Ctrl Pts',(-2.84250423844022,5.09614219820049,3.15329744333611));
#55109=CARTESIAN_POINT('Ctrl Pts',(-5.82201720884499,0.393206705834578,
3.31158776591675));
#55110=CARTESIAN_POINT('Ctrl Pts',(-3.50193025017819,-4.66765255027645,
3.4698780884974));
#55111=CARTESIAN_POINT('Ctrl Pts',(2.00585411337058,-5.47969388429905,3.62816841107804));
#55112=CARTESIAN_POINT('Ctrl Pts',(5.68777231250098,-1.30374151751568,3.78645873365868));
#55113=CARTESIAN_POINT('Ctrl Pts',(4.19228952744401,4.05896591843996,3.94474905623933));
#55114=CARTESIAN_POINT('Ctrl Pts',(-1.11930309959379,5.72692381468561,4.10303937881998));
#55115=CARTESIAN_POINT('Ctrl Pts',(-5.41202917540188,2.18184234468851,4.26132970140061));
#55116=CARTESIAN_POINT('Ctrl Pts',(-4.77835461070898,-3.34930187121133,
4.41962002398127));
#55117=CARTESIAN_POINT('Ctrl Pts',(0.204906485773977,-5.83168150213524,
4.57791034656191));
#55118=CARTESIAN_POINT('Ctrl Pts',(5.00164762657821,-3.00566412467992,4.73620066914256));
#55119=CARTESIAN_POINT('Ctrl Pts',(5.24554559701654,2.55631516056015,4.8944909917232));
#55120=CARTESIAN_POINT('Ctrl Pts',(0.714587714204218,5.79136082533626,5.05278131430385));
#55121=CARTESIAN_POINT('Ctrl Pts',(-4.46683698218372,3.75471213080312,5.21107163688449));
#55122=CARTESIAN_POINT('Ctrl Pts',(-5.58223988624457,-1.69973340938259,
5.36936195946513));
#55123=CARTESIAN_POINT('Ctrl Pts',(-1.61630467165047,-5.60696486692776,
5.52765228204579));
#55124=CARTESIAN_POINT('Ctrl Pts',(3.82090205882377,-4.41035183034713,5.68594260462642));
#55125=CARTESIAN_POINT('Ctrl Pts',(5.78006132540833,0.800866334091529,5.84423292720708));
#55126=CARTESIAN_POINT('Ctrl Pts',(2.47781181352747,5.28308095975332,6.00252324978771));
#55127=CARTESIAN_POINT('Ctrl Pts',(-3.07991218091209,4.95627246713037,6.16081357236837));
#55128=CARTESIAN_POINT('Ctrl Pts',(-5.83408858766023,0.117924390593317,
6.319103894949));
#55129=CARTESIAN_POINT('Ctrl Pts',(-3.27767689138409,-4.82776656501236,
6.47739421752966));
#55130=CARTESIAN_POINT('Ctrl Pts',(2.26230141403803,-5.37889283427418,6.63568454011029));
#55131=CARTESIAN_POINT('Ctrl Pts',(5.7429776032295,-1.03378143694346,6.79397486269095));
#55132=CARTESIAN_POINT('Ctrl Pts',(3.99600116469878,4.25234882180315,6.95226518527158));
#55133=CARTESIAN_POINT('Ctrl Pts',(-1.38840996925396,5.66769914231875,7.11055550785224));
#55134=CARTESIAN_POINT('Ctrl Pts',(-5.50899499668582,1.92392046016856,7.26884583043288));
#55135=CARTESIAN_POINT('Ctrl Pts',(-4.61491443420867,-3.57114275484712,
7.42713615301353));
#55136=CARTESIAN_POINT('Ctrl Pts',(0.47997818700567,-5.81550657729517,7.58542647559416));
#55137=CARTESIAN_POINT('Ctrl Pts',(5.13796169871233,-2.76619691871885,7.74371679817482));
#55138=CARTESIAN_POINT('Ctrl Pts',(5.1190196099595,2.80109515072493,7.90200712075546));
#55139=CARTESIAN_POINT('Ctrl Pts',(0.440394310825021,5.81863804180648,8.06029744333611));
#55140=CARTESIAN_POINT('Ctrl Pts',(-4.63910813519642,3.53965697780435,8.21858776591675));
#55141=CARTESIAN_POINT('Ctrl Pts',(-5.49577575427904,-1.96136296213705,
8.3768780884974));
#55142=CARTESIAN_POINT('Ctrl Pts',(-1.34981084575569,-5.67701563246438,
8.53516841107803));
#55143=CARTESIAN_POINT('Ctrl Pts',(4.02484459618971,-4.22505879096223,8.69345873365869));
#55144=CARTESIAN_POINT('Ctrl Pts',(5.73581007047566,1.07283672848883,8.85174905623933));
#55145=CARTESIAN_POINT('Ctrl Pts',(2.22564729760008,5.39416257794014,9.01003937881998));
#55146=CARTESIAN_POINT('Ctrl Pts',(-3.31045249741171,4.80535119142661,9.16832970140062));
#55147=CARTESIAN_POINT('Ctrl Pts',(-5.83315107572507,-0.157620868961595,
9.32662002398126));
#55148=CARTESIAN_POINT('Ctrl Pts',(-3.04611493876333,-4.97711558941596,
9.48491034656191));
#55149=CARTESIAN_POINT('Ctrl Pts',(2.51370421497615,-5.26609788459876,9.64320066914256));
#55150=CARTESIAN_POINT('Ctrl Pts',(5.78537715735888,-0.761516222857186,
9.8014909917232));
#55151=CARTESIAN_POINT('Ctrl Pts',(3.79080248595607,4.43624980394858,9.95978131430386));
#55152=CARTESIAN_POINT('Ctrl Pts',(-1.6544209509478,5.59583658871751,10.1180716368845));
#55153=CARTESIAN_POINT('Ctrl Pts',(-5.59367681682763,1.66170860244797,10.2763619594652));
#55154=CARTESIAN_POINT('Ctrl Pts',(-4.44118388437089,-3.78502067573863,
10.4346522820458));
#55155=CARTESIAN_POINT('Ctrl Pts',(0.753979628983335,-5.78636418916428,
10.5929426046264));
#55156=CARTESIAN_POINT('Ctrl Pts',(5.26281910261167,-2.52056162466824,10.7512329272071));
#55157=CARTESIAN_POINT('Ctrl Pts',(4.98107919185876,3.03962923643596,10.9095232497877));
#55158=CARTESIAN_POINT('Ctrl Pts',(0.165218912680596,5.83294081244249,11.0678135723684));
#55159=CARTESIAN_POINT('Ctrl Pts',(-4.80103496763896,3.31670906925412,11.226103894949));
#55160=CARTESIAN_POINT('Ctrl Pts',(-5.3970570974028,-2.21861905200931,11.3843942175297));
#55161=CARTESIAN_POINT('Ctrl Pts',(-1.08030720079852,-5.73440774295545,
11.5426845401103));
#55162=CARTESIAN_POINT('Ctrl Pts',(4.219812502755,-4.03034468155729,11.7009748626909));
#55163=CARTESIAN_POINT('Ctrl Pts',(5.67876906018774,1.34241490293389,11.8592651852716));
#55164=CARTESIAN_POINT('Ctrl Pts',(1.96852001545618,5.49321624909424,12.0175555078522));
#55165=CARTESIAN_POINT('Ctrl Pts',(-3.53361114034896,4.64371490504813,12.1758458304329));
#55166=CARTESIAN_POINT('Ctrl Pts',(-5.81920675667964,-0.432814664237157,
12.3341361530135));
#55167=CARTESIAN_POINT('Ctrl Pts',(-2.80776073459116,-5.11536660151085,
12.4924264755942));
#55168=CARTESIAN_POINT('Ctrl Pts',(2.75950193807008,-5.14156054757227,12.6507167981748));
#55169=CARTESIAN_POINT('Ctrl Pts',(5.81487643104491,-0.487552973782061,
12.8090071207555));
#55170=CARTESIAN_POINT('Ctrl Pts',(3.57715104538901,4.61025880065714,12.9672974433361));
#55171=CARTESIAN_POINT('Ctrl Pts',(-1.91674289151962,5.51149639375472,13.1255877659167));
#55172=CARTESIAN_POINT('Ctrl Pts',(-5.66588581148519,1.39579145354196,13.2838780884974));
#55173=CARTESIAN_POINT('Ctrl Pts',(-4.25755034704318,-3.99045872713326,
13.442168411078));
#55174=CARTESIAN_POINT('Ctrl Pts',(1.02629984112814,-5.74431931969763,13.6004587336587));
#55175=CARTESIAN_POINT('Ctrl Pts',(5.37594143021732,-2.26930596206795,13.7587490562393));
#55176=CARTESIAN_POINT('Ctrl Pts',(4.8320319233711,3.27138553246996,13.91703937882));
#55177=CARTESIAN_POINT('Ctrl Pts',(-0.110324891911251,5.8342372448088,14.0753297014006));
#55178=CARTESIAN_POINT('Ctrl Pts',(-4.95225641377798,3.0863655361992,14.2336200239813));
#55179=CARTESIAN_POINT('Ctrl Pts',(-5.28630403923151,-2.47092804732617,
14.3919103465619));
#55180=CARTESIAN_POINT('Ctrl Pts',(-0.808394678245584,-5.77901322496909,
14.5502006691425));
#55181=CARTESIAN_POINT('Ctrl Pts',(4.40537103766032,-3.82664367730009,14.7084909917232));
#55182=CARTESIAN_POINT('Ctrl Pts',(5.60906548477092,1.60899975000773,14.8667813143038));
#55183=CARTESIAN_POINT('Ctrl Pts',(1.70700331210297,5.58002110223998,15.0250716368845));
#55184=CARTESIAN_POINT('Ctrl Pts',(-3.74889050980069,4.47172402646598,15.1833619594651));
#55185=CARTESIAN_POINT('Ctrl Pts',(-5.7922867217461,-0.707043367010812,
15.3416522820458));
#55186=CARTESIAN_POINT('Ctrl Pts',(-2.56314576668009,-5.24221132595445,
15.4999426046264));
#55187=CARTESIAN_POINT('Ctrl Pts',(2.99914650864464,-5.00555852161226,15.658232927207));
#55188=CARTESIAN_POINT('Ctrl Pts',(5.83140963307135,-0.2125025674033,15.8165232497877));
#55189=CARTESIAN_POINT('Ctrl Pts',(3.35552327049972,4.77398779042229,15.9748135723683));
#55190=CARTESIAN_POINT('Ctrl Pts',(-2.17479091272675,5.41486664825819,16.133103894949));
#55191=CARTESIAN_POINT('Ctrl Pts',(-5.72546087416986,1.12676190338666,16.2913942175296));
#55192=CARTESIAN_POINT('Ctrl Pts',(-4.06442347000951,-4.18699871789581,
16.4496845401103));
#55193=CARTESIAN_POINT('Ctrl Pts',(1.29633194620277,-5.68946591914921,16.6079748626909));
#55194=CARTESIAN_POINT('Ctrl Pts',(5.47707578180272,-2.01298980380955,16.7662651852716));
#55195=CARTESIAN_POINT('Ctrl Pts',(4.67221141036031,3.49584654228241,16.9245555078522));
#55196=CARTESIAN_POINT('Ctrl Pts',(-0.385625099973721,5.82252583304098,
17.0828458304329));
#55197=CARTESIAN_POINT('Ctrl Pts',(-5.09243067800049,2.84913735309004,17.2411361530135));
#55198=CARTESIAN_POINT('Ctrl Pts',(-5.163772332666,-2.71772228672297,17.3994264755942));
#55199=CARTESIAN_POINT('Ctrl Pts',(-0.534662778757779,-5.81074229086598,
17.5577167981748));
#55200=CARTESIAN_POINT('Ctrl Pts',(4.58107430334251,-3.61439149963352,17.7160071207555));
#55201=CARTESIAN_POINT('Ctrl Pts',(5.52691620363093,1.87196148635973,17.8742974433361));
#55202=CARTESIAN_POINT('Ctrl Pts',(1.44156288337564,5.6544511543935,18.0325877659168));
#55203=CARTESIAN_POINT('Ctrl Pts',(-3.95558608138272,4.2896328856293,18.1908780884974));
#55204=CARTESIAN_POINT('Ctrl Pts',(-5.75288016701676,-0.979448557484372,
18.349168411078));
#55205=CARTESIAN_POINT('Ctrl Pts',(-2.31199479018177,-5.35783906812632,
18.5074587336587));
#55206=CARTESIAN_POINT('Ctrl Pts',(3.23053211221357,-4.8574916848313,18.6657490562393));
#55207=CARTESIAN_POINT('Ctrl Pts',(5.83796734686214,0.0612873527283092,
18.82403937882));
#55208=CARTESIAN_POINT('Ctrl Pts',(3.12041701848007,4.9304530959418,18.9823297014006));
#55209=CARTESIAN_POINT('Ctrl Pts',(-1.49215234175522,5.23769617354117,19.1142383035512));
#55210=CARTESIAN_POINT('Ctrl Pts',(-4.11442054260868,3.08380732139205,19.2197651852716));
#55211=CARTESIAN_POINT('Ctrl Pts',(-4.76857407193705,1.53464683800148,19.2725286261318));
#55212=CARTESIAN_POINT('Ctrl Pts',(-4.8886350428845,0.724300640260437,19.2989103465619));
#55213=CARTESIAN_POINT('Ctrl Pts',(2.75898463274061,-3.86904481704479,-0.21939310229206));
#55214=CARTESIAN_POINT('Ctrl Pts',(3.40032229220555,-3.4117121081895,-0.193011381861952));
#55215=CARTESIAN_POINT('Ctrl Pts',(4.44060745341011,-2.17382463487172,-0.140247941001737));
#55216=CARTESIAN_POINT('Ctrl Pts',(5.13763779242852,1.01384631572915,-0.0347210592813072));
#55217=CARTESIAN_POINT('Ctrl Pts',(2.85654153638278,4.82897220710893,0.0971875428692309));
#55218=CARTESIAN_POINT('Ctrl Pts',(-2.50165581870078,5.02561530273532,0.255477865449875));
#55219=CARTESIAN_POINT('Ctrl Pts',(-5.57263289575413,0.640994911623377,
0.413768188030522));
#55220=CARTESIAN_POINT('Ctrl Pts',(-3.5761817604452,-4.32373785104547,0.572058510611166));
#55221=CARTESIAN_POINT('Ctrl Pts',(1.67824765945831,-5.35445790830635,0.730348833191812));
#55222=CARTESIAN_POINT('Ctrl Pts',(5.4036136325935,-1.51026807361131,0.888639155772457));
#55223=CARTESIAN_POINT('Ctrl Pts',(4.2109753740215,3.70819317158555,1.0469294783531));
#55224=CARTESIAN_POINT('Ctrl Pts',(-0.815166878242221,5.55145252603366,
1.20521980093375));
#55225=CARTESIAN_POINT('Ctrl Pts',(-5.09908684732198,2.3412676449565,1.36351012351439));
#55226=CARTESIAN_POINT('Ctrl Pts',(-4.74157313673304,-3.0000313688591,1.52180044609504));
#55227=CARTESIAN_POINT('Ctrl Pts',(-0.0678988005016982,-5.6105316146419,
1.68009076867568));
#55228=CARTESIAN_POINT('Ctrl Pts',(4.66755285374621,-3.11392192994849,1.83838109125633));
#55229=CARTESIAN_POINT('Ctrl Pts',(5.15429242820228,2.21718354955942,1.99667141383697));
#55230=CARTESIAN_POINT('Ctrl Pts',(0.94923316008907,5.53006141943627,2.15496173641762));
#55231=CARTESIAN_POINT('Ctrl Pts',(-4.11987919351274,3.8090949121538,2.31325205899827));
#55232=CARTESIAN_POINT('Ctrl Pts',(-5.43879672158246,-1.37916997995865,
2.47154238157891));
#55233=CARTESIAN_POINT('Ctrl Pts',(-1.80694682117044,-5.31202037247638,
2.62983270415955));
#55234=CARTESIAN_POINT('Ctrl Pts',(3.46970958150474,-4.40950462174014,2.7881230267402));
#55235=CARTESIAN_POINT('Ctrl Pts',(5.58799834129561,0.506844868502552,2.94641334932084));
#55236=CARTESIAN_POINT('Ctrl Pts',(2.61970707944744,4.96182945569518,3.10470367190149));
#55237=CARTESIAN_POINT('Ctrl Pts',(-2.73322139641198,4.90021605136558,3.26299399448213));
#55238=CARTESIAN_POINT('Ctrl Pts',(-5.59818409073885,0.378089491324522,
3.42128431706278));
#55239=CARTESIAN_POINT('Ctrl Pts',(-3.3672951333158,-4.48820010500075,3.57957463964342));
#55240=CARTESIAN_POINT('Ctrl Pts',(1.92873709970399,-5.269021719585,3.73786496222407));
#55241=CARTESIAN_POINT('Ctrl Pts',(5.46910037009403,-1.25361790595597,3.89615528480471));
#55242=CARTESIAN_POINT('Ctrl Pts',(4.03111287624724,3.90291502315395,4.05444560738536));
#55243=CARTESIAN_POINT('Ctrl Pts',(-1.07627040252322,5.50674665467138,4.21273592996601));
#55244=CARTESIAN_POINT('Ctrl Pts',(-5.20395844627879,2.09795929218125,4.37102625254665));
#55245=CARTESIAN_POINT('Ctrl Pts',(-4.5946461169747,-3.22053470093006,4.5293165751273));
#55246=CARTESIAN_POINT('Ctrl Pts',(0.197028656494944,-5.60747683086738,
4.68760689770794));
#55247=CARTESIAN_POINT('Ctrl Pts',(4.80935441551997,-2.89010844202325,4.84589722028858));
#55248=CARTESIAN_POINT('Ctrl Pts',(5.04387549110129,2.45803513617603,5.00418754286923));
#55249=CARTESIAN_POINT('Ctrl Pts',(0.687114694030425,5.56870632173167,5.16247786544987));
#55250=CARTESIAN_POINT('Ctrl Pts',(-4.29510508687517,3.61035856850998,5.32076818803052));
#55251=CARTESIAN_POINT('Ctrl Pts',(-5.3676252406787,-1.63438550412508,5.47905851061116));
#55252=CARTESIAN_POINT('Ctrl Pts',(-1.55416426541541,-5.39139964541496,
5.63734883319181));
#55253=CARTESIAN_POINT('Ctrl Pts',(3.67400376032591,-4.24079156167736,5.79563915577246));
#55254=CARTESIAN_POINT('Ctrl Pts',(5.55784124207616,0.770076248402076,5.95392947835309));
#55255=CARTESIAN_POINT('Ctrl Pts',(2.38254992672651,5.07996777028487,6.11221980093375));
#55256=CARTESIAN_POINT('Ctrl Pts',(-2.9615019594687,4.76572374824029,6.27051012351439));
#55257=CARTESIAN_POINT('Ctrl Pts',(-5.60979137364659,0.113390672622288,
6.42880044609503));
#55258=CARTESIAN_POINT('Ctrl Pts',(-3.15166341316413,-4.64215838060276,
6.58709076867568));
#55259=CARTESIAN_POINT('Ctrl Pts',(2.17532503429963,-5.17209606403701,6.74538109125632));
#55260=CARTESIAN_POINT('Ctrl Pts',(5.52218323968972,-0.994036703430842,
6.90367141383697));
#55261=CARTESIAN_POINT('Ctrl Pts',(3.84237101065328,4.08886313257964,7.06196173641762));
#55262=CARTESIAN_POINT('Ctrl Pts',(-1.33503119666024,5.44979893247647,7.22025205899827));
#55263=CARTESIAN_POINT('Ctrl Pts',(-5.29719632218758,1.84995346554449,7.3785423815789));
#55264=CARTESIAN_POINT('Ctrl Pts',(-4.43748955713467,-3.43384669587891,
7.53683270415955));
#55265=CARTESIAN_POINT('Ctrl Pts',(0.461524958448211,-5.59192376675569,
7.6951230267402));
#55266=CARTESIAN_POINT('Ctrl Pts',(4.94042776047775,-2.65984778586643,7.85341334932084));
#55267=CARTESIAN_POINT('Ctrl Pts',(4.92221391876315,2.69340432137696,8.01170367190149));
#55268=CARTESIAN_POINT('Ctrl Pts',(0.42346292291388,5.59493483906605,8.16999399448214));
#55269=CARTESIAN_POINT('Ctrl Pts',(-4.46075310774047,3.40357142017932,8.32828431706278));
#55270=CARTESIAN_POINT('Ctrl Pts',(-5.28448530642128,-1.88595645408243,
8.48657463964342));
#55271=CARTESIAN_POINT('Ctrl Pts',(-1.29791605403297,-5.4587572410908,8.64486496222408));
#55272=CARTESIAN_POINT('Ctrl Pts',(3.87010552834755,-4.0626222935355,8.8031552848047));
#55273=CARTESIAN_POINT('Ctrl Pts',(5.51529126970868,1.03159047628066,8.96144560738537));
#55274=CARTESIAN_POINT('Ctrl Pts',(2.1400801210432,5.18677874754585,9.11973592996599));
#55275=CARTESIAN_POINT('Ctrl Pts',(-3.18317892911787,4.62060478787114,9.27802625254666));
#55276=CARTESIAN_POINT('Ctrl Pts',(-5.60888990527024,-0.151560981243543,
9.43631657512728));
#55277=CARTESIAN_POINT('Ctrl Pts',(-2.92900408518884,-4.78576553640322,
9.59460689770795));
#55278=CARTESIAN_POINT('Ctrl Pts',(2.41706240986782,-5.06363762598407,9.75289722028857));
#55279=CARTESIAN_POINT('Ctrl Pts',(5.56295270169353,-0.732238990493172,
9.91118754286925));
#55280=CARTESIAN_POINT('Ctrl Pts',(3.6450613948327,4.26569386247748,10.0694778654499));
#55281=CARTESIAN_POINT('Ctrl Pts',(-1.59081512725699,5.38069920469153,10.2277681880305));
#55282=CARTESIAN_POINT('Ctrl Pts',(-5.37862246733407,1.5978225979022,10.3860585106112));
#55283=CARTESIAN_POINT('Ctrl Pts',(-4.27043824737563,-3.63950187193647,
10.5443488331918));
#55284=CARTESIAN_POINT('Ctrl Pts',(0.724992148306133,-5.56390178610049,
10.7026391557725));
#55285=CARTESIAN_POINT('Ctrl Pts',(5.0604848999617,-2.42365617977001,10.8609294783531));
#55286=CARTESIAN_POINT('Ctrl Pts',(4.78957675429235,2.92276773199996,11.0192198009338));
#55287=CARTESIAN_POINT('Ctrl Pts',(0.158866910776627,5.60868772576421,11.1775101235144));
#55288=CARTESIAN_POINT('Ctrl Pts',(-4.61645450550797,3.18919496096631,11.335800446095));
#55289=CARTESIAN_POINT('Ctrl Pts',(-5.18956198439054,-2.13332208319472,
11.4940907686757));
#55290=CARTESIAN_POINT('Ctrl Pts',(-1.03877373901142,-5.51394285603487,
11.6523810912563));
#55291=CARTESIAN_POINT('Ctrl Pts',(4.05757770398459,-3.87539415757996,11.810671413837));
#55292=CARTESIAN_POINT('Ctrl Pts',(5.46044325657874,1.29080445543139,11.9689617364176));
#55293=CARTESIAN_POINT('Ctrl Pts',(1.89283834752078,5.28202420390446,12.1272520589983));
#55294=CARTESIAN_POINT('Ctrl Pts',(-3.39775802082929,4.4651827658415,12.2855423815789));
#55295=CARTESIAN_POINT('Ctrl Pts',(-5.59548168914238,-0.416174683216324,
12.4438327041595));
#55296=CARTESIAN_POINT('Ctrl Pts',(-2.69981364038388,-4.91870135377977,
12.6021230267402));
#55297=CARTESIAN_POINT('Ctrl Pts',(2.65341020026489,-4.94388824809053,12.7604133493208));
#55298=CARTESIAN_POINT('Ctrl Pts',(5.59131784709134,-0.468808525174477,
12.9187036719015));
#55299=CARTESIAN_POINT('Ctrl Pts',(3.43962399184309,4.43301291394634,13.0769939944821));
#55300=CARTESIAN_POINT('Ctrl Pts',(-1.84305184550816,5.29960155061157,13.2352843170628));
#55301=CARTESIAN_POINT('Ctrl Pts',(-5.44805531691171,1.34212889260043,13.3935746396434));
#55302=CARTESIAN_POINT('Ctrl Pts',(-4.0938646801192,-3.8370416574944,13.5518649622241));
#55303=CARTESIAN_POINT('Ctrl Pts',(0.986842744848443,-5.52347337256235,
13.7101552848047));
#55304=CARTESIAN_POINT('Ctrl Pts',(5.1692581295817,-2.18206028566305,13.8684456073854));
#55305=CARTESIAN_POINT('Ctrl Pts',(4.64625975310793,3.1456139316668,14.026735929966));
#55306=CARTESIAN_POINT('Ctrl Pts',(-0.106083344063608,5.60993431552639,
14.1850262525467));
#55307=CARTESIAN_POINT('Ctrl Pts',(-4.76186209596784,2.96770720923078,14.3433165751273));
#55308=CARTESIAN_POINT('Ctrl Pts',(-5.08306693533551,-2.37593081361676,
14.5016068977079));
#55309=CARTESIAN_POINT('Ctrl Pts',(-0.777315158037826,-5.55683343687841,
14.6598972202886));
#55310=CARTESIAN_POINT('Ctrl Pts',(4.23600226041317,-3.67952463669161,14.8181875428692));
#55311=CARTESIAN_POINT('Ctrl Pts',(5.39341950296062,1.54714018859507,14.9764778654499));
#55312=CARTESIAN_POINT('Ctrl Pts',(1.64137590835962,5.3654917599847,15.1347681880305));
#55313=CARTESIAN_POINT('Ctrl Pts',(-3.60476076539315,4.29980424398346,15.2930585106112));
#55314=CARTESIAN_POINT('Ctrl Pts',(-5.56959662115286,-0.679860396607744,
15.4513488331918));
#55315=CARTESIAN_POINT('Ctrl Pts',(-2.46460313299549,-5.04066940933542,
15.6096391557725));
#55316=CARTESIAN_POINT('Ctrl Pts',(2.88384140208001,-4.81311495238798,15.7679294783531));
#55317=CARTESIAN_POINT('Ctrl Pts',(5.60721541407427,-0.204332699372805,
15.9262198009337));
#55318=CARTESIAN_POINT('Ctrl Pts',(3.22651691246755,4.59044718334415,16.0845101235144));
#55319=CARTESIAN_POINT('Ctrl Pts',(-2.09117895938438,5.20668682972943,16.242800446095));
#55320=CARTESIAN_POINT('Ctrl Pts',(-5.50533995832764,1.08344244534466,16.4010907686757));
#55321=CARTESIAN_POINT('Ctrl Pts',(-3.90816275384159,-4.02602547702165,
16.5593810912563));
#55322=CARTESIAN_POINT('Ctrl Pts',(1.24649320282389,-5.47072886438628,16.717671413837));
#55323=CARTESIAN_POINT('Ctrl Pts',(5.26650427258732,-1.9355984515789,16.8759617364176));
#55324=CARTESIAN_POINT('Ctrl Pts',(4.49258369527158,3.36144531949132,17.0342520589983));
#55325=CARTESIAN_POINT('Ctrl Pts',(-0.370799367680139,5.59867316038258,
17.1925423815789));
#55326=CARTESIAN_POINT('Ctrl Pts',(-4.89664722417207,2.73959949451312,17.3508327041595));
#55327=CARTESIAN_POINT('Ctrl Pts',(-4.96524607948782,-2.61323680827755,
17.5091230267402));
#55328=CARTESIAN_POINT('Ctrl Pts',(-0.51410714784639,-5.58734264795531,
17.6674133493208));
#55329=CARTESIAN_POINT('Ctrl Pts',(4.40495044303595,-3.47543270057839,17.8257036719015));
#55330=CARTESIAN_POINT('Ctrl Pts',(5.31442853088914,1.79999210505495,17.9839939944821));
#55331=CARTESIAN_POINT('Ctrl Pts',(1.38614059526527,5.43706027634114,18.1422843170628));
#55332=CARTESIAN_POINT('Ctrl Pts',(-3.80350972455094,4.12471377428376,18.3005746396434));
#55333=CARTESIAN_POINT('Ctrl Pts',(-5.53170508977411,-0.941792704404255,
18.4588649622241));
#55334=CARTESIAN_POINT('Ctrl Pts',(-2.22310790023142,-5.15185173042014,
18.6171552848047));
#55335=CARTESIAN_POINT('Ctrl Pts',(3.1063311609144,-4.67074068925906,18.7754456073854));
#55336=CARTESIAN_POINT('Ctrl Pts',(5.61352101017582,0.0589311008023047,
18.933735929966));
#55337=CARTESIAN_POINT('Ctrl Pts',(3.00044954913339,4.74089702790683,19.0920262525466));
#55338=CARTESIAN_POINT('Ctrl Pts',(-1.43478509267926,5.03632784635119,19.2239348546972));
#55339=CARTESIAN_POINT('Ctrl Pts',(-3.95623764032305,2.96524734748178,19.3294617364176));
#55340=CARTESIAN_POINT('Ctrl Pts',(-4.58524160053518,1.47564584665783,19.3822251772778));
#55341=CARTESIAN_POINT('Ctrl Pts',(-4.70068671060039,0.696454197190917,
19.4086068977079));
#55342=CARTESIAN_POINT('Ctrl Pts',(2.64867169498374,-3.71434815979762,-0.109696551146031));
#55343=CARTESIAN_POINT('Ctrl Pts',(3.26436664500038,-3.27530106009269,-0.0833148307159233));
#55344=CARTESIAN_POINT('Ctrl Pts',(4.26305791297495,-2.08690824585116,-0.0305513898557082));
#55345=CARTESIAN_POINT('Ctrl Pts',(4.93221877295011,0.973309531219794,0.0749754918647217));
#55346=CARTESIAN_POINT('Ctrl Pts',(2.74232796485231,4.63589461465298,0.20688409401526));
#55347=CARTESIAN_POINT('Ctrl Pts',(-2.40163170137059,4.82467529694413,0.365174416595904));
#55348=CARTESIAN_POINT('Ctrl Pts',(-5.34982139529258,0.615365906318545,
0.52346473917655));
#55349=CARTESIAN_POINT('Ctrl Pts',(-3.43319469510752,-4.15086112720317,
0.681755061757195));
#55350=CARTESIAN_POINT('Ctrl Pts',(1.6111460064076,-5.14036973436311,0.84004538433784));
#55351=CARTESIAN_POINT('Ctrl Pts',(5.18756005721624,-1.44988277605528,0.998335706918485));
#55352=CARTESIAN_POINT('Ctrl Pts',(4.04260725090194,3.55992787221662,1.15662602949913));
#55353=CARTESIAN_POINT('Ctrl Pts',(-0.782573926460673,5.32948788378904,
1.31491635207978));
#55354=CARTESIAN_POINT('Ctrl Pts',(-4.89520921664203,2.24765635443844,1.47320667466042));
#55355=CARTESIAN_POINT('Ctrl Pts',(-4.55199003572729,-2.88008061968337,
1.63149699724107));
#55356=CARTESIAN_POINT('Ctrl Pts',(-0.065183991559061,-5.3862048034504,
1.78978731982171));
#55357=CARTESIAN_POINT('Ctrl Pts',(4.48092931792725,-2.98941747567865,1.94807764240236));
#55358=CARTESIAN_POINT('Ctrl Pts',(4.94820750367398,2.12853353389945,2.106367964983));
#55359=CARTESIAN_POINT('Ctrl Pts',(0.911279814041717,5.30895206133591,2.26465828756365));
#55360=CARTESIAN_POINT('Ctrl Pts',(-3.95515338400782,3.6567952418446,2.42294861014429));
#55361=CARTESIAN_POINT('Ctrl Pts',(-5.22133641495353,-1.32402639911015,
2.58123893272494));
#55362=CARTESIAN_POINT('Ctrl Pts',(-1.73469936830376,-5.09962898552972,
2.73952925530558));
#55363=CARTESIAN_POINT('Ctrl Pts',(3.33097961086378,-4.23319867095506,2.89781957788623));
#55364=CARTESIAN_POINT('Ctrl Pts',(5.36457248168994,0.486579606504366,3.05610990046687));
#55365=CARTESIAN_POINT('Ctrl Pts',(2.51496289908231,4.7634398099498,3.21440022304752));
#55366=CARTESIAN_POINT('Ctrl Pts',(-2.62393855438374,4.70428990453067,3.37269054562815));
#55367=CARTESIAN_POINT('Ctrl Pts',(-5.37435097263271,0.362972276814471,
3.53098086820881));
#55368=CARTESIAN_POINT('Ctrl Pts',(-3.23266001645341,-4.30874765972506,
3.68927119078945));
#55369=CARTESIAN_POINT('Ctrl Pts',(1.85162008603739,-5.05834955487095,3.8475615133701));
#55370=CARTESIAN_POINT('Ctrl Pts',(5.25042842768707,-1.20349429439626,4.00585183595074));
#55371=CARTESIAN_POINT('Ctrl Pts',(3.86993622505047,3.74686412786792,4.16414215853139));
#55372=CARTESIAN_POINT('Ctrl Pts',(-1.03323770545266,5.28656949465716,4.32243248111203));
#55373=CARTESIAN_POINT('Ctrl Pts',(-4.9958877171557,2.01407623967397,4.48072280369268));
#55374=CARTESIAN_POINT('Ctrl Pts',(-4.41093762324043,-3.09176753064878,
4.63901312627333));
#55375=CARTESIAN_POINT('Ctrl Pts',(0.18915082721592,-5.38327215959954,4.79730344885396));
#55376=CARTESIAN_POINT('Ctrl Pts',(4.61706120446174,-2.77455275936658,4.95559377143462));
#55377=CARTESIAN_POINT('Ctrl Pts',(4.84220538518603,2.3597551117919,5.11388409401526));
#55378=CARTESIAN_POINT('Ctrl Pts',(0.65964167385663,5.34605181812708,5.2721744165959));
#55379=CARTESIAN_POINT('Ctrl Pts',(-4.12337319156663,3.46600500621685,5.43046473917655));
#55380=CARTESIAN_POINT('Ctrl Pts',(-5.15301059511283,-1.56903759886758,
5.58875506175719));
#55381=CARTESIAN_POINT('Ctrl Pts',(-1.49202385918035,-5.17583442390216,
5.74704538433784));
#55382=CARTESIAN_POINT('Ctrl Pts',(3.52710546182805,-4.07123129300759,5.90533570691848));
#55383=CARTESIAN_POINT('Ctrl Pts',(5.33562115874398,0.739286162712621,6.06362602949913));
#55384=CARTESIAN_POINT('Ctrl Pts',(2.28728803992556,4.87685458081641,6.22191635207978));
#55385=CARTESIAN_POINT('Ctrl Pts',(-2.84309173802532,4.5751750293502,6.38020667466042));
#55386=CARTESIAN_POINT('Ctrl Pts',(-5.38549415963294,0.108856954651256,
6.53849699724107));
#55387=CARTESIAN_POINT('Ctrl Pts',(-3.02564993494416,-4.45655019619314,
6.6967873198217));
#55388=CARTESIAN_POINT('Ctrl Pts',(2.08834865456124,-4.96529929379983,6.85507764240235));
#55389=CARTESIAN_POINT('Ctrl Pts',(5.30138887614994,-0.954291969918219,
7.013367964983));
#55390=CARTESIAN_POINT('Ctrl Pts',(3.68874085660779,3.92537744335614,7.17165828756364));
#55391=CARTESIAN_POINT('Ctrl Pts',(-1.28165242406652,5.23189872263419,7.32994861014429));
#55392=CARTESIAN_POINT('Ctrl Pts',(-5.08539764768935,1.77598647092042,7.48823893272493));
#55393=CARTESIAN_POINT('Ctrl Pts',(-4.26006468006067,-3.2965506369107,7.64652925530558));
#55394=CARTESIAN_POINT('Ctrl Pts',(0.443071729890745,-5.36834095621621,
7.80481957788623));
#55395=CARTESIAN_POINT('Ctrl Pts',(4.74289382224317,-2.55349865301401,7.96310990046686));
#55396=CARTESIAN_POINT('Ctrl Pts',(4.7254082275668,2.58571349202899,8.12140022304752));
#55397=CARTESIAN_POINT('Ctrl Pts',(0.406531535002743,5.37123163632562,8.27969054562816));
#55398=CARTESIAN_POINT('Ctrl Pts',(-4.28239808028453,3.26748586255429,8.43798086820882));
#55399=CARTESIAN_POINT('Ctrl Pts',(-5.07319485856352,-1.81054994602781,
8.59627119078944));
#55400=CARTESIAN_POINT('Ctrl Pts',(-1.24602126231025,-5.24049884971722,
8.7545615133701));
#55401=CARTESIAN_POINT('Ctrl Pts',(3.71536646050538,-3.90018579610877,8.91285183595074));
#55402=CARTESIAN_POINT('Ctrl Pts',(5.29477246894171,0.99034422407249,9.07114215853139));
#55403=CARTESIAN_POINT('Ctrl Pts',(2.05451294448632,4.97939491715156,9.22943248111203));
#55404=CARTESIAN_POINT('Ctrl Pts',(-3.05590536082404,4.43585838431568,9.38772280369268));
#55405=CARTESIAN_POINT('Ctrl Pts',(-5.38462873481541,-0.145501093525492,
9.54601312627332));
#55406=CARTESIAN_POINT('Ctrl Pts',(-2.81189323161436,-4.59441548339048,
9.70430344885398));
#55407=CARTESIAN_POINT('Ctrl Pts',(2.32042060475949,-4.86117736736937,9.8625937714346));
#55408=CARTESIAN_POINT('Ctrl Pts',(5.34052824602817,-0.702961758129157,
10.0208840940153));
#55409=CARTESIAN_POINT('Ctrl Pts',(3.49932030370932,4.09513792100639,10.1791744165959));
#55410=CARTESIAN_POINT('Ctrl Pts',(-1.52720930356618,5.16556182066556,10.3374647391766));
#55411=CARTESIAN_POINT('Ctrl Pts',(-5.16356811784049,1.53393659335643,10.4957550617572));
#55412=CARTESIAN_POINT('Ctrl Pts',(-4.09969261038038,-3.49398306813431,
10.6540453843378));
#55413=CARTESIAN_POINT('Ctrl Pts',(0.69600466762893,-5.34143938303671,10.8123357069185));
#55414=CARTESIAN_POINT('Ctrl Pts',(4.85815069731172,-2.32675073487178,10.9706260294991));
#55415=CARTESIAN_POINT('Ctrl Pts',(4.59807431672593,2.80590622756395,11.1289163520798));
#55416=CARTESIAN_POINT('Ctrl Pts',(0.152514908872657,5.38443463908592,11.2872066746604));
#55417=CARTESIAN_POINT('Ctrl Pts',(-4.43187404337698,3.0616808526785,11.4454969972411));
#55418=CARTESIAN_POINT('Ctrl Pts',(-4.98206687137828,-2.04802511438014,
11.6037873198217));
#55419=CARTESIAN_POINT('Ctrl Pts',(-0.997240277224328,-5.29347796911429,
11.7620776424023));
#55420=CARTESIAN_POINT('Ctrl Pts',(3.89534290521418,-3.72044363360263,11.920367964983));
#55421=CARTESIAN_POINT('Ctrl Pts',(5.24211745296974,1.2391940079289,12.0786582875636));
#55422=CARTESIAN_POINT('Ctrl Pts',(1.81715667958537,5.07083215871469,12.2369486101443));
#55423=CARTESIAN_POINT('Ctrl Pts',(-3.26190490130962,4.28665062663486,12.3952389327249));
#55424=CARTESIAN_POINT('Ctrl Pts',(-5.37175662160512,-0.399534702195488,
12.5535292553056));
#55425=CARTESIAN_POINT('Ctrl Pts',(-2.59186654617659,-4.72203610604869,
12.7118195778862));
#55426=CARTESIAN_POINT('Ctrl Pts',(2.5473184624597,-4.74621594860878,12.8701099004669));
#55427=CARTESIAN_POINT('Ctrl Pts',(5.36775926313778,-0.450064076566892,
13.0284002230475));
#55428=CARTESIAN_POINT('Ctrl Pts',(3.30209693829715,4.25576702723554,13.1866905456282));
#55429=CARTESIAN_POINT('Ctrl Pts',(-1.76936079949669,5.08770670746843,13.3449808682088));
#55430=CARTESIAN_POINT('Ctrl Pts',(-5.23022482233823,1.28846633165889,13.5032711907894));
#55431=CARTESIAN_POINT('Ctrl Pts',(-3.93017901319522,-3.68362458785553,
13.6615615133701));
#55432=CARTESIAN_POINT('Ctrl Pts',(0.947385648568746,-5.30262742542707,
13.8198518359507));
#55433=CARTESIAN_POINT('Ctrl Pts',(4.96257482894607,-2.09481460925815,13.9781421585314));
#55434=CARTESIAN_POINT('Ctrl Pts',(4.46048758284477,3.01984233086364,14.136432481112));
#55435=CARTESIAN_POINT('Ctrl Pts',(-0.101841796215968,5.38563138624398,
14.2947228036927));
#55436=CARTESIAN_POINT('Ctrl Pts',(-4.57146777815769,2.84904888226236,14.4530131262733));
#55437=CARTESIAN_POINT('Ctrl Pts',(-4.87982983143951,-2.28093357990735,
14.611303448854));
#55438=CARTESIAN_POINT('Ctrl Pts',(-0.746235637830062,-5.33465364878775,
14.7695937714346));
#55439=CARTESIAN_POINT('Ctrl Pts',(4.06663348316603,-3.53240559608313,14.9278840940153));
#55440=CARTESIAN_POINT('Ctrl Pts',(5.17777352115031,1.48528062718241,15.0861744165959));
#55441=CARTESIAN_POINT('Ctrl Pts',(1.57574850461626,5.15096241772943,15.2444647391765));
#55442=CARTESIAN_POINT('Ctrl Pts',(-3.46063102098561,4.12788446150094,15.4027550617572));
#55443=CARTESIAN_POINT('Ctrl Pts',(-5.34690652055963,-0.652677426204677,
15.5610453843378));
#55444=CARTESIAN_POINT('Ctrl Pts',(-2.36606049931089,-4.83912749271637,
15.7193357069185));
#55445=CARTESIAN_POINT('Ctrl Pts',(2.76853629551539,-4.62067138316371,15.8776260294991));
#55446=CARTESIAN_POINT('Ctrl Pts',(5.3830211950772,-0.196162831342301,16.0359163520798));
#55447=CARTESIAN_POINT('Ctrl Pts',(3.09751055443537,4.406906576266,16.1942066746604));
#55448=CARTESIAN_POINT('Ctrl Pts',(-2.00756700604201,4.99850701120068,16.3524969972411));
#55449=CARTESIAN_POINT('Ctrl Pts',(-5.28521904248542,1.04012298730266,16.5107873198217));
#55450=CARTESIAN_POINT('Ctrl Pts',(-3.75190203767367,-3.86505223614748,
16.6690776424023));
#55451=CARTESIAN_POINT('Ctrl Pts',(1.19665445944501,-5.25199180962336,16.827367964983));
#55452=CARTESIAN_POINT('Ctrl Pts',(5.05593276337192,-1.85820709934824,16.9856582875636));
#55453=CARTESIAN_POINT('Ctrl Pts',(4.31295598018285,3.22704409670023,17.1439486101443));
#55454=CARTESIAN_POINT('Ctrl Pts',(-0.355973635386551,5.37482048772419,
17.3022389327249));
#55455=CARTESIAN_POINT('Ctrl Pts',(-4.70086377034365,2.63006163593618,17.4605292553056));
#55456=CARTESIAN_POINT('Ctrl Pts',(-4.76671982630963,-2.50875132983212,
17.6188195778862));
#55457=CARTESIAN_POINT('Ctrl Pts',(-0.493551516935001,-5.36394300504465,
17.7771099004669));
#55458=CARTESIAN_POINT('Ctrl Pts',(4.22882658272939,-3.33647390152326,17.9354002230475));
#55459=CARTESIAN_POINT('Ctrl Pts',(5.10194085814736,1.72802272375016,18.0936905456282));
#55460=CARTESIAN_POINT('Ctrl Pts',(1.3307183071549,5.21966939828879,18.2519808682088));
#55461=CARTESIAN_POINT('Ctrl Pts',(-3.65143336771916,3.95979466293823,18.4102711907895));
#55462=CARTESIAN_POINT('Ctrl Pts',(-5.31053001253145,-0.904136851324141,
18.5685615133701));
#55463=CARTESIAN_POINT('Ctrl Pts',(-2.13422101028107,-4.94586439271395,
18.7268518359507));
#55464=CARTESIAN_POINT('Ctrl Pts',(2.98213020961523,-4.48398969368682,18.8851421585314));
#55465=CARTESIAN_POINT('Ctrl Pts',(5.3890746734895,0.056574848876316,19.043432481112));
#55466=CARTESIAN_POINT('Ctrl Pts',(2.88048207978671,4.55134095987183,19.2017228036927));
#55467=CARTESIAN_POINT('Ctrl Pts',(-1.3774178436033,4.83495951916122,19.3336314058432));
#55468=CARTESIAN_POINT('Ctrl Pts',(-3.79805473803742,2.8466873735715,19.4391582875636));
#55469=CARTESIAN_POINT('Ctrl Pts',(-4.40190912913332,1.41664485531417,19.4919217284239));
#55470=CARTESIAN_POINT('Ctrl Pts',(-4.51273837831629,0.668607754121397,
19.518303448854));
#55471=CARTESIAN_POINT('Ctrl Pts',(2.53835875722687,-3.55965150255045,-1.94289029309402E-15));
#55472=CARTESIAN_POINT('Ctrl Pts',(3.1284109977952,-3.13889001199587,0.0263817204301056));
#55473=CARTESIAN_POINT('Ctrl Pts',(4.08550837253979,-1.9999918568306,0.0791451612903207));
#55474=CARTESIAN_POINT('Ctrl Pts',(4.72679975347169,0.932772746710439,0.184672043010751));
#55475=CARTESIAN_POINT('Ctrl Pts',(2.62811439332184,4.44281702219704,0.316580645161289));
#55476=CARTESIAN_POINT('Ctrl Pts',(-2.3016075840404,4.62373529115294,0.474870967741933));
#55477=CARTESIAN_POINT('Ctrl Pts',(-5.12700989483103,0.589736901013719,
0.633161290322578));
#55478=CARTESIAN_POINT('Ctrl Pts',(-3.29020762976984,-3.97798440336088,
0.791451612903224));
#55479=CARTESIAN_POINT('Ctrl Pts',(1.54404435335689,-4.92628156041988,0.949741935483869));
#55480=CARTESIAN_POINT('Ctrl Pts',(4.97150648183897,-1.38949747849925,1.10803225806451));
#55481=CARTESIAN_POINT('Ctrl Pts',(3.87423912778238,3.41166257284768,1.26632258064516));
#55482=CARTESIAN_POINT('Ctrl Pts',(-0.749980974679123,5.10752324154442,
1.42461290322581));
#55483=CARTESIAN_POINT('Ctrl Pts',(-4.69133158596208,2.15404506392038,1.58290322580645));
#55484=CARTESIAN_POINT('Ctrl Pts',(-4.36240693472153,-2.76012987050762,
1.7411935483871));
#55485=CARTESIAN_POINT('Ctrl Pts',(-0.0624691826164238,-5.16187799225891,
1.89948387096774));
#55486=CARTESIAN_POINT('Ctrl Pts',(4.29430578210828,-2.8649130214088,2.05777419354839));
#55487=CARTESIAN_POINT('Ctrl Pts',(4.74212257914569,2.03988351823947,2.21606451612903));
#55488=CARTESIAN_POINT('Ctrl Pts',(0.873326467994359,5.08784270323556,2.37435483870968));
#55489=CARTESIAN_POINT('Ctrl Pts',(-3.7904275745029,3.50449557153541,2.53264516129032));
#55490=CARTESIAN_POINT('Ctrl Pts',(-5.00387610832461,-1.26888281826166,
2.69093548387097));
#55491=CARTESIAN_POINT('Ctrl Pts',(-1.66245191543707,-4.88723759858308,
2.84922580645161));
#55492=CARTESIAN_POINT('Ctrl Pts',(3.19224964022283,-4.05689272016998,3.00751612903226));
#55493=CARTESIAN_POINT('Ctrl Pts',(5.14114662208426,0.466314344506177,3.1658064516129));
#55494=CARTESIAN_POINT('Ctrl Pts',(2.41021871871718,4.56505016420442,3.32409677419355));
#55495=CARTESIAN_POINT('Ctrl Pts',(-2.5146557123555,4.50836375769575,3.48238709677419));
#55496=CARTESIAN_POINT('Ctrl Pts',(-5.15051785452657,0.347855062304423,
3.64067741935484));
#55497=CARTESIAN_POINT('Ctrl Pts',(-3.09802489959102,-4.12929521444937,
3.79896774193548));
#55498=CARTESIAN_POINT('Ctrl Pts',(1.77450307237079,-4.84767739015689,3.95725806451612));
#55499=CARTESIAN_POINT('Ctrl Pts',(5.03175648528012,-1.15337068283656,4.11554838709677));
#55500=CARTESIAN_POINT('Ctrl Pts',(3.7087595738537,3.5908132325819,4.27383870967742));
#55501=CARTESIAN_POINT('Ctrl Pts',(-0.990205008382098,5.06639233464293,
4.43212903225806));
#55502=CARTESIAN_POINT('Ctrl Pts',(-4.7878169880326,1.93019318716672,4.59041935483871));
#55503=CARTESIAN_POINT('Ctrl Pts',(-4.22722912950617,-2.96300036036751,
4.74870967741935));
#55504=CARTESIAN_POINT('Ctrl Pts',(0.181272997936893,-5.15906748833169,
4.907));
#55505=CARTESIAN_POINT('Ctrl Pts',(4.4247679934035,-2.65899707670991,5.06529032258064));
#55506=CARTESIAN_POINT('Ctrl Pts',(4.64053527927078,2.26147508740778,5.22358064516129));
#55507=CARTESIAN_POINT('Ctrl Pts',(0.63216865368283,5.12339731452249,5.38187096774192));
#55508=CARTESIAN_POINT('Ctrl Pts',(-3.95164129625807,3.32165144392371,5.54016129032259));
#55509=CARTESIAN_POINT('Ctrl Pts',(-4.93839594954698,-1.50368969361007,
5.69845161290321));
#55510=CARTESIAN_POINT('Ctrl Pts',(-1.42988345294528,-4.96026920238937,
5.85674193548387));
#55511=CARTESIAN_POINT('Ctrl Pts',(3.38020716333018,-3.90167102433782,6.01503225806451));
#55512=CARTESIAN_POINT('Ctrl Pts',(5.11340107541181,0.708496077023162,6.17332258064516));
#55513=CARTESIAN_POINT('Ctrl Pts',(2.19202615312461,4.67374139134797,6.3316129032258));
#55514=CARTESIAN_POINT('Ctrl Pts',(-2.72468151658193,4.38462631046011,6.48990322580645));
#55515=CARTESIAN_POINT('Ctrl Pts',(-5.16119694561929,0.104323236680228,
6.64819354838708));
#55516=CARTESIAN_POINT('Ctrl Pts',(-2.8996364567242,-4.27094201178353,6.80648387096775));
#55517=CARTESIAN_POINT('Ctrl Pts',(2.00137227482285,-4.75850252356265,6.96477419354837));
#55518=CARTESIAN_POINT('Ctrl Pts',(5.08059451261016,-0.914547236405604,
7.12306451612904));
#55519=CARTESIAN_POINT('Ctrl Pts',(3.53511070256229,3.76189175413264,7.28135483870967));
#55520=CARTESIAN_POINT('Ctrl Pts',(-1.22827365147281,5.01399851279189,7.43964516129032));
#55521=CARTESIAN_POINT('Ctrl Pts',(-4.87359897319111,1.70201947629637,7.59793548387097));
#55522=CARTESIAN_POINT('Ctrl Pts',(-4.08263980298667,-3.1592545779425,7.75622580645161));
#55523=CARTESIAN_POINT('Ctrl Pts',(0.424618501333285,-5.14475814567673,
7.91451612903225));
#55524=CARTESIAN_POINT('Ctrl Pts',(4.54535988400859,-2.44714952016159,8.0728064516129));
#55525=CARTESIAN_POINT('Ctrl Pts',(4.52860253637045,2.47802266268103,8.23109677419354));
#55526=CARTESIAN_POINT('Ctrl Pts',(0.389600147091602,5.14752843358518,8.38938709677419));
#55527=CARTESIAN_POINT('Ctrl Pts',(-4.10404305282859,3.13140030492926,8.54767741935484));
#55528=CARTESIAN_POINT('Ctrl Pts',(-4.86190441070575,-1.73514343797319,
8.70596774193548));
#55529=CARTESIAN_POINT('Ctrl Pts',(-1.19412647058753,-5.02224045834365,
8.86425806451613));
#55530=CARTESIAN_POINT('Ctrl Pts',(3.56062739266322,-3.73774929868204,9.02254838709676));
#55531=CARTESIAN_POINT('Ctrl Pts',(5.07425366817473,0.949097971864315,9.18083870967742));
#55532=CARTESIAN_POINT('Ctrl Pts',(1.96894576792944,4.77201108675727,9.33912903225805));
#55533=CARTESIAN_POINT('Ctrl Pts',(-2.9286317925302,4.25111198076021,9.4974193548387));
#55534=CARTESIAN_POINT('Ctrl Pts',(-5.16036756436058,-0.139441205807441,
9.65570967741936));
#55535=CARTESIAN_POINT('Ctrl Pts',(-2.69478237803987,-4.40306543037773,
9.81399999999999));
#55536=CARTESIAN_POINT('Ctrl Pts',(2.22377879965116,-4.65871710875468,9.97229032258064));
#55537=CARTESIAN_POINT('Ctrl Pts',(5.11810379036282,-0.67368452576514,10.1305806451613));
#55538=CARTESIAN_POINT('Ctrl Pts',(3.35357921258595,3.92458197953528,10.2888709677419));
#55539=CARTESIAN_POINT('Ctrl Pts',(-1.46360347987537,4.95042443663959,10.4471612903226));
#55540=CARTESIAN_POINT('Ctrl Pts',(-4.94851376834693,1.47005058881065,10.6054516129032));
#55541=CARTESIAN_POINT('Ctrl Pts',(-3.92894697338513,-3.34846426433215,
10.7637419354839));
#55542=CARTESIAN_POINT('Ctrl Pts',(0.667017186951725,-5.11897697997292,
10.9220322580645));
#55543=CARTESIAN_POINT('Ctrl Pts',(4.65581649466175,-2.22984528997355,11.0803225806452));
#55544=CARTESIAN_POINT('Ctrl Pts',(4.40657187915952,2.68904472312794,11.2386129032258));
#55545=CARTESIAN_POINT('Ctrl Pts',(0.14616290696869,5.16018155240764,11.3969032258064));
#55546=CARTESIAN_POINT('Ctrl Pts',(-4.24729358124599,2.93416674439068,11.5551935483871));
#55547=CARTESIAN_POINT('Ctrl Pts',(-4.77457175836603,-1.96272814556555,
11.7134838709677));
#55548=CARTESIAN_POINT('Ctrl Pts',(-0.955706815437237,-5.07301308219371,
11.8717741935484));
#55549=CARTESIAN_POINT('Ctrl Pts',(3.73310810644377,-3.5654931096253,12.030064516129));
#55550=CARTESIAN_POINT('Ctrl Pts',(5.02379164936073,1.1875835604264,12.1883548387097));
#55551=CARTESIAN_POINT('Ctrl Pts',(1.74147501164997,4.85964011352491,12.3466451612903));
#55552=CARTESIAN_POINT('Ctrl Pts',(-3.12605178178994,4.10811848742822,12.504935483871));
#55553=CARTESIAN_POINT('Ctrl Pts',(-5.14803155406786,-0.382894721174656,
12.6632258064516));
#55554=CARTESIAN_POINT('Ctrl Pts',(-2.4839194519693,-4.5253708583176,12.8215161290323));
#55555=CARTESIAN_POINT('Ctrl Pts',(2.44122672465452,-4.54854364912704,12.9798064516129));
#55556=CARTESIAN_POINT('Ctrl Pts',(5.14420067918421,-0.431319627959304,
13.1380967741936));
#55557=CARTESIAN_POINT('Ctrl Pts',(3.16456988475122,4.07852114052473,13.2963870967742));
#55558=CARTESIAN_POINT('Ctrl Pts',(-1.69566975348524,4.87581186432528,13.4546774193548));
#55559=CARTESIAN_POINT('Ctrl Pts',(-5.01239432776474,1.23480377071736,13.6129677419355));
#55560=CARTESIAN_POINT('Ctrl Pts',(-3.76649334627126,-3.53020751821668,
13.7712580645161));
#55561=CARTESIAN_POINT('Ctrl Pts',(0.907928552289056,-5.08178147829179,
13.9295483870968));
#55562=CARTESIAN_POINT('Ctrl Pts',(4.75589152831045,-2.00756893285326,14.0878387096774));
#55563=CARTESIAN_POINT('Ctrl Pts',(4.2747154125816,2.89407073006048,14.2461290322581));
#55564=CARTESIAN_POINT('Ctrl Pts',(-0.0976002483683332,5.16132845696157,
14.4044193548387));
#55565=CARTESIAN_POINT('Ctrl Pts',(-4.38107346034753,2.73039055529394,14.5627096774194));
#55566=CARTESIAN_POINT('Ctrl Pts',(-4.67659272754351,-2.18593634619795,
14.721));
#55567=CARTESIAN_POINT('Ctrl Pts',(-0.715156117622299,-5.11247386069707,
14.8792903225806));
#55568=CARTESIAN_POINT('Ctrl Pts',(3.89726470591888,-3.38528655547465,15.0375806451613));
#55569=CARTESIAN_POINT('Ctrl Pts',(4.96212753934002,1.42342106576975,15.1958709677419));
#55570=CARTESIAN_POINT('Ctrl Pts',(1.5101211008729,4.93643307547415,15.3541612903226));
#55571=CARTESIAN_POINT('Ctrl Pts',(-3.31650127657807,3.95596467901843,15.5124516129032));
#55572=CARTESIAN_POINT('Ctrl Pts',(-5.1242164199664,-0.62549445580161,15.6707419354839));
#55573=CARTESIAN_POINT('Ctrl Pts',(-2.26751786562628,-4.63758557609733,
15.8290322580645));
#55574=CARTESIAN_POINT('Ctrl Pts',(2.65323118895075,-4.42822781393943,15.9873225806452));
#55575=CARTESIAN_POINT('Ctrl Pts',(5.15882697608013,-0.187992963311806,
16.1456129032258));
#55576=CARTESIAN_POINT('Ctrl Pts',(2.96850419640318,4.22336596918787,16.3039032258064));
#55577=CARTESIAN_POINT('Ctrl Pts',(-1.92395505269964,4.79032719267193,16.4621935483871));
#55578=CARTESIAN_POINT('Ctrl Pts',(-5.06509812664321,0.99680352926066,16.6204838709677));
#55579=CARTESIAN_POINT('Ctrl Pts',(-3.59564132150574,-3.70407899527331,
16.7787741935484));
#55580=CARTESIAN_POINT('Ctrl Pts',(1.14681571606612,-5.03325475486043,16.937064516129));
#55581=CARTESIAN_POINT('Ctrl Pts',(4.84536125415653,-1.78081574711759,17.0953548387097));
#55582=CARTESIAN_POINT('Ctrl Pts',(4.13332826509411,3.09264287390914,17.2536451612903));
#55583=CARTESIAN_POINT('Ctrl Pts',(-0.341147903092961,5.15096781506579,
17.411935483871));
#55584=CARTESIAN_POINT('Ctrl Pts',(-4.50508031651524,2.52052377735926,17.5702258064516));
#55585=CARTESIAN_POINT('Ctrl Pts',(-4.56819357313145,-2.40426585138671,
17.7285161290323));
#55586=CARTESIAN_POINT('Ctrl Pts',(-0.472995886023615,-5.14054336213398,
17.8868064516129));
#55587=CARTESIAN_POINT('Ctrl Pts',(4.05270272242283,-3.19751510246813,18.0450967741935));
#55588=CARTESIAN_POINT('Ctrl Pts',(4.88945318540557,1.65605334244537,18.2033870967742));
#55589=CARTESIAN_POINT('Ctrl Pts',(1.27529601904452,5.00227852023644,18.3616774193548));
#55590=CARTESIAN_POINT('Ctrl Pts',(-3.49935701088739,3.79487555159269,18.5199677419355));
#55591=CARTESIAN_POINT('Ctrl Pts',(-5.0893549352888,-0.866480998244023,
18.6782580645161));
#55592=CARTESIAN_POINT('Ctrl Pts',(-2.04533412033072,-4.73987705500777,
18.8365483870968));
#55593=CARTESIAN_POINT('Ctrl Pts',(2.85792925831606,-4.29723869811459,18.9948387096774));
#55594=CARTESIAN_POINT('Ctrl Pts',(5.16462833680317,0.0542185969503185,
19.1531290322581));
#55595=CARTESIAN_POINT('Ctrl Pts',(2.76051461044002,4.36178489183685,19.3114193548387));
#55596=CARTESIAN_POINT('Ctrl Pts',(-1.32005059452733,4.63359119197125,19.4433279569892));
#55597=CARTESIAN_POINT('Ctrl Pts',(-3.63987183575178,2.72812739966123,19.5488548387097));
#55598=CARTESIAN_POINT('Ctrl Pts',(-4.21857665773145,1.35764386397051,19.6016182795699));
#55599=CARTESIAN_POINT('Ctrl Pts',(-4.32479004603219,0.640761311051878,
19.628));
#55600=CARTESIAN_POINT('',(2.53835875722687,-3.55965150255045,0.));
#55601=CARTESIAN_POINT('Ctrl Pts',(2.53835875722687,-3.55965150255045,-1.94289029309402E-15));
#55602=CARTESIAN_POINT('Ctrl Pts',(3.1284109977952,-3.13889001199587,0.0263817204301056));
#55603=CARTESIAN_POINT('Ctrl Pts',(4.08550837253979,-1.9999918568306,0.0791451612903207));
#55604=CARTESIAN_POINT('Ctrl Pts',(4.72679975347169,0.932772746710439,0.184672043010751));
#55605=CARTESIAN_POINT('Ctrl Pts',(2.62811439332184,4.44281702219704,0.316580645161289));
#55606=CARTESIAN_POINT('Ctrl Pts',(-2.3016075840404,4.62373529115294,0.474870967741933));
#55607=CARTESIAN_POINT('Ctrl Pts',(-4.29378651801925,1.77938049543143,0.58648078871983));
#55608=CARTESIAN_POINT('Ctrl Pts',(-4.37763907935493,0.169045277724475,
0.645327168837512));
#55609=CARTESIAN_POINT('Ctrl Pts',(-4.37640441740291,0.00246357316762608,
0.651410108094978));
#55610=CARTESIAN_POINT('Ctrl Pts',(2.17571852337094,4.44456444733847,4.16333634234434E-17));
#55611=CARTESIAN_POINT('Ctrl Pts',(2.288553758881,4.38223977042994,4.80899030934479E-17));
#55612=CARTESIAN_POINT('Ctrl Pts',(2.39856816217823,4.31535914976362,1.26999648448827E-16));
#55613=CARTESIAN_POINT('Ctrl Pts',(2.50544378309707,4.24391302988421,1.37043154602168E-16));
#55614=CARTESIAN_POINT('Ctrl Pts',(2.62554044419194,4.16362867343386,1.45788230031228E-16));
#55615=CARTESIAN_POINT('Ctrl Pts',(2.7416747038151,4.07757963945051,2.86902645733316E-16));
#55616=CARTESIAN_POINT('Ctrl Pts',(2.85366454038282,3.98618686426695,3.64291929955129E-16));
#55617=CARTESIAN_POINT('Ctrl Pts',(2.9232629976869,3.92938888726778,4.12387140724083E-16));
#55618=CARTESIAN_POINT('Ctrl Pts',(2.99126006746036,3.87052620415169,6.62527936102846E-16));
#55619=CARTESIAN_POINT('Ctrl Pts',(3.05760444128136,3.80969336998723,7.21644966006352E-16));
#55620=CARTESIAN_POINT('Ctrl Pts',(3.09753791324214,3.7730773596537,7.57228213237312E-16));
#55621=CARTESIAN_POINT('Ctrl Pts',(3.13687250045182,3.73574748028041,-2.48343235400226E-16));
#55622=CARTESIAN_POINT('Ctrl Pts',(3.17559590361344,3.69772367591327,-3.60822483003176E-16));
#55623=CARTESIAN_POINT('Ctrl Pts',(3.19355313598542,3.68009086900739,-4.12982567637309E-16));
#55624=CARTESIAN_POINT('Ctrl Pts',(3.21137384475144,3.66231375739153,2.85386760819859E-16));
#55625=CARTESIAN_POINT('Ctrl Pts',(3.22905135321198,3.64440041383412,2.77555756156289E-16));
#55626=CARTESIAN_POINT('Ctrl Pts',(3.33032953777236,3.54177108012739,2.32690274271181E-16));
#55627=CARTESIAN_POINT('Ctrl Pts',(3.42697009782031,3.4346145361773,1.17947475774344E-16));
#55628=CARTESIAN_POINT('Ctrl Pts',(3.51879473621821,3.32334962039163,1.38777878078145E-16));
#55629=CARTESIAN_POINT('Ctrl Pts',(3.60865605635445,3.21446367875555,1.59162901995989E-16));
#55630=CARTESIAN_POINT('Ctrl Pts',(3.69390536375717,3.10164237133953,1.64416256607793E-16));
#55631=CARTESIAN_POINT('Ctrl Pts',(3.77433601631748,2.9852523894932,1.52655665885959E-16));
#55632=CARTESIAN_POINT('Ctrl Pts',(3.80952442681261,2.93433177243543,1.47510407445157E-16));
#55633=CARTESIAN_POINT('Ctrl Pts',(3.84378998451378,2.88272782098782,-1.03604202083645E-16));
#55634=CARTESIAN_POINT('Ctrl Pts',(3.87711279910771,2.83047021492504,-1.52655665885959E-16));
#55635=CARTESIAN_POINT('Ctrl Pts',(3.90167945166607,2.79194422402902,-1.88817985407716E-16));
#55636=CARTESIAN_POINT('Ctrl Pts',(3.92573367987553,2.75306295204808,1.37038491228682E-16));
#55637=CARTESIAN_POINT('Ctrl Pts',(3.94926693181774,2.71383814709955,1.2490009027033E-16));
#55638=CARTESIAN_POINT('Ctrl Pts',(3.95979885299727,2.69628372856808,1.19467747878689E-16));
#55639=CARTESIAN_POINT('Ctrl Pts',(3.97022193097802,2.67866796640904,3.81603872600368E-16));
#55640=CARTESIAN_POINT('Ctrl Pts',(3.98053410416003,2.66099477842828,3.7470027081099E-16));
#55641=CARTESIAN_POINT('Ctrl Pts',(4.05311436653015,2.53660541859884,3.26110587499023E-16));
#55642=CARTESIAN_POINT('Ctrl Pts',(4.12023044721824,2.40933003202768,5.80264781591426E-16));
#55643=CARTESIAN_POINT('Ctrl Pts',(4.1817056161975,2.27957303631144,5.41233724504764E-16));
#55644=CARTESIAN_POINT('Ctrl Pts',(4.24306352883745,2.15006353613803,5.02277114368784E-16));
#55645=CARTESIAN_POINT('Ctrl Pts',(4.29880233786649,2.01808110524174,-2.01806554237873E-16));
#55646=CARTESIAN_POINT('Ctrl Pts',(4.34869895497134,1.88400727320529,-2.08166817117217E-16));
#55647=CARTESIAN_POINT('Ctrl Pts',(4.3987130094648,1.74961788308838,-2.14542049601851E-16));
#55648=CARTESIAN_POINT('Ctrl Pts',(4.44285769397013,1.61312648052743,2.07700331834603E-16));
#55649=CARTESIAN_POINT('Ctrl Pts',(4.48085566800584,1.47490808725521,2.22044604925031E-16));
#55650=CARTESIAN_POINT('Ctrl Pts',(4.50935414853263,1.37124429230104,2.32802809742852E-16));
#55651=CARTESIAN_POINT('Ctrl Pts',(4.53439405643066,1.26660880723853,3.27090126933202E-16));
#55652=CARTESIAN_POINT('Ctrl Pts',(4.55583718119808,1.16116031586893,3.33066907387547E-16));
#55653=CARTESIAN_POINT('Ctrl Pts',(4.5647459632839,1.1173505800641,3.35550026579367E-16));
#55654=CARTESIAN_POINT('Ctrl Pts',(4.57303368750873,1.073400536371,3.93488937669688E-16));
#55655=CARTESIAN_POINT('Ctrl Pts',(4.58068946156208,1.02932171064127,4.16333634234434E-16));
#55656=CARTESIAN_POINT('Ctrl Pts',(4.58528213032192,1.00287899635937,4.3003807790138E-16));
#55657=CARTESIAN_POINT('Ctrl Pts',(4.58964820129846,0.976383975558462,1.1911498064296E-16));
#55658=CARTESIAN_POINT('Ctrl Pts',(4.59378028021791,0.949872636571533,1.38777878078145E-16));
#55659=CARTESIAN_POINT('Ctrl Pts',(4.61514939077547,0.812768833647209,2.40464858739661E-16));
#55660=CARTESIAN_POINT('Ctrl Pts',(4.63029132458926,0.675091193156248,-6.4053354410212E-17));
#55661=CARTESIAN_POINT('Ctrl Pts',(4.63900152451931,0.537186451104229,-1.38777878078145E-16));
#55662=CARTESIAN_POINT('Ctrl Pts',(4.64607280433788,0.42523000611001,-1.99442159083017E-16));
#55663=CARTESIAN_POINT('Ctrl Pts',(4.64890419840177,0.313123505052828,4.93108554065338E-16));
#55664=CARTESIAN_POINT('Ctrl Pts',(4.64736094433393,0.20105139156818,4.71844785465692E-16));
#55665=CARTESIAN_POINT('Ctrl Pts',(4.64544832051237,0.0621554064876461,
4.17736069944506E-16));
#55666=CARTESIAN_POINT('Ctrl Pts',(4.63681759992347,-0.0766885915146454,
3.72153370275118E-16));
#55667=CARTESIAN_POINT('Ctrl Pts',(4.62166663169142,-0.215038242011895,
4.16333634234434E-16));
#55668=CARTESIAN_POINT('Ctrl Pts',(4.60648817669052,-0.353638885370275,
4.605940496854E-16));
#55669=CARTESIAN_POINT('Ctrl Pts',(4.58476541728463,-0.491744202092864,
1.3585326957315E-16));
#55670=CARTESIAN_POINT('Ctrl Pts',(4.55664910490708,-0.628889846984247,
2.22044604925031E-16));
#55671=CARTESIAN_POINT('Ctrl Pts',(4.54627797904168,-0.679478086507271,
2.53837578891091E-16));
#55672=CARTESIAN_POINT('Ctrl Pts',(4.53503649423606,-0.729935498537829,
-4.17628381648536E-17));
#55673=CARTESIAN_POINT('Ctrl Pts',(4.52293072203927,-0.780237766000663,
-5.55111512312578E-17));
#55674=CARTESIAN_POINT('Ctrl Pts',(4.51852089045776,-0.798561630358381,
-6.05193195799785E-17));
#55675=CARTESIAN_POINT('Ctrl Pts',(4.51399616118864,-0.816865466942453,
-2.76721061431502E-16));
#55676=CARTESIAN_POINT('Ctrl Pts',(4.50936083932464,-0.835132869996713,
-2.77555756156289E-16));
#55677=CARTESIAN_POINT('Ctrl Pts',(4.47555258032973,-0.968368298245966,
-2.83643699187054E-16));
#55678=CARTESIAN_POINT('Ctrl Pts',(4.43581935723855,-1.09986196998026,4.56182438062644E-17));
#55679=CARTESIAN_POINT('Ctrl Pts',(4.39038959840621,-1.229200829575,5.55111512312578E-17));
#55680=CARTESIAN_POINT('Ctrl Pts',(4.34480983538931,-1.35896675219327,6.54367239740816E-17));
#55681=CARTESIAN_POINT('Ctrl Pts',(4.29349546516567,-1.48656440482432,-4.64120495657098E-16));
#55682=CARTESIAN_POINT('Ctrl Pts',(4.23662839209755,-1.61155805192221,-3.05311331771918E-16));
#55683=CARTESIAN_POINT('Ctrl Pts',(4.17976131902944,-1.7365516990201,-1.46502167886738E-16));
#55684=CARTESIAN_POINT('Ctrl Pts',(4.11734114389621,-1.85894212089202,1.98375931461375E-16));
#55685=CARTESIAN_POINT('Ctrl Pts',(4.04950702451708,-1.97826322671605,2.22044604925031E-16));
#55686=CARTESIAN_POINT('Ctrl Pts',(4.0039219578893,-2.05844795689127,2.37950141352824E-16));
#55687=CARTESIAN_POINT('Ctrl Pts',(3.95589106826036,-2.13724588577774,1.34209299017938E-16));
#55688=CARTESIAN_POINT('Ctrl Pts',(3.90547300064698,-2.21455451296583,1.66533453693773E-16));
#55689=CARTESIAN_POINT('Ctrl Pts',(3.88226355505238,-2.25014275467462,1.81413550152313E-16));
#55690=CARTESIAN_POINT('Ctrl Pts',(3.85854814303777,-2.28541527809141,-1.96535868138964E-16));
#55691=CARTESIAN_POINT('Ctrl Pts',(3.8343320388377,-2.32036145673223,-2.22044604925031E-16));
#55692=CARTESIAN_POINT('Ctrl Pts',(3.81846869581275,-2.34325379377416,-2.38754718097135E-16));
#55693=CARTESIAN_POINT('Ctrl Pts',(3.80239048915502,-2.36600608076709,-1.28420314193019E-17));
#55694=CARTESIAN_POINT('Ctrl Pts',(3.78609884210449,-2.38861523157554,0.));
#55695=CARTESIAN_POINT('Ctrl Pts',(3.77490538198125,-2.40414924279059,8.82334156561408E-18));
#55696=CARTESIAN_POINT('Ctrl Pts',(3.76361599384939,-2.41960894071961,1.65364095173029E-16));
#55697=CARTESIAN_POINT('Ctrl Pts',(3.7522346949218,-2.43498912758705,1.66533453693773E-16));
#55698=CARTESIAN_POINT('Ctrl Pts',(3.66941253061457,-2.54691135824948,1.75042922090602E-16));
#55699=CARTESIAN_POINT('Ctrl Pts',(3.58167249725696,-2.65470179052059,3.28026165867355E-16));
#55700=CARTESIAN_POINT('Ctrl Pts',(3.48928766288614,-2.75807107487432,2.22044604925031E-16));
#55701=CARTESIAN_POINT('Ctrl Pts',(3.39991887248819,-2.85806571111424,1.19522973854221E-16));
#55702=CARTESIAN_POINT('Ctrl Pts',(3.30620285470906,-2.9539234934181,-1.0442180859248E-16));
#55703=CARTESIAN_POINT('Ctrl Pts',(3.20834980062004,-3.04534562649001,-1.66533453693773E-16));
#55704=CARTESIAN_POINT('Ctrl Pts',(3.11144260907094,-3.13588405928502,-2.28044718163707E-16));
#55705=CARTESIAN_POINT('Ctrl Pts',(3.01047744826623,-3.22207261031851,3.41219002678743E-16));
#55706=CARTESIAN_POINT('Ctrl Pts',(2.90563068007557,-3.30357847782834,3.33066907387547E-16));
#55707=CARTESIAN_POINT('Ctrl Pts',(2.80291415997029,-3.38342833131688,3.25080444148589E-16));
#55708=CARTESIAN_POINT('Ctrl Pts',(2.69647166403099,-3.45878415557578,1.92670969748543E-16));
#55709=CARTESIAN_POINT('Ctrl Pts',(2.58644978075874,-3.52928668450907,1.66533453693773E-16));
#55710=CARTESIAN_POINT('Ctrl Pts',(2.57049460076127,-3.53951083724989,1.62743037088118E-16));
#55711=CARTESIAN_POINT('Ctrl Pts',(2.5544641189252,-3.54963283815124,3.31276988434876E-16));
#55712=CARTESIAN_POINT('Ctrl Pts',(2.53835875722692,-3.55965150255041,3.33066907387547E-16));
#55713=CARTESIAN_POINT('Ctrl Pts',(0.446494146901359,4.91265885279923,19.058));
#55714=CARTESIAN_POINT('Ctrl Pts',(1.22846295052447,4.84360722676543,19.0327765671335));
#55715=CARTESIAN_POINT('Ctrl Pts',(1.9933030120195,4.59769822736177,19.0075531342671));
#55716=CARTESIAN_POINT('Ctrl Pts',(2.65082820116331,4.18037408759279,18.9823297014006));
#55717=CARTESIAN_POINT('Ctrl Pts',(4.02626712794074,3.307397848204,18.9295662605404));
#55718=CARTESIAN_POINT('Ctrl Pts',(4.93211723740144,1.68434260046616,18.8768028196802));
#55719=CARTESIAN_POINT('Ctrl Pts',(4.95046975302369,0.05301847033729,18.82403937882));
#55720=CARTESIAN_POINT('Ctrl Pts',(4.96882226864594,-1.57830565979157,18.7712759379598));
#55721=CARTESIAN_POINT('Ctrl Pts',(4.09967719042974,-3.21789867231146,18.7185124970995));
#55722=CARTESIAN_POINT('Ctrl Pts',(2.74135016758908,-4.12108640912056,18.6657490562393));
#55723=CARTESIAN_POINT('Ctrl Pts',(1.38302314474846,-5.02427414592964,18.6129856153791));
#55724=CARTESIAN_POINT('Ctrl Pts',(-0.464485822716606,-5.19105660702797,
18.5602221745189));
#55725=CARTESIAN_POINT('Ctrl Pts',(-1.9617212025883,-4.54471608580352,18.5074587336587));
#55726=CARTESIAN_POINT('Ctrl Pts',(-3.45895658246008,-3.89837556457903,
18.4546952927985));
#55727=CARTESIAN_POINT('Ctrl Pts',(-4.60591837473846,-2.43891206103166,
18.4019318519383));
#55728=CARTESIAN_POINT('Ctrl Pts',(-4.87985025660527,-0.831000068739,18.349168411078));
#55729=CARTESIAN_POINT('Ctrl Pts',(-4.92631242249651,-0.558278714746532,
18.340219092271));
#55730=CARTESIAN_POINT('Ctrl Pts',(-4.94765902855038,-0.28128675460715,
18.3312697734639));
#55731=CARTESIAN_POINT('Ctrl Pts',(-4.94522242777803,-0.0039236424385497,
18.3223204546569));
#55732=CARTESIAN_POINT('Origin',(0.,0.,-1.84858989190501));
#55733=CARTESIAN_POINT('',(-2.53835875722683,-3.55965150255047,0.));
#55734=CARTESIAN_POINT('Ctrl Pts',(-2.54467524200888,-3.56229978442276,
-3.12521276218947E-15));
#55735=CARTESIAN_POINT('Ctrl Pts',(-1.45608504857279,-4.32913804450291,
0.0486930492780809));
#55736=CARTESIAN_POINT('Ctrl Pts',(1.60942354292801,-4.84594693373762,0.150182632030869));
#55737=CARTESIAN_POINT('Ctrl Pts',(4.96501177239675,-1.41203703483287,0.304468748258361));
#55738=CARTESIAN_POINT('Ctrl Pts',(3.88934922870828,3.39617009289883,0.462858348682473));
#55739=CARTESIAN_POINT('Ctrl Pts',(-0.732920742143878,5.1113964007393,0.621247949106584));
#55740=CARTESIAN_POINT('Ctrl Pts',(-3.9420462167219,2.72159457156631,0.749825130180767));
#55741=CARTESIAN_POINT('Ctrl Pts',(-4.36729319104836,0.635050406119092,
0.825605777780246));
#55742=CARTESIAN_POINT('Ctrl Pts',(-4.36535621882271,0.0014563306878905,
0.848589891905021));
#55743=CARTESIAN_POINT('Origin',(0.,0.,0.));
#55744=CARTESIAN_POINT('Ctrl Pts',(-1.91898364244012,3.92834389788461,-0.329089653438086));
#55745=CARTESIAN_POINT('Ctrl Pts',(-2.57055919540632,3.61005128897394,-0.302691386700734));
#55746=CARTESIAN_POINT('Ctrl Pts',(-3.7023655534584,2.64307614504004,-0.24989485322603));
#55747=CARTESIAN_POINT('Ctrl Pts',(-4.81630944128875,-0.146849281373132,
-0.144301786276623));
#55748=CARTESIAN_POINT('Ctrl Pts',(-3.3181593418561,-3.95557434013013,-0.0123104525898624));
#55749=CARTESIAN_POINT('Ctrl Pts',(1.52017634683108,-4.93727721897207,0.146079147834249));
#55750=CARTESIAN_POINT('Ctrl Pts',(4.96501177239675,-1.41203703483287,0.304468748258361));
#55751=CARTESIAN_POINT('Ctrl Pts',(3.88934922870828,3.39617009289883,0.462858348682473));
#55752=CARTESIAN_POINT('Ctrl Pts',(-0.732920742143878,5.1113964007393,0.621247949106584));
#55753=CARTESIAN_POINT('Ctrl Pts',(-4.68612688169979,2.16748556327014,0.779637549530696));
#55754=CARTESIAN_POINT('Ctrl Pts',(-4.36939265644683,-2.75114092476471,
0.938027149954809));
#55755=CARTESIAN_POINT('Ctrl Pts',(-0.0704529116473286,-5.16289724783097,
1.09641675037892));
#55756=CARTESIAN_POINT('Ctrl Pts',(4.29252819085395,-2.86947836000301,1.25480635080303));
#55757=CARTESIAN_POINT('Ctrl Pts',(4.74374945851672,2.03886099295457,1.41319595122714));
#55758=CARTESIAN_POINT('Ctrl Pts',(0.87187597225223,5.08919664880298,1.57158555165126));
#55759=CARTESIAN_POINT('Ctrl Pts',(-3.79452777359949,3.50164966549009,1.72997515207536));
#55760=CARTESIAN_POINT('Ctrl Pts',(-5.00293367927747,-1.2769919878773,1.88836475249948));
#55761=CARTESIAN_POINT('Ctrl Pts',(-1.65208468153467,-4.89189754332655,
2.04675435292359));
#55762=CARTESIAN_POINT('Ctrl Pts',(3.20433051897175,-4.04874042926377,2.20514395334771));
#55763=CARTESIAN_POINT('Ctrl Pts',(5.14059300557593,0.484092964878372,2.36353355377181));
#55764=CARTESIAN_POINT('Ctrl Pts',(2.392155064142,4.57576601695794,2.52192315419593));
#55765=CARTESIAN_POINT('Ctrl Pts',(-2.53628918908134,4.49747442552335,2.68031275462004));
#55766=CARTESIAN_POINT('Ctrl Pts',(-5.15337531200808,0.320567159775624,
2.83870235504415));
#55767=CARTESIAN_POINT('Ctrl Pts',(-3.07411308423917,-4.14847788693502,
2.99709195546826));
#55768=CARTESIAN_POINT('Ctrl Pts',(1.80663443860224,-4.83695274769126,3.15548155589238));
#55769=CARTESIAN_POINT('Ctrl Pts',(5.04096893490742,-1.11744005069485,3.31387115631648));
#55770=CARTESIAN_POINT('Ctrl Pts',(3.68139281034196,3.62041254264275,3.4722607567406));
#55771=CARTESIAN_POINT('Ctrl Pts',(-1.03309179131411,5.05892887272037,3.63065035716471));
#55772=CARTESIAN_POINT('Ctrl Pts',(-4.80610435287845,1.88716744466989,3.78903995758882));
#55773=CARTESIAN_POINT('Ctrl Pts',(-4.19924192609147,-3.00439798462519,
3.94742955801293));
#55774=CARTESIAN_POINT('Ctrl Pts',(0.234452652827207,-5.15801046495039,
4.10581915843705));
#55775=CARTESIAN_POINT('Ctrl Pts',(4.4544870133001,-2.61105064195526,4.26420875886115));
#55776=CARTESIAN_POINT('Ctrl Pts',(4.61508054334482,2.31539879571022,4.42259835928526));
#55777=CARTESIAN_POINT('Ctrl Pts',(0.56988195080356,5.13179058096912,4.58098795970938));
#55778=CARTESIAN_POINT('Ctrl Pts',(-3.99465861152192,3.27150463588748,4.73937756013348));
#55779=CARTESIAN_POINT('Ctrl Pts',(-4.91880686345887,-1.5701525546756,4.89776716055761));
#55780=CARTESIAN_POINT('Ctrl Pts',(-1.36037264139205,-4.98090617072295,
5.05615676098171));
#55781=CARTESIAN_POINT('Ctrl Pts',(3.43778957362211,-3.85248528258675,5.21454636140584));
#55782=CARTESIAN_POINT('Ctrl Pts',(5.10304258525828,0.786763228710822,5.37293596182993));
#55783=CARTESIAN_POINT('Ctrl Pts',(2.11781634615703,4.70902260867037,5.53132556225406));
#55784=CARTESIAN_POINT('Ctrl Pts',(-2.79740769526454,4.33987905263503,5.68971516267816));
#55785=CARTESIAN_POINT('Ctrl Pts',(-5.16331214443354,0.0157386201644824,
5.84810476310228));
#55786=CARTESIAN_POINT('Ctrl Pts',(-2.82381278957536,-4.32274465293194,
6.00649436352639));
#55787=CARTESIAN_POINT('Ctrl Pts',(2.08906951604171,-4.72184588505036,6.16488396395049));
#55788=CARTESIAN_POINT('Ctrl Pts',(5.098151436811,-0.817858137064712,6.32327356437462));
#55789=CARTESIAN_POINT('Ctrl Pts',(3.46121148378334,3.83145599864432,6.48166316479871));
#55790=CARTESIAN_POINT('Ctrl Pts',(-1.32998241066,4.98910681308353,6.64005276522284));
#55791=CARTESIAN_POINT('Ctrl Pts',(-4.90914338527368,1.60010975493711,6.79844236564693));
#55792=CARTESIAN_POINT('Ctrl Pts',(-4.01452835847177,-3.24709132363831,
6.95683196607106));
#55793=CARTESIAN_POINT('Ctrl Pts',(0.538586577094185,-5.13516937442138,
7.11522156649516));
#55794=CARTESIAN_POINT('Ctrl Pts',(4.60087948645563,-2.34349054961462,7.27361116691928));
#55795=CARTESIAN_POINT('Ctrl Pts',(4.47032190918109,2.58384636410851,7.43200076734339));
#55796=CARTESIAN_POINT('Ctrl Pts',(0.26589292373178,5.15648532996368,7.59039036776751));
#55797=CARTESIAN_POINT('Ctrl Pts',(-4.18084827136001,3.02994187021587,7.74877996819161));
#55798=CARTESIAN_POINT('Ctrl Pts',(-4.81751972636668,-1.85783306329961,
7.90716956861574));
#55799=CARTESIAN_POINT('Ctrl Pts',(-1.06391319462353,-5.05253685976928,
8.06555916903983));
#55800=CARTESIAN_POINT('Ctrl Pts',(3.65925338948522,-3.64278803069328,8.22394876946396));
#55801=CARTESIAN_POINT('Ctrl Pts',(5.04768747299395,1.08668817054443,8.38233836988805));
#55802=CARTESIAN_POINT('Ctrl Pts',(1.83608824986349,4.82584914224785,8.54072797031219));
#55803=CARTESIAN_POINT('Ctrl Pts',(-3.04876573566835,4.1671414055724,8.69911757073628));
#55804=CARTESIAN_POINT('Ctrl Pts',(-5.15523377649819,-0.289144798800594,
8.8575071711604));
#55805=CARTESIAN_POINT('Ctrl Pts',(-2.56365995117077,-4.48192901101572,
9.01589677158451));
#55806=CARTESIAN_POINT('Ctrl Pts',(2.36421564112952,-4.59026408905411,9.17428637200862));
#55807=CARTESIAN_POINT('Ctrl Pts',(5.13754605775107,-0.515422651333577,
9.33267597243274));
#55808=CARTESIAN_POINT('Ctrl Pts',(3.22895369161553,4.02913117959985,9.49106557285684));
#55809=CARTESIAN_POINT('Ctrl Pts',(-1.62223260619563,4.90187733184103,9.64945517328097));
#55810=CARTESIAN_POINT('Ctrl Pts',(-4.99505399739544,1.30746914614654,9.80784477370506));
#55811=CARTESIAN_POINT('Ctrl Pts',(-3.81580775774175,-3.47845528374006,
9.96623437412919));
#55812=CARTESIAN_POINT('Ctrl Pts',(0.840841326532404,-5.09441123866306,
10.1246239745533));
#55813=CARTESIAN_POINT('Ctrl Pts',(4.73121909778617,-2.06775381846214,10.2830135749774));
#55814=CARTESIAN_POINT('Ctrl Pts',(4.30996593957687,2.84327867165857,10.4414031754015));
#55815=CARTESIAN_POINT('Ctrl Pts',(-0.0390238264566685,5.16318866070086,
10.5997927758256));
#55816=CARTESIAN_POINT('Ctrl Pts',(-4.35245059410458,2.77780737829316,10.7581823762498));
#55817=CARTESIAN_POINT('Ctrl Pts',(-4.69942385101101,-2.13903143351615,
10.9165719766738));
#55818=CARTESIAN_POINT('Ctrl Pts',(-0.763741663751577,-5.10653881568242,
11.074961577098));
#55819=CARTESIAN_POINT('Ctrl Pts',(3.86794975738412,-3.42038077988013,11.2333511775221));
#55820=CARTESIAN_POINT('Ctrl Pts',(4.97472054752429,1.38282156443299,11.3917407779462));
#55821=CARTESIAN_POINT('Ctrl Pts',(1.54795388466898,4.92583787552529,11.5501303783703));
#55822=CARTESIAN_POINT('Ctrl Pts',(-3.28948637173101,3.97986424582764,11.7085199787944));
#55823=CARTESIAN_POINT('Ctrl Pts',(-5.12916835710966,-0.593019366839089,
11.8669095792185));
#55824=CARTESIAN_POINT('Ctrl Pts',(-2.29456228398659,-4.62547553554524,
12.0252991796426));
#55825=CARTESIAN_POINT('Ctrl Pts',(2.63111281568934,-4.44266646915302,12.1836887800668));
#55826=CARTESIAN_POINT('Ctrl Pts',(5.15901534120123,-0.211188811899807,
12.3420783804909));
#55827=CARTESIAN_POINT('Ctrl Pts',(2.98542980392062,4.2127483773522,12.500467980915));
#55828=CARTESIAN_POINT('Ctrl Pts',(-1.90882269345658,4.79754478144462,12.6588575813391));
#55829=CARTESIAN_POINT('Ctrl Pts',(-5.0635364390099,1.01026666570772,12.8172471817632));
#55830=CARTESIAN_POINT('Ctrl Pts',(-3.60377347746801,-3.6976826159257,12.9756367821873));
#55831=CARTESIAN_POINT('Ctrl Pts',(1.14016230868481,-5.03587826648703,13.1340263826114));
#55832=CARTESIAN_POINT('Ctrl Pts',(4.84505108113381,-1.78480251743019,13.2924159830355));
#55833=CARTESIAN_POINT('Ctrl Pts',(4.13457213027864,3.09279053680373,13.4508055834596));
#55834=CARTESIAN_POINT('Ctrl Pts',(-0.343804419177731,5.15187718471428,
13.6091951838838));
#55835=CARTESIAN_POINT('Ctrl Pts',(-4.50886684456297,2.51598087890574,13.7675847843078));
#55836=CARTESIAN_POINT('Ctrl Pts',(-4.56493128400683,-2.41276654015816,
13.925974384732));
#55837=CARTESIAN_POINT('Ctrl Pts',(-0.460905372910369,-5.14272362102755,
14.0843639851561));
#55838=CARTESIAN_POINT('Ctrl Pts',(4.06315051784514,-3.18603952805496,14.2427535855802));
#55839=CARTESIAN_POINT('Ctrl Pts',(4.88439639669049,1.67413017563193,14.4011431860043));
#55840=CARTESIAN_POINT('Ctrl Pts',(1.25441857601452,5.00863993928383,14.5595327864284));
#55841=CARTESIAN_POINT('Ctrl Pts',(-3.51872970857736,3.7787009993846,14.7179223868525));
#55842=CARTESIAN_POINT('Ctrl Pts',(-5.08520683073047,-0.894824839523584,
14.8763119872766));
#55843=CARTESIAN_POINT('Ctrl Pts',(-2.01745869282129,-4.75288338056742,
15.0347015877008));
#55844=CARTESIAN_POINT('Ctrl Pts',(2.88882981271105,-4.27956800578602,15.1930911881249));
#55845=CARTESIAN_POINT('Ctrl Pts',(5.16248437889336,0.0937818828261288,
15.351480788549));
#55846=CARTESIAN_POINT('Ctrl Pts',(2.73148949656154,4.38166693681219,15.5098703889731));
#55847=CARTESIAN_POINT('Ctrl Pts',(-2.18875273549729,4.67647318514471,15.6682599893972));
#55848=CARTESIAN_POINT('Ctrl Pts',(-5.11435176830703,0.709539282194621,
15.8266495898213));
#55849=CARTESIAN_POINT('Ctrl Pts',(-3.37916532475269,-3.90400842437456,
15.9850391902454));
#55850=CARTESIAN_POINT('Ctrl Pts',(1.43550516966593,-4.9597746708902,16.1434287906695));
#55851=CARTESIAN_POINT('Ctrl Pts',(4.94197826197569,-1.49562391370258,16.3018183910937));
#55852=CARTESIAN_POINT('Ctrl Pts',(3.94475245484231,3.3315114408263,16.4602079915177));
#55853=CARTESIAN_POINT('Ctrl Pts',(-0.647385467154988,5.12259027405121,
16.6185975919419));
#55854=CARTESIAN_POINT('Ctrl Pts',(-4.64955123813058,2.24537608806315,16.776987192366));
#55855=CARTESIAN_POINT('Ctrl Pts',(-4.41451134820182,-2.67808364399215,
16.9353767927901));
#55856=CARTESIAN_POINT('Ctrl Pts',(-0.156460816144074,-5.16096436253732,
17.0937663932142));
#55857=CARTESIAN_POINT('Ctrl Pts',(4.24417435465306,-2.94058317628852,17.2521559936383));
#55858=CARTESIAN_POINT('Ctrl Pts',(4.7770306357801,1.95960002071087,17.4105455940624));
#55859=CARTESIAN_POINT('Ctrl Pts',(0.956505601666415,5.07396180892462,17.5689351944865));
#55860=CARTESIAN_POINT('Ctrl Pts',(-3.73569419127765,3.5643623764192,17.7273247949107));
#55861=CARTESIAN_POINT('Ctrl Pts',(-5.02350584303606,-1.19352508090609,
17.8857143953348));
#55862=CARTESIAN_POINT('Ctrl Pts',(-1.7333097832156,-4.86367572142824,18.0441039957589));
#55863=CARTESIAN_POINT('Ctrl Pts',(3.13645552043595,-4.10159948955856,18.202493596183));
#55864=CARTESIAN_POINT('Ctrl Pts',(5.14796384574126,0.398543369117654,18.3608831966071));
#55865=CARTESIAN_POINT('Ctrl Pts',(2.46797524199195,4.53507188733415,18.5192727970312));
#55866=CARTESIAN_POINT('Ctrl Pts',(-2.46096278237594,4.53951629179981,18.6776623974553));
#55867=CARTESIAN_POINT('Ctrl Pts',(-5.14748183280556,0.405511410062441,
18.8360519978794));
#55868=CARTESIAN_POINT('Ctrl Pts',(-3.14246278706502,-4.0951334678725,18.9944415983036));
#55869=CARTESIAN_POINT('Ctrl Pts',(1.72525842040716,-4.86940713488401,19.1528311987277));
#55870=CARTESIAN_POINT('Ctrl Pts',(5.02276837180745,-1.19521866677756,19.3112207991518));
#55871=CARTESIAN_POINT('Ctrl Pts',(3.95306672650205,2.75529758855723,19.4432121328385));
#55872=CARTESIAN_POINT('Ctrl Pts',(1.3947178009747,4.32991044428859,19.548805199788));
#55873=CARTESIAN_POINT('Ctrl Pts',(-0.0904913830656236,4.43080762341373,
19.6016017332627));
#55874=CARTESIAN_POINT('Ctrl Pts',(-0.803308159453631,4.29756675351939,
19.628));
#55875=CARTESIAN_POINT('Ctrl Pts',(-2.00237954638878,4.09906332620074,-0.219393102292058));
#55876=CARTESIAN_POINT('Ctrl Pts',(-2.6822715117666,3.76693823886074,-0.192994835554706));
#55877=CARTESIAN_POINT('Ctrl Pts',(-3.86326433094171,2.75793992993429,-0.140198302080001));
#55878=CARTESIAN_POINT('Ctrl Pts',(-5.02561840602911,-0.153231111990883,
-0.0346052351305939));
#55879=CARTESIAN_POINT('Ctrl Pts',(-3.46236114308042,-4.12747715912022,
0.0973860985561662));
#55880=CARTESIAN_POINT('Ctrl Pts',(1.58624073518831,-5.15184324632905,0.255775698980278));
#55881=CARTESIAN_POINT('Ctrl Pts',(5.18078309827857,-1.47340186480046,0.414165299404389));
#55882=CARTESIAN_POINT('Ctrl Pts',(4.0583740122066,3.54376211431939,0.572554899828502));
#55883=CARTESIAN_POINT('Ctrl Pts',(-0.764772284002811,5.33352936417491,
0.730944500252612));
#55884=CARTESIAN_POINT('Ctrl Pts',(-4.88977832440859,2.26168095600148,0.889334100676726));
#55885=CARTESIAN_POINT('Ctrl Pts',(-4.55927934554221,-2.87070102899737,
1.04772370110084));
#55886=CARTESIAN_POINT('Ctrl Pts',(-0.0735146804517841,-5.38726835420972,
1.20611330152495));
#55887=CARTESIAN_POINT('Ctrl Pts',(4.47907447545189,-2.9941812164533,1.36450290194906));
#55888=CARTESIAN_POINT('Ctrl Pts',(4.94990508457304,2.12746657133089,1.52289250237317));
#55889=CARTESIAN_POINT('Ctrl Pts',(0.909766282116828,5.31036484717274,1.68128210279728));
#55890=CARTESIAN_POINT('Ctrl Pts',(-3.95943177107978,3.65382565735724,1.8396717032214));
#55891=CARTESIAN_POINT('Ctrl Pts',(-5.2203530294748,-1.33248798003114,1.99806130364551));
#55892=CARTESIAN_POINT('Ctrl Pts',(-1.72388159129946,-5.10449144388282,
2.15645090406962));
#55893=CARTESIAN_POINT('Ctrl Pts',(3.34358550492888,-4.22469209476243,2.31484050449373));
#55894=CARTESIAN_POINT('Ctrl Pts',(5.36399480590974,0.505130856764646,2.47323010491784));
#55895=CARTESIAN_POINT('Ctrl Pts',(2.49611422749678,4.77462135621273,2.63161970534196));
#55896=CARTESIAN_POINT('Ctrl Pts',(-2.64651218677699,4.69292733971583,2.79000930576607));
#55897=CARTESIAN_POINT('Ctrl Pts',(-5.37733261056287,0.334498486481351,
2.94839890619018));
#55898=CARTESIAN_POINT('Ctrl Pts',(-3.20770903254784,-4.32876397991708,
3.10678850661429));
#55899=CARTESIAN_POINT('Ctrl Pts',(1.88514782911787,-5.04715883690933,3.2651781070384));
#55900=CARTESIAN_POINT('Ctrl Pts',(5.26004123537227,-1.16600217549634,3.42356770746252));
#55901=CARTESIAN_POINT('Ctrl Pts',(3.84138014656453,3.77774977574021,3.58195730788662));
#55902=CARTESIAN_POINT('Ctrl Pts',(-1.07798827812784,5.27878168283402,3.74034690831074));
#55903=CARTESIAN_POINT('Ctrl Pts',(-5.01496982109594,1.96918066847761,3.89873650873484));
#55904=CARTESIAN_POINT('Ctrl Pts',(-4.38173414154377,-3.1349642282388,4.05712610915897));
#55905=CARTESIAN_POINT('Ctrl Pts',(0.244641583302294,-5.38216919970349,
4.21551570958307));
#55906=CARTESIAN_POINT('Ctrl Pts',(4.64807176456428,-2.72452265064043,4.37390531000719));
#55907=CARTESIAN_POINT('Ctrl Pts',(4.81564442789093,2.41602225663996,4.53229491043129));
#55908=CARTESIAN_POINT('Ctrl Pts',(0.594648092306935,5.35480984226466,4.69068451085541));
#55909=CARTESIAN_POINT('Ctrl Pts',(-4.16825996929618,3.41367889956971,4.84907411127951));
#55910=CARTESIAN_POINT('Ctrl Pts',(-5.13257019924506,-1.63838882763724,
5.00746371170364));
#55911=CARTESIAN_POINT('Ctrl Pts',(-1.41949222095851,-5.19736824127129,
5.16585331212774));
#55912=CARTESIAN_POINT('Ctrl Pts',(3.58719030989569,-4.01990801902123,5.32424291255186));
#55913=CARTESIAN_POINT('Ctrl Pts',(5.32481250547765,0.820954677351021,5.48263251297596));
#55914=CARTESIAN_POINT('Ctrl Pts',(2.2098531956012,4.91366906238659,5.64102211340008));
#55915=CARTESIAN_POINT('Ctrl Pts',(-2.9189784779956,4.52848312857297,5.79941171382418));
#55916=CARTESIAN_POINT('Ctrl Pts',(-5.38770128154296,0.0164225949658002,
5.9578013142483));
#55917=CARTESIAN_POINT('Ctrl Pts',(-2.9465310947033,-4.51060409576292,6.11619091467242));
#55918=CARTESIAN_POINT('Ctrl Pts',(2.17985707506455,-4.92704961747478,6.27458051509652));
#55919=CARTESIAN_POINT('Ctrl Pts',(5.3197087956843,-0.853400919782555,6.43297011552065));
#55920=CARTESIAN_POINT('Ctrl Pts',(3.61163009812893,3.99796483664578,6.59135971594474));
#55921=CARTESIAN_POINT('Ctrl Pts',(-1.38778128029068,5.20592527019374,6.74974931636887));
#55922=CARTESIAN_POINT('Ctrl Pts',(-5.12248676203533,1.6696479190355,6.90813891679296));
#55923=CARTESIAN_POINT('Ctrl Pts',(-4.18899322308973,-3.38820462452834,
7.0665285172171));
#55924=CARTESIAN_POINT('Ctrl Pts',(0.561992672622043,-5.35833547257784,
7.22491811764118));
#55925=CARTESIAN_POINT('Ctrl Pts',(4.80082621619637,-2.44533483242041,7.38330771806533));
#55926=CARTESIAN_POINT('Ctrl Pts',(4.66459481923242,2.69613611918183,7.5416973184894));
#55927=CARTESIAN_POINT('Ctrl Pts',(0.27744819717852,5.38057778483401,7.70008691891355));
#55928=CARTESIAN_POINT('Ctrl Pts',(-4.36254112853255,3.16161820949792,7.85847651933763));
#55929=CARTESIAN_POINT('Ctrl Pts',(-5.02688128812553,-1.93857146266532,
8.01686611976177));
#55930=CARTESIAN_POINT('Ctrl Pts',(-1.11014912943107,-5.27211188340975,
8.17525572018585));
#55931=CARTESIAN_POINT('Ctrl Pts',(3.81827858253237,-3.80109766606194,8.33364532061));
#55932=CARTESIAN_POINT('Ctrl Pts',(5.26705175018262,1.13391386871537,8.49203492103408));
#55933=CARTESIAN_POINT('Ctrl Pts',(1.91588165504971,5.03557268685605,8.65042452145821));
#55934=CARTESIAN_POINT('Ctrl Pts',(-3.18126012948741,4.34823858468009,8.80881412188231));
#55935=CARTESIAN_POINT('Ctrl Pts',(-5.37927184089313,-0.301710560871043,
8.96720372230643));
#55936=CARTESIAN_POINT('Ctrl Pts',(-2.67507243761234,-4.67670634681008,
9.12559332273054));
#55937=CARTESIAN_POINT('Ctrl Pts',(2.46696060266074,-4.78974949091146,9.28398292315464));
#55938=CARTESIAN_POINT('Ctrl Pts',(5.36081544269451,-0.537822080371423,
9.44237252357877));
#55939=CARTESIAN_POINT('Ctrl Pts',(3.36927876055584,4.20423065904265,9.60076212400287));
#55940=CARTESIAN_POINT('Ctrl Pts',(-1.69273219338161,5.11490493775362,9.75915172442699));
#55941=CARTESIAN_POINT('Ctrl Pts',(-5.21213090945059,1.36428962596537,9.91754132485109));
#55942=CARTESIAN_POINT('Ctrl Pts',(-3.98163654867748,-3.62962328554942,
10.0759309252752));
#55943=CARTESIAN_POINT('Ctrl Pts',(0.877382921235304,-5.31580605461594,
10.2343205256993));
#55944=CARTESIAN_POINT('Ctrl Pts',(4.93683017477137,-2.15761503198178,10.3927101261234));
#55945=CARTESIAN_POINT('Ctrl Pts',(4.49727004033617,2.96684293232075,10.5510997265475));
#55946=CARTESIAN_POINT('Ctrl Pts',(-0.0407197384023858,5.38757243140836,
10.7094893269717));
#55947=CARTESIAN_POINT('Ctrl Pts',(-4.54160100876145,2.89852636316868,10.8678789273958));
#55948=CARTESIAN_POINT('Ctrl Pts',(-4.90365315835139,-2.23199025610718,
11.0262685278199));
#55949=CARTESIAN_POINT('Ctrl Pts',(-0.796932632670351,-5.32846067638225,
11.184658128244));
#55950=CARTESIAN_POINT('Ctrl Pts',(4.03604455470867,-3.56902495832874,11.3430477286681));
#55951=CARTESIAN_POINT('Ctrl Pts',(5.19091380096199,1.44291673763568,11.5014373290922));
#55952=CARTESIAN_POINT('Ctrl Pts',(1.6152254395837,5.13990676764554,11.6598269295163));
#55953=CARTESIAN_POINT('Ctrl Pts',(-3.43244209236889,4.15282266456216,11.8182165299404));
#55954=CARTESIAN_POINT('Ctrl Pts',(-5.3520736608267,-0.618791022762998,
11.9766061303646));
#55955=CARTESIAN_POINT('Ctrl Pts',(-2.39428022405006,-4.82649116952364,
12.1349957307887));
#55956=CARTESIAN_POINT('Ctrl Pts',(2.7454566937728,-4.63573751881888,12.2933853312128));
#55957=CARTESIAN_POINT('Ctrl Pts',(5.38321774623971,-0.22036673373445,12.4517749316369));
#55958=CARTESIAN_POINT('Ctrl Pts',(3.11517172129139,4.39582756118039,12.610164532061));
#55959=CARTESIAN_POINT('Ctrl Pts',(-1.99177701910997,5.00603826462726,12.7685541324851));
#55960=CARTESIAN_POINT('Ctrl Pts',(-5.28358948645086,1.05417120973438,12.9269437329092));
#55961=CARTESIAN_POINT('Ctrl Pts',(-3.76038760389046,-3.85837788057022,
13.0853333333334));
#55962=CARTESIAN_POINT('Ctrl Pts',(1.18971190581428,-5.25472933479274,13.2437229337574));
#55963=CARTESIAN_POINT('Ctrl Pts',(5.05560911073477,-1.862367128206,13.4021125341816));
#55964=CARTESIAN_POINT('Ctrl Pts',(4.3142539017226,3.22719817678374,13.5605021346057));
#55965=CARTESIAN_POINT('Ctrl Pts',(-0.358745599334103,5.37576937709664,
13.7188917350298));
#55966=CARTESIAN_POINT('Ctrl Pts',(-4.70481485473382,2.6253213105142,13.8772813354539));
#55967=CARTESIAN_POINT('Ctrl Pts',(-4.76331576341244,-2.51762144469383,
14.035670935878));
#55968=CARTESIAN_POINT('Ctrl Pts',(-0.480935569811807,-5.36621801443908,
14.1940605363021));
#55969=CARTESIAN_POINT('Ctrl Pts',(4.23972842232605,-3.32449961733459,14.3524501367262));
#55970=CARTESIAN_POINT('Ctrl Pts',(5.09666430962992,1.74688514666806,14.5108397371504));
#55971=CARTESIAN_POINT('Ctrl Pts',(1.30893356445067,5.22630727424813,14.6692293375744));
#55972=CARTESIAN_POINT('Ctrl Pts',(-3.67164797130143,3.94291719103216,14.8276189379986));
#55973=CARTESIAN_POINT('Ctrl Pts',(-5.30620163810439,-0.933712469786478,
14.9860085384227));
#55974=CARTESIAN_POINT('Ctrl Pts',(-2.10513416208848,-4.95943595200104,
15.1443981388468));
#55975=CARTESIAN_POINT('Ctrl Pts',(3.01437365178127,-4.46555106184718,15.3027877392709));
#55976=CARTESIAN_POINT('Ctrl Pts',(5.38683754266046,0.0978574907256861,
15.461177339695));
#55977=CARTESIAN_POINT('Ctrl Pts',(2.85019558172777,4.57208704614299,15.6195669401191));
#55978=CARTESIAN_POINT('Ctrl Pts',(-2.28387236489903,4.87970509392274,15.7779565405432));
#55979=CARTESIAN_POINT('Ctrl Pts',(-5.33661316720418,0.740374703881965,
15.9363461409674));
#55980=CARTESIAN_POINT('Ctrl Pts',(-3.5260183466427,-4.07367027264334,16.0947357413914));
#55981=CARTESIAN_POINT('Ctrl Pts',(1.49788988655441,-5.17531840086943,16.2531253418156));
#55982=CARTESIAN_POINT('Ctrl Pts',(5.15674858900573,-1.56062129330084,16.4115149422397));
#55983=CARTESIAN_POINT('Ctrl Pts',(4.11618497232175,3.47629350252734,16.5699045426638));
#55984=CARTESIAN_POINT('Ctrl Pts',(-0.675519785260975,5.34520970499122,
16.7282941430879));
#55985=CARTESIAN_POINT('Ctrl Pts',(-4.85161316293496,2.34295647615374,16.886683743512));
#55986=CARTESIAN_POINT('Ctrl Pts',(-4.60635882216303,-2.79446879777952,
17.0450733439361));
#55987=CARTESIAN_POINT('Ctrl Pts',(-0.16326034841019,-5.385251468869,17.2034629443603));
#55988=CARTESIAN_POINT('Ctrl Pts',(4.42861926027611,-3.06837613225715,17.3618525447843));
#55989=CARTESIAN_POINT('Ctrl Pts',(4.98463260760038,2.04476104631356,17.5202421452085));
#55990=CARTESIAN_POINT('Ctrl Pts',(0.998073777402168,5.29446792596388,17.6786317456326));
#55991=CARTESIAN_POINT('Ctrl Pts',(-3.89804137708339,3.71926376057284,17.8370213460567));
#55992=CARTESIAN_POINT('Ctrl Pts',(-5.24181922596764,-1.24539373721259,
17.9954109464808));
#55993=CARTESIAN_POINT('Ctrl Pts',(-1.8086366036207,-5.07504314756533,18.1538005469049));
#55994=CARTESIAN_POINT('Ctrl Pts',(3.27276076949422,-4.27984832373426,18.312190147329));
#55995=CARTESIAN_POINT('Ctrl Pts',(5.37168597078491,0.415863414893554,18.4705797477531));
#55996=CARTESIAN_POINT('Ctrl Pts',(2.57522942679949,4.73215872598774,18.6289693481773));
#55997=CARTESIAN_POINT('Ctrl Pts',(-2.56791221710864,4.73679627703356,18.7873589486013));
#55998=CARTESIAN_POINT('Ctrl Pts',(-5.371183010352,0.423134275550087,18.9457485490255));
#55999=CARTESIAN_POINT('Ctrl Pts',(-3.27902910214792,-4.27310129927592,
19.1041381494496));
#56000=CARTESIAN_POINT('Ctrl Pts',(1.80023534169657,-5.08102363891602,19.2625277498737));
#56001=CARTESIAN_POINT('Ctrl Pts',(5.24104970544042,-1.24716092356801,19.4209173502978));
#56002=CARTESIAN_POINT('Ctrl Pts',(4.12486056868766,2.87503833462901,19.5529086839846));
#56003=CARTESIAN_POINT('Ctrl Pts',(1.45532996524397,4.51808130074211,19.658501750934));
#56004=CARTESIAN_POINT('Ctrl Pts',(-0.0944239912043199,4.62336330695642,
19.7112982844087));
#56005=CARTESIAN_POINT('Ctrl Pts',(-0.838218623839749,4.48433200584526,
19.737696551146));
#56006=CARTESIAN_POINT('Ctrl Pts',(-2.08577545033744,4.26978275451687,-0.109696551146029));
#56007=CARTESIAN_POINT('Ctrl Pts',(-2.79398382812688,3.92382518874754,-0.0832982844086765));
#56008=CARTESIAN_POINT('Ctrl Pts',(-4.02416310842503,2.87280371482855,-0.0305017509339729));
#56009=CARTESIAN_POINT('Ctrl Pts',(-5.23492737076948,-0.159612942608633,
0.0750913160154349));
#56010=CARTESIAN_POINT('Ctrl Pts',(-3.60656294430474,-4.29937997811031,
0.207082649702195));
#56011=CARTESIAN_POINT('Ctrl Pts',(1.65230512354554,-5.36640927368603,0.365472250126306));
#56012=CARTESIAN_POINT('Ctrl Pts',(5.39655442416041,-1.53476669476806,0.523861850550419));
#56013=CARTESIAN_POINT('Ctrl Pts',(4.22739879570491,3.69135413573996,0.68225145097453));
#56014=CARTESIAN_POINT('Ctrl Pts',(-0.796623825861737,5.55566232761052,
0.840641051398642));
#56015=CARTESIAN_POINT('Ctrl Pts',(-5.09342976711741,2.35587634873282,0.999030651822753));
#56016=CARTESIAN_POINT('Ctrl Pts',(-4.74916603463757,-2.99026113323004,
1.15742025224687));
#56017=CARTESIAN_POINT('Ctrl Pts',(-0.0765764492562429,-5.61163946058846,
1.31580985267098));
#56018=CARTESIAN_POINT('Ctrl Pts',(4.66562076004983,-3.11888407290359,1.47419945309509));
#56019=CARTESIAN_POINT('Ctrl Pts',(5.15606071062936,2.21607214970721,1.6325890535192));
#56020=CARTESIAN_POINT('Ctrl Pts',(0.947656591981422,5.53153304554248,1.79097865394331));
#56021=CARTESIAN_POINT('Ctrl Pts',(-4.12433576856007,3.80600164922439,1.94936825436742));
#56022=CARTESIAN_POINT('Ctrl Pts',(-5.43777237967215,-1.38798397218498,
2.10775785479154));
#56023=CARTESIAN_POINT('Ctrl Pts',(-1.79567850106425,-5.31708534443909,
2.26614745521565));
#56024=CARTESIAN_POINT('Ctrl Pts',(3.482840490886,-4.4006437602611,2.42453705563976));
#56025=CARTESIAN_POINT('Ctrl Pts',(5.58739660624356,0.526168748650917,2.58292665606387));
#56026=CARTESIAN_POINT('Ctrl Pts',(2.60007339085155,4.97347669546753,2.74131625648798));
#56027=CARTESIAN_POINT('Ctrl Pts',(-2.75673518447264,4.88838025390829,2.8997058569121));
#56028=CARTESIAN_POINT('Ctrl Pts',(-5.60128990911765,0.348429813187091,
3.05809545733621));
#56029=CARTESIAN_POINT('Ctrl Pts',(-3.34130498085651,-4.50905007289915,
3.21648505776032));
#56030=CARTESIAN_POINT('Ctrl Pts',(1.9636612196335,-5.25736492612739,3.37487465818443));
#56031=CARTESIAN_POINT('Ctrl Pts',(5.47911353583714,-1.21456430029784,3.53326425860854));
#56032=CARTESIAN_POINT('Ctrl Pts',(4.00136748278709,3.93508700883766,3.69165385903265));
#56033=CARTESIAN_POINT('Ctrl Pts',(-1.12288476494156,5.49863449294768,3.85004345945677));
#56034=CARTESIAN_POINT('Ctrl Pts',(-5.22383528931343,2.05119389228533,4.00843305988088));
#56035=CARTESIAN_POINT('Ctrl Pts',(-4.56422635699607,-3.26553047185241,
4.16682266030499));
#56036=CARTESIAN_POINT('Ctrl Pts',(0.254830513777376,-5.6063279344566,4.3252122607291));
#56037=CARTESIAN_POINT('Ctrl Pts',(4.84165651582845,-2.8379946593256,4.48360186115322));
#56038=CARTESIAN_POINT('Ctrl Pts',(5.01620831243703,2.51664571756971,4.64199146157732));
#56039=CARTESIAN_POINT('Ctrl Pts',(0.619414233810315,5.57782910356021,4.80038106200144));
#56040=CARTESIAN_POINT('Ctrl Pts',(-4.34186132707045,3.55585316325194,4.95877066242554));
#56041=CARTESIAN_POINT('Ctrl Pts',(-5.34633353503125,-1.70662510059887,
5.11716026284966));
#56042=CARTESIAN_POINT('Ctrl Pts',(-1.47861180052498,-5.41383031181963,
5.27554986327377));
#56043=CARTESIAN_POINT('Ctrl Pts',(3.73659104616929,-4.18733075545571,5.43393946369789));
#56044=CARTESIAN_POINT('Ctrl Pts',(5.54658242569702,0.855146125991221,5.59232906412199));
#56045=CARTESIAN_POINT('Ctrl Pts',(2.30189004504538,5.11831551610282,5.75071866454611));
#56046=CARTESIAN_POINT('Ctrl Pts',(-3.04054926072666,4.71708720451092,5.90910826497022));
#56047=CARTESIAN_POINT('Ctrl Pts',(-5.61209041865238,0.0171065697671163,
6.06749786539433));
#56048=CARTESIAN_POINT('Ctrl Pts',(-3.06924939983126,-4.69846353859389,
6.22588746581845));
#56049=CARTESIAN_POINT('Ctrl Pts',(2.27064463408739,-5.13225334989921,6.38427706624255));
#56050=CARTESIAN_POINT('Ctrl Pts',(5.5412661545576,-0.888943702500394,6.54266666666667));
#56051=CARTESIAN_POINT('Ctrl Pts',(3.76204871247451,4.16447367464723,6.70105626709077));
#56052=CARTESIAN_POINT('Ctrl Pts',(-1.44558014992134,5.42274372730397,6.85944586751489));
#56053=CARTESIAN_POINT('Ctrl Pts',(-5.33583013879699,1.73918608313389,7.017835467939));
#56054=CARTESIAN_POINT('Ctrl Pts',(-4.36345808770768,-3.52931792541838,
7.17622506836312));
#56055=CARTESIAN_POINT('Ctrl Pts',(0.585398768149902,-5.58150157073431,
7.33461466878722));
#56056=CARTESIAN_POINT('Ctrl Pts',(5.00077294593711,-2.54717911522619,7.49300426921134));
#56057=CARTESIAN_POINT('Ctrl Pts',(4.85886772928377,2.80842587425515,7.65139386963545));
#56058=CARTESIAN_POINT('Ctrl Pts',(0.289003470625252,5.60467023970434,7.80978347005956));
#56059=CARTESIAN_POINT('Ctrl Pts',(-4.54423398570509,3.29329454877997,7.96817307048368));
#56060=CARTESIAN_POINT('Ctrl Pts',(-5.23624284988438,-2.01930986203101,
8.12656267090778));
#56061=CARTESIAN_POINT('Ctrl Pts',(-1.15638506423861,-5.49168690705022,
8.2849522713319));
#56062=CARTESIAN_POINT('Ctrl Pts',(3.97730377557951,-3.9594073014306,8.44334187175601));
#56063=CARTESIAN_POINT('Ctrl Pts',(5.48641602737129,1.1811395668863,8.60173147218012));
#56064=CARTESIAN_POINT('Ctrl Pts',(1.99567506023593,5.24529623146426,8.76012107260423));
#56065=CARTESIAN_POINT('Ctrl Pts',(-3.31375452330647,4.52933576378778,8.91851067302835));
#56066=CARTESIAN_POINT('Ctrl Pts',(-5.60330990528806,-0.314276322941499,
9.07690027345245));
#56067=CARTESIAN_POINT('Ctrl Pts',(-2.78648492405391,-4.87148368260443,
9.23528987387657));
#56068=CARTESIAN_POINT('Ctrl Pts',(2.56970556419197,-4.98923489276881,9.39367947430067));
#56069=CARTESIAN_POINT('Ctrl Pts',(5.58408482763794,-0.560221509409272,
9.5520690747248));
#56070=CARTESIAN_POINT('Ctrl Pts',(3.50960382949614,4.37933013848544,9.7104586751489));
#56071=CARTESIAN_POINT('Ctrl Pts',(-1.76323178056758,5.32793254366621,9.86884827557301));
#56072=CARTESIAN_POINT('Ctrl Pts',(-5.42920782150573,1.4211101057842,10.0272378759971));
#56073=CARTESIAN_POINT('Ctrl Pts',(-4.14746533961321,-3.78079128735878,
10.1856274764213));
#56074=CARTESIAN_POINT('Ctrl Pts',(0.913924515938199,-5.53720087056882,
10.3440170768453));
#56075=CARTESIAN_POINT('Ctrl Pts',(5.14244125175658,-2.24747624550143,10.5024066772695));
#56076=CARTESIAN_POINT('Ctrl Pts',(4.68457414109547,3.09040719298293,10.6607962776936));
#56077=CARTESIAN_POINT('Ctrl Pts',(-0.0424156503481004,5.61195620211585,
10.8191858781177));
#56078=CARTESIAN_POINT('Ctrl Pts',(-4.73075142341831,3.01924534804421,10.9775754785418));
#56079=CARTESIAN_POINT('Ctrl Pts',(-5.10788246569177,-2.32494907869821,
11.1359650789659));
#56080=CARTESIAN_POINT('Ctrl Pts',(-0.83012360158913,-5.55038253708208,
11.29435467939));
#56081=CARTESIAN_POINT('Ctrl Pts',(4.20413935203321,-3.71766913677734,11.4527442798141));
#56082=CARTESIAN_POINT('Ctrl Pts',(5.4071070543997,1.50301191083837,11.6111338802383));
#56083=CARTESIAN_POINT('Ctrl Pts',(1.68249699449844,5.35397565976581,11.7695234806624));
#56084=CARTESIAN_POINT('Ctrl Pts',(-3.57539781300678,4.32578108329668,11.9279130810865));
#56085=CARTESIAN_POINT('Ctrl Pts',(-5.57497896454372,-0.644562678686908,
12.0863026815106));
#56086=CARTESIAN_POINT('Ctrl Pts',(-2.49399816411355,-5.02750680350203,
12.2446922819347));
#56087=CARTESIAN_POINT('Ctrl Pts',(2.85980057185626,-4.82880856848474,12.4030818823588));
#56088=CARTESIAN_POINT('Ctrl Pts',(5.60742015127818,-0.229544655569092,
12.5614714827829));
#56089=CARTESIAN_POINT('Ctrl Pts',(3.24491363866216,4.57890674500859,12.719861083207));
#56090=CARTESIAN_POINT('Ctrl Pts',(-2.07473134476337,5.2145317478099,12.8782506836311));
#56091=CARTESIAN_POINT('Ctrl Pts',(-5.50364253389182,1.09807575376104,13.0366402840552));
#56092=CARTESIAN_POINT('Ctrl Pts',(-3.91700173031292,-4.01907314521474,
13.1950298844794));
#56093=CARTESIAN_POINT('Ctrl Pts',(1.23926150294374,-5.47358040309844,13.3534194849035));
#56094=CARTESIAN_POINT('Ctrl Pts',(5.26616714033573,-1.93993173898181,13.5118090853276));
#56095=CARTESIAN_POINT('Ctrl Pts',(4.49393567316656,3.36160581676376,13.6701986857517));
#56096=CARTESIAN_POINT('Ctrl Pts',(-0.37368677949048,5.59966156947901,13.8285882861758));
#56097=CARTESIAN_POINT('Ctrl Pts',(-4.90076286490465,2.73466174212266,13.9869778865999));
#56098=CARTESIAN_POINT('Ctrl Pts',(-4.96170024281806,-2.6224763492295,14.1453674870241));
#56099=CARTESIAN_POINT('Ctrl Pts',(-0.500965766713239,-5.58971240785062,
14.3037570874481));
#56100=CARTESIAN_POINT('Ctrl Pts',(4.41630632680696,-3.46295970661421,14.4621466878723));
#56101=CARTESIAN_POINT('Ctrl Pts',(5.30893222256936,1.81964011770419,14.6205362882964));
#56102=CARTESIAN_POINT('Ctrl Pts',(1.36344855288682,5.44397460921243,14.7789258887205));
#56103=CARTESIAN_POINT('Ctrl Pts',(-3.8245662340255,4.10713338267972,14.9373154891446));
#56104=CARTESIAN_POINT('Ctrl Pts',(-5.52719644547832,-0.972600100049373,
15.0957050895687));
#56105=CARTESIAN_POINT('Ctrl Pts',(-2.19280963135567,-5.16598852343466,
15.2540946899928));
#56106=CARTESIAN_POINT('Ctrl Pts',(3.1399174908515,-4.65153411790834,15.4124842904169));
#56107=CARTESIAN_POINT('Ctrl Pts',(5.61119070642755,0.101933098625243,15.570873890841));
#56108=CARTESIAN_POINT('Ctrl Pts',(2.96890166689401,4.76250715547379,15.7292634912652));
#56109=CARTESIAN_POINT('Ctrl Pts',(-2.37899199430077,5.08293700270077,15.8876530916893));
#56110=CARTESIAN_POINT('Ctrl Pts',(-5.55887456610132,0.77121012556931,16.0460426921134));
#56111=CARTESIAN_POINT('Ctrl Pts',(-3.6728713685327,-4.24333212091212,16.2044322925375));
#56112=CARTESIAN_POINT('Ctrl Pts',(1.56027460344289,-5.39086213084865,16.3628218929616));
#56113=CARTESIAN_POINT('Ctrl Pts',(5.37151891603578,-1.6256186728991,16.5212114933857));
#56114=CARTESIAN_POINT('Ctrl Pts',(4.28761748980119,3.62107556422837,16.6796010938098));
#56115=CARTESIAN_POINT('Ctrl Pts',(-0.703654103366955,5.56782913593124,
16.837990694234));
#56116=CARTESIAN_POINT('Ctrl Pts',(-5.05367508773934,2.44053686424434,16.996380294658));
#56117=CARTESIAN_POINT('Ctrl Pts',(-4.79820629612424,-2.91085395156691,
17.1547698950822));
#56118=CARTESIAN_POINT('Ctrl Pts',(-0.170059880676311,-5.60953857520067,
17.3131594955063));
#56119=CARTESIAN_POINT('Ctrl Pts',(4.61306416589918,-3.1961690882258,17.4715490959304));
#56120=CARTESIAN_POINT('Ctrl Pts',(5.19223457942065,2.12992207191625,17.6299386963545));
#56121=CARTESIAN_POINT('Ctrl Pts',(1.03964195313792,5.51497404300314,17.7883282967786));
#56122=CARTESIAN_POINT('Ctrl Pts',(-4.06038856288912,3.87416514472648,17.9467178972027));
#56123=CARTESIAN_POINT('Ctrl Pts',(-5.46013260889923,-1.2972623935191,18.1051074976268));
#56124=CARTESIAN_POINT('Ctrl Pts',(-1.88396342402579,-5.28641057370242,
18.263497098051));
#56125=CARTESIAN_POINT('Ctrl Pts',(3.40906601855249,-4.45809715790996,18.421886698475));
#56126=CARTESIAN_POINT('Ctrl Pts',(5.59540809582856,0.433183460669457,18.5802762988992));
#56127=CARTESIAN_POINT('Ctrl Pts',(2.68248361160703,4.92924556464132,18.7386658993233));
#56128=CARTESIAN_POINT('Ctrl Pts',(-2.67486165184133,4.93407626226733,18.8970554997474));
#56129=CARTESIAN_POINT('Ctrl Pts',(-5.59488418789844,0.440757141037727,
19.0554451001715));
#56130=CARTESIAN_POINT('Ctrl Pts',(-3.41559541723082,-4.45106913067933,
19.2138347005956));
#56131=CARTESIAN_POINT('Ctrl Pts',(1.87521226298597,-5.29264014294805,19.3722243010197));
#56132=CARTESIAN_POINT('Ctrl Pts',(5.4593310390734,-1.29910318035845,19.5306139014438));
#56133=CARTESIAN_POINT('Ctrl Pts',(4.29665441087326,2.99477908070078,19.6626052351306));
#56134=CARTESIAN_POINT('Ctrl Pts',(1.51594212951325,4.70625215719564,19.76819830208));
#56135=CARTESIAN_POINT('Ctrl Pts',(-0.098356599343019,4.8159189904991,19.8209948355547));
#56136=CARTESIAN_POINT('Ctrl Pts',(-0.873129088225867,4.67109725817113,
19.8473931022921));
#56137=CARTESIAN_POINT('Ctrl Pts',(-2.1691713542861,4.440502182833,2.77555756156289E-16));
#56138=CARTESIAN_POINT('Ctrl Pts',(-2.90569614448715,4.08071213863434,0.0263982667373523));
#56139=CARTESIAN_POINT('Ctrl Pts',(-4.18506188590834,2.9876674997228,0.079194800212056));
#56140=CARTESIAN_POINT('Ctrl Pts',(-5.44423633550983,-0.165994773226382,
0.184787867161464));
#56141=CARTESIAN_POINT('Ctrl Pts',(-3.75076474552906,-4.4712827971004,0.316779200848224));
#56142=CARTESIAN_POINT('Ctrl Pts',(1.71836951190277,-5.58097530104301,0.475168801272335));
#56143=CARTESIAN_POINT('Ctrl Pts',(5.61232575004223,-1.59613152473566,0.633558401696447));
#56144=CARTESIAN_POINT('Ctrl Pts',(4.39642357920323,3.83894615716052,0.79194800212056));
#56145=CARTESIAN_POINT('Ctrl Pts',(-0.828475367720669,5.77779529104613,
0.95033760254467));
#56146=CARTESIAN_POINT('Ctrl Pts',(-5.29708120982622,2.45007174146416,1.10872720296878));
#56147=CARTESIAN_POINT('Ctrl Pts',(-4.93905272373294,-3.10982123746271,
1.26711680339289));
#56148=CARTESIAN_POINT('Ctrl Pts',(-0.0796382180607007,-5.83601056696721,
1.42550640381701));
#56149=CARTESIAN_POINT('Ctrl Pts',(4.85216704464777,-3.24358692935388,1.58389600424112));
#56150=CARTESIAN_POINT('Ctrl Pts',(5.36221633668567,2.30467772808354,1.74228560466523));
#56151=CARTESIAN_POINT('Ctrl Pts',(0.985546901846022,5.75270124391223,1.90067520508934));
#56152=CARTESIAN_POINT('Ctrl Pts',(-4.28923976604036,3.95817764109155,2.05906480551345));
#56153=CARTESIAN_POINT('Ctrl Pts',(-5.65519172986948,-1.44347996433883,
2.21745440593756));
#56154=CARTESIAN_POINT('Ctrl Pts',(-1.86747541082905,-5.52967924499536,
2.37584400636168));
#56155=CARTESIAN_POINT('Ctrl Pts',(3.62209547684312,-4.57659542575977,2.53423360678579));
#56156=CARTESIAN_POINT('Ctrl Pts',(5.81079840657738,0.547206640537195,2.6926232072099));
#56157=CARTESIAN_POINT('Ctrl Pts',(2.70403255420632,5.17233203472232,2.85101280763401));
#56158=CARTESIAN_POINT('Ctrl Pts',(-2.86695818216828,5.08383316810077,3.00940240805812));
#56159=CARTESIAN_POINT('Ctrl Pts',(-5.82524720767244,0.362361139892822,
3.16779200848224));
#56160=CARTESIAN_POINT('Ctrl Pts',(-3.47490092916519,-4.68933616588121,
3.32618160890635));
#56161=CARTESIAN_POINT('Ctrl Pts',(2.04217461014913,-5.46757101534546,3.48457120933046));
#56162=CARTESIAN_POINT('Ctrl Pts',(5.698185836302,-1.26312642509933,3.64296080975457));
#56163=CARTESIAN_POINT('Ctrl Pts',(4.16135481900965,4.09242424193511,3.80135041017868));
#56164=CARTESIAN_POINT('Ctrl Pts',(-1.16778125175528,5.71848730306133,3.95974001060279));
#56165=CARTESIAN_POINT('Ctrl Pts',(-5.43270075753092,2.13320711609306,4.11812961102691));
#56166=CARTESIAN_POINT('Ctrl Pts',(-4.74671857244836,-3.39609671546603,
4.27651921145102));
#56167=CARTESIAN_POINT('Ctrl Pts',(0.265019444252462,-5.8304866692097,4.43490881187513));
#56168=CARTESIAN_POINT('Ctrl Pts',(5.03524126709262,-2.95146666801078,4.59329841229924));
#56169=CARTESIAN_POINT('Ctrl Pts',(5.21677219698313,2.61726917849946,4.75168801272335));
#56170=CARTESIAN_POINT('Ctrl Pts',(0.644180375313696,5.80084836485576,4.91007761314747));
#56171=CARTESIAN_POINT('Ctrl Pts',(-4.51546268484472,3.69802742693416,5.06846721357158));
#56172=CARTESIAN_POINT('Ctrl Pts',(-5.56009687081743,-1.77486137356051,
5.22685681399569));
#56173=CARTESIAN_POINT('Ctrl Pts',(-1.53773138009144,-5.63029238236797,
5.3852464144198));
#56174=CARTESIAN_POINT('Ctrl Pts',(3.88599178244287,-4.35475349189019,5.54363601484391));
#56175=CARTESIAN_POINT('Ctrl Pts',(5.7683523459164,0.889337574631424,5.70202561526803));
#56176=CARTESIAN_POINT('Ctrl Pts',(2.39392689448955,5.32296196981904,5.86041521569214));
#56177=CARTESIAN_POINT('Ctrl Pts',(-3.16212004345771,4.90569128044887,6.01880481611624));
#56178=CARTESIAN_POINT('Ctrl Pts',(-5.8364795557618,0.0177905445684291,
6.17719441654037));
#56179=CARTESIAN_POINT('Ctrl Pts',(-3.19196770495921,-4.88632298142486,
6.33558401696446));
#56180=CARTESIAN_POINT('Ctrl Pts',(2.36143219311022,-5.33745708232365,6.49397361738859));
#56181=CARTESIAN_POINT('Ctrl Pts',(5.7628235134309,-0.924486485218232,6.65236321781269));
#56182=CARTESIAN_POINT('Ctrl Pts',(3.9124673268201,4.33098251264868,6.81075281823681));
#56183=CARTESIAN_POINT('Ctrl Pts',(-1.50337901955202,5.63956218441419,6.96914241866092));
#56184=CARTESIAN_POINT('Ctrl Pts',(-5.54917351555865,1.80872424723227,7.12753201908502));
#56185=CARTESIAN_POINT('Ctrl Pts',(-4.53792295232564,-3.6704312263084,7.28592161950915));
#56186=CARTESIAN_POINT('Ctrl Pts',(0.60880486367776,-5.80466766889078,7.44431121993324));
#56187=CARTESIAN_POINT('Ctrl Pts',(5.20071967567786,-2.64902339803196,7.60270082035738));
#56188=CARTESIAN_POINT('Ctrl Pts',(5.0531406393351,2.92071562932846,7.76109042078146));
#56189=CARTESIAN_POINT('Ctrl Pts',(0.300558744071995,5.82876269457468,7.9194800212056));
#56190=CARTESIAN_POINT('Ctrl Pts',(-4.72592684287763,3.42497088806201,8.07786962162969));
#56191=CARTESIAN_POINT('Ctrl Pts',(-5.44560441164323,-2.10004826139671,
8.23625922205382));
#56192=CARTESIAN_POINT('Ctrl Pts',(-1.20262099904615,-5.7112619306907,8.39464882247792));
#56193=CARTESIAN_POINT('Ctrl Pts',(4.13632896862666,-4.11771693679927,8.55303842290205));
#56194=CARTESIAN_POINT('Ctrl Pts',(5.70578030455996,1.22836526505724,8.71142802332614));
#56195=CARTESIAN_POINT('Ctrl Pts',(2.07546846542215,5.45501977607246,8.86981762375027));
#56196=CARTESIAN_POINT('Ctrl Pts',(-3.44624891712552,4.71043294289546,9.02820722417436));
#56197=CARTESIAN_POINT('Ctrl Pts',(-5.827347969683,-0.32684208501195,9.18659682459849));
#56198=CARTESIAN_POINT('Ctrl Pts',(-2.89789741049547,-5.06626101839879,
9.3449864250226));
#56199=CARTESIAN_POINT('Ctrl Pts',(2.6724505257232,-5.18872029462616,9.50337602544671));
#56200=CARTESIAN_POINT('Ctrl Pts',(5.80735421258137,-0.582620938447121,
9.66176562587082));
#56201=CARTESIAN_POINT('Ctrl Pts',(3.64992889843646,4.55442961792825,9.82015522629493));
#56202=CARTESIAN_POINT('Ctrl Pts',(-1.83373136775356,5.54096014957879,9.97854482671904));
#56203=CARTESIAN_POINT('Ctrl Pts',(-5.64628473356088,1.47793058560304,10.1369344271431));
#56204=CARTESIAN_POINT('Ctrl Pts',(-4.31329413054894,-3.93195928916814,
10.2953240275673));
#56205=CARTESIAN_POINT('Ctrl Pts',(0.950466110641093,-5.7585956865217,10.4537136279914));
#56206=CARTESIAN_POINT('Ctrl Pts',(5.34805232874179,-2.33733745902108,10.6121032284155));
#56207=CARTESIAN_POINT('Ctrl Pts',(4.87187824185477,3.2139714536451,10.7704928288396));
#56208=CARTESIAN_POINT('Ctrl Pts',(-0.0441115622938141,5.83633997282335,
10.9288824292637));
#56209=CARTESIAN_POINT('Ctrl Pts',(-4.91990183807518,3.13996433291973,11.0872720296878));
#56210=CARTESIAN_POINT('Ctrl Pts',(-5.31211177303214,-2.41790790128923,
11.2456616301119));
#56211=CARTESIAN_POINT('Ctrl Pts',(-0.863314570507911,-5.77230439778191,
11.404051230536));
#56212=CARTESIAN_POINT('Ctrl Pts',(4.37223414935776,-3.86631331522594,11.5624408309602));
#56213=CARTESIAN_POINT('Ctrl Pts',(5.6233003078374,1.56310708404107,11.7208304313843));
#56214=CARTESIAN_POINT('Ctrl Pts',(1.74976854941316,5.56804455188607,11.8792200318084));
#56215=CARTESIAN_POINT('Ctrl Pts',(-3.71835353364465,4.4987395020312,12.0376096322325));
#56216=CARTESIAN_POINT('Ctrl Pts',(-5.79788426826075,-0.670334334610817,
12.1959992326566));
#56217=CARTESIAN_POINT('Ctrl Pts',(-2.59371610417703,-5.22852243748043,
12.3543888330807));
#56218=CARTESIAN_POINT('Ctrl Pts',(2.97414444993972,-5.0218796181506,12.5127784335049));
#56219=CARTESIAN_POINT('Ctrl Pts',(5.83162255631666,-0.238722577403733,
12.6711680339289));
#56220=CARTESIAN_POINT('Ctrl Pts',(3.37465555603293,4.76198592883678,12.8295576343531));
#56221=CARTESIAN_POINT('Ctrl Pts',(-2.15768567041678,5.42302523099255,12.9879472347772));
#56222=CARTESIAN_POINT('Ctrl Pts',(-5.72369558133277,1.1419802977877,13.1463368352013));
#56223=CARTESIAN_POINT('Ctrl Pts',(-4.07361585673539,-4.17976840985925,
13.3047264356254));
#56224=CARTESIAN_POINT('Ctrl Pts',(1.28881110007321,-5.69243147140415,13.4631160360495));
#56225=CARTESIAN_POINT('Ctrl Pts',(5.47672516993668,-2.01749634975762,13.6215056364736));
#56226=CARTESIAN_POINT('Ctrl Pts',(4.67361744461052,3.49601345674377,13.7798952368977));
#56227=CARTESIAN_POINT('Ctrl Pts',(-0.388627959646856,5.82355376186139,
13.9382848373218));
#56228=CARTESIAN_POINT('Ctrl Pts',(-5.09671087507549,2.84400217373111,14.096674437746));
#56229=CARTESIAN_POINT('Ctrl Pts',(-5.16008472222368,-2.72733125376517,
14.2550640381701));
#56230=CARTESIAN_POINT('Ctrl Pts',(-0.520995963614669,-5.81320680126216,
14.4134536385942));
#56231=CARTESIAN_POINT('Ctrl Pts',(4.59288423128786,-3.60141979589384,14.5718432390183));
#56232=CARTESIAN_POINT('Ctrl Pts',(5.5212001355088,1.89239508874033,14.7302328394424));
#56233=CARTESIAN_POINT('Ctrl Pts',(1.41796354132297,5.66164194417672,14.8886224398665));
#56234=CARTESIAN_POINT('Ctrl Pts',(-3.97748449674956,4.27134957432729,15.0470120402906));
#56235=CARTESIAN_POINT('Ctrl Pts',(-5.74819125285225,-1.01148773031227,
15.2054016407147));
#56236=CARTESIAN_POINT('Ctrl Pts',(-2.28048510062285,-5.37254109486827,
15.3637912411389));
#56237=CARTESIAN_POINT('Ctrl Pts',(3.26546132992172,-4.8375171739695,15.5221808415629));
#56238=CARTESIAN_POINT('Ctrl Pts',(5.83554387019465,0.106008706524804,15.6805704419871));
#56239=CARTESIAN_POINT('Ctrl Pts',(3.08760775206024,4.95292726480458,15.8389600424112));
#56240=CARTESIAN_POINT('Ctrl Pts',(-2.4741116237025,5.2861689114788,15.9973496428353));
#56241=CARTESIAN_POINT('Ctrl Pts',(-5.78113596499847,0.802045547256652,
16.1557392432594));
#56242=CARTESIAN_POINT('Ctrl Pts',(-3.81972439042269,-4.4129939691809,16.3141288436835));
#56243=CARTESIAN_POINT('Ctrl Pts',(1.62265932033137,-5.60640586082788,16.4725184441076));
#56244=CARTESIAN_POINT('Ctrl Pts',(5.58628924306583,-1.69061605249735,16.6309080445317));
#56245=CARTESIAN_POINT('Ctrl Pts',(4.45905000728063,3.76585762592941,16.7892976449558));
#56246=CARTESIAN_POINT('Ctrl Pts',(-0.731788421472935,5.79044856687125,
16.94768724538));
#56247=CARTESIAN_POINT('Ctrl Pts',(-5.25573701254373,2.53811725233494,17.106076845804));
#56248=CARTESIAN_POINT('Ctrl Pts',(-4.99005377008544,-3.02723910535429,
17.2644664462282));
#56249=CARTESIAN_POINT('Ctrl Pts',(-0.176859412942431,-5.83382568153235,
17.4228560466523));
#56250=CARTESIAN_POINT('Ctrl Pts',(4.79750907152224,-3.32396204419444,17.5812456470764));
#56251=CARTESIAN_POINT('Ctrl Pts',(5.39983655124094,2.21508309751895,17.7396352475005));
#56252=CARTESIAN_POINT('Ctrl Pts',(1.08121012887367,5.73548016004241,17.8980248479246));
#56253=CARTESIAN_POINT('Ctrl Pts',(-4.22273574869486,4.02906652888012,18.0564144483487));
#56254=CARTESIAN_POINT('Ctrl Pts',(-5.67844599183081,-1.34913104982561,
18.2148040487729));
#56255=CARTESIAN_POINT('Ctrl Pts',(-1.95929024443088,-5.4977779998395,18.373193649197));
#56256=CARTESIAN_POINT('Ctrl Pts',(3.54537126761076,-4.63634599208567,18.5315832496211));
#56257=CARTESIAN_POINT('Ctrl Pts',(5.81913022087222,0.450503506445362,18.6899728500452));
#56258=CARTESIAN_POINT('Ctrl Pts',(2.78973779641457,5.12633240329489,18.8483624504693));
#56259=CARTESIAN_POINT('Ctrl Pts',(-2.78181108657403,5.13135624750109,19.0067520508934));
#56260=CARTESIAN_POINT('Ctrl Pts',(-5.81858536544488,0.458380006525366,
19.1651416513175));
#56261=CARTESIAN_POINT('Ctrl Pts',(-3.55216173231372,-4.62903696208274,
19.3235312517416));
#56262=CARTESIAN_POINT('Ctrl Pts',(1.95018918427537,-5.50425664698007,19.4819208521657));
#56263=CARTESIAN_POINT('Ctrl Pts',(5.67761237270639,-1.3510454371489,19.6403104525899));
#56264=CARTESIAN_POINT('Ctrl Pts',(4.46844825305886,3.11451982677256,19.7723017862766));
#56265=CARTESIAN_POINT('Ctrl Pts',(1.57655429378253,4.89442301364916,19.877894853226));
#56266=CARTESIAN_POINT('Ctrl Pts',(-0.102289207481715,5.00847467404178,
19.9306913867007));
#56267=CARTESIAN_POINT('Ctrl Pts',(-0.908039552611985,4.857862510497,19.9570896534381));
#56268=CARTESIAN_POINT('Ctrl Pts',(-4.94192999916445,-0.00446510791632448,
18.1776795453431));
#56269=CARTESIAN_POINT('Ctrl Pts',(-4.94542698461402,-0.388624254474772,
18.1900543798197));
#56270=CARTESIAN_POINT('Ctrl Pts',(-4.90438878928145,-0.772044124408378,
18.2024292142963));
#56271=CARTESIAN_POINT('Ctrl Pts',(-4.81596832674149,-1.14420594504366,
18.2148040487729));
#56272=CARTESIAN_POINT('Ctrl Pts',(-4.43872740936416,-2.73201336649694,
18.2676005822476));
#56273=CARTESIAN_POINT('Ctrl Pts',(-3.19900882689749,-4.11489568316824,
18.3203971157223));
#56274=CARTESIAN_POINT('Ctrl Pts',(-1.66170595032388,-4.66276484021157,
18.373193649197));
#56275=CARTESIAN_POINT('Ctrl Pts',(-0.124403073750308,-5.21063399725488,
18.4259901826717));
#56276=CARTESIAN_POINT('Ctrl Pts',(1.71048409693019,-4.92348999467027,18.4787867161464));
#56277=CARTESIAN_POINT('Ctrl Pts',(3.00688750781402,-3.93210974362283,18.5315832496211));
#56278=CARTESIAN_POINT('Ctrl Pts',(4.3032909186979,-2.94072949257537,18.5843797830958));
#56279=CARTESIAN_POINT('Ctrl Pts',(5.06121056978506,-1.24511299306501,18.6371763165705));
#56280=CARTESIAN_POINT('Ctrl Pts',(4.93527165791903,0.38200007283176,18.6899728500452));
#56281=CARTESIAN_POINT('Ctrl Pts',(4.80933274605301,2.00911313872853,18.7427693835199));
#56282=CARTESIAN_POINT('Ctrl Pts',(3.79953527123378,3.56772277101172,18.7955659169946));
#56283=CARTESIAN_POINT('Ctrl Pts',(2.36604505332606,4.34786489452101,18.8483624504693));
#56284=CARTESIAN_POINT('Ctrl Pts',(0.932554835418334,5.1280070180303,18.901158983944));
#56285=CARTESIAN_POINT('Ctrl Pts',(-0.92462812557789,5.12968163276569,18.9539555174187));
#56286=CARTESIAN_POINT('Ctrl Pts',(-2.35934865255447,4.3516895666374,19.0067520508934));
#56287=CARTESIAN_POINT('Ctrl Pts',(-2.82356148188028,4.09996535176783,19.0238347005956));
#56288=CARTESIAN_POINT('Ctrl Pts',(-3.24354728379133,3.7666188744385,19.0409173502978));
#56289=CARTESIAN_POINT('Ctrl Pts',(-3.60367707498796,3.37571982724537,19.058));
#56290=CARTESIAN_POINT('Ctrl Pts',(-2.54467524200881,-3.56229978442281,
-6.93889390390723E-18));
#56291=CARTESIAN_POINT('Ctrl Pts',(-2.64087676169121,-3.50326719695733,
3.78010404015323E-18));
#56292=CARTESIAN_POINT('Ctrl Pts',(-2.73444512499906,-3.44042480726573,
1.70774935809012E-16));
#56293=CARTESIAN_POINT('Ctrl Pts',(-2.82511133337028,-3.37382080685403,
1.33573707650214E-16));
#56294=CARTESIAN_POINT('Ctrl Pts',(-2.93010592262241,-3.29669108243516,
6.34680042936623E-17));
#56295=CARTESIAN_POINT('Ctrl Pts',(-3.0312098993845,-3.21451805045997,-1.1579302301566E-16));
#56296=CARTESIAN_POINT('Ctrl Pts',(-3.12833116102487,-3.1277186925041,-1.87350135405495E-16));
#56297=CARTESIAN_POINT('Ctrl Pts',(-3.19203631412683,-3.07078402861756,
-2.34286889761188E-16));
#56298=CARTESIAN_POINT('Ctrl Pts',(-3.25402740755314,-3.01185787186213,
2.54730009275007E-16));
#56299=CARTESIAN_POINT('Ctrl Pts',(-3.3142718238098,-2.95104792020956,3.67761376907083E-16));
#56300=CARTESIAN_POINT('Ctrl Pts',(-3.34056115234898,-2.92451180455305,
4.17085761531429E-16));
#56301=CARTESIAN_POINT('Ctrl Pts',(-3.36651779652415,-2.8976168731598,-1.29958168485043E-16));
#56302=CARTESIAN_POINT('Ctrl Pts',(-3.39213869657566,-2.87037166754254,
-1.66533453693773E-16));
#56303=CARTESIAN_POINT('Ctrl Pts',(-3.4107075535189,-2.85062558819017,-1.9304154815313E-16));
#56304=CARTESIAN_POINT('Ctrl Pts',(-3.42910165503002,-2.83069359301782,
5.20445990861309E-16));
#56305=CARTESIAN_POINT('Ctrl Pts',(-3.44730402197008,-2.81059669044114,
5.13478148889135E-16));
#56306=CARTESIAN_POINT('Ctrl Pts',(-3.53659117665104,-2.71201636542733,
4.79299144256909E-16));
#56307=CARTESIAN_POINT('Ctrl Pts',(-3.62135066124632,-2.60938482813861,
1.69265913904123E-16));
#56308=CARTESIAN_POINT('Ctrl Pts',(-3.70148784592851,-2.50313357384095,
1.80411241501588E-16));
#56309=CARTESIAN_POINT('Ctrl Pts',(-3.78346559823418,-2.39444197154017,
1.91812551751929E-16));
#56310=CARTESIAN_POINT('Ctrl Pts',(-3.86060678067413,-2.28196193869908,
-1.60403205534396E-16));
#56311=CARTESIAN_POINT('Ctrl Pts',(-3.93277586934314,-2.16611326123794,
-5.55111512312578E-17));
#56312=CARTESIAN_POINT('Ctrl Pts',(-3.96434984563583,-2.1154294648487,-9.62087747363501E-18));
#56313=CARTESIAN_POINT('Ctrl Pts',(-3.99497165206884,-2.06410040223293,
2.30246512287273E-16));
#56314=CARTESIAN_POINT('Ctrl Pts',(-4.02462756948077,-2.01215919201488,
2.91433543964104E-16));
#56315=CARTESIAN_POINT('Ctrl Pts',(-4.03961656660672,-1.98590653424469,
3.22359319390632E-16));
#56316=CARTESIAN_POINT('Ctrl Pts',(-4.05435879396083,-1.95949747991113,
2.06007824657555E-17));
#56317=CARTESIAN_POINT('Ctrl Pts',(-4.06885232846184,-1.93293620549746,
1.38777878078145E-17));
#56318=CARTESIAN_POINT('Ctrl Pts',(-4.08041475408644,-1.91174656677398,
8.51442211522865E-18));
#56319=CARTESIAN_POINT('Ctrl Pts',(-4.09181979945551,-1.89045816584063,
2.1634594979841E-16));
#56320=CARTESIAN_POINT('Ctrl Pts',(-4.10305617212226,-1.86909315496197,
2.08166817117217E-16));
#56321=CARTESIAN_POINT('Ctrl Pts',(-4.16736596175704,-1.74681353716178,
1.61354708109947E-16));
#56322=CARTESIAN_POINT('Ctrl Pts',(-4.22623125974132,-1.62188769970873,
-1.58091925840003E-16));
#56323=CARTESIAN_POINT('Ctrl Pts',(-4.27954887166761,-1.49476314498018,
-1.66533453693773E-16));
#56324=CARTESIAN_POINT('Ctrl Pts',(-4.33347479304113,-1.36618820519452,
-1.75071292334113E-16));
#56325=CARTESIAN_POINT('Ctrl Pts',(-4.38172617240059,-1.23536340764327,
-1.43714543602008E-16));
#56326=CARTESIAN_POINT('Ctrl Pts',(-4.42415678995003,-1.10271583109255,
-9.71445146547012E-17));
#56327=CARTESIAN_POINT('Ctrl Pts',(-4.46710218965978,-0.968458930662989,
-5.00094828511621E-17));
#56328=CARTESIAN_POINT('Ctrl Pts',(-4.50408524649974,-0.832334009558243,
-1.01069852635313E-16));
#56329=CARTESIAN_POINT('Ctrl Pts',(-4.53490679318661,-0.694758137572736,
-1.38777878078145E-16));
#56330=CARTESIAN_POINT('Ctrl Pts',(-4.55802295320176,-0.591576233583606,
-1.67058897160268E-16));
#56331=CARTESIAN_POINT('Ctrl Pts',(-4.5776723273625,-0.487577560717138,
-2.48733805589575E-17));
#56332=CARTESIAN_POINT('Ctrl Pts',(-4.59375100179198,-0.38293266212137,
-5.55111512312578E-17));
#56333=CARTESIAN_POINT('Ctrl Pts',(-4.60074932415958,-0.337385453754768,
-6.88463920640666E-17));
#56334=CARTESIAN_POINT('Ctrl Pts',(-4.60707095895173,-0.291715781756126,
-3.50051711561292E-16));
#56335=CARTESIAN_POINT('Ctrl Pts',(-4.61270623945594,-0.245937595982269,
-3.60822483003176E-16));
#56336=CARTESIAN_POINT('Ctrl Pts',(-4.61510536794149,-0.226448282287078,
-3.65407962742523E-16));
#56337=CARTESIAN_POINT('Ctrl Pts',(-4.61738026973089,-0.206937176747096,
-2.11235974110856E-16));
#56338=CARTESIAN_POINT('Ctrl Pts',(-4.61952832377542,-0.187423425576886,
-2.22044604925031E-16));
#56339=CARTESIAN_POINT('Ctrl Pts',(-4.63503826526744,-0.0465251368621273,
-3.00087907403534E-16));
#56340=CARTESIAN_POINT('Ctrl Pts',(-4.64396392467283,0.0947008669712182,
-1.99183435512137E-16));
#56341=CARTESIAN_POINT('Ctrl Pts',(-4.64615947496329,0.235825173850752,
-2.22044604925031E-16));
#56342=CARTESIAN_POINT('Ctrl Pts',(-4.64786848339456,0.345675825581053,
-2.39839656782873E-16));
#56343=CARTESIAN_POINT('Ctrl Pts',(-4.64549890174975,0.455465549450203,
-1.5964104232527E-16));
#56344=CARTESIAN_POINT('Ctrl Pts',(-4.63896138884064,0.56499930567962,-1.38777878078145E-16));
#56345=CARTESIAN_POINT('Ctrl Pts',(-4.63077575597687,0.702146738831947,
-1.08813479195783E-16));
#56346=CARTESIAN_POINT('Ctrl Pts',(-4.61605776615402,0.838893185885087,
-2.45094142526848E-16));
#56347=CARTESIAN_POINT('Ctrl Pts',(-4.59507497843275,0.974861012835041,
-2.22044604925031E-16));
#56348=CARTESIAN_POINT('Ctrl Pts',(-4.57379787866946,1.11273597287572,-1.98671766312435E-16));
#56349=CARTESIAN_POINT('Ctrl Pts',(-4.54607882402517,1.24981106593623,-1.79874459778951E-16));
#56350=CARTESIAN_POINT('Ctrl Pts',(-4.51214338117474,1.38568894112939,-8.32667268468867E-17));
#56351=CARTESIAN_POINT('Ctrl Pts',(-4.50044605637916,1.43252515439685,-4.99666743073618E-17));
#56352=CARTESIAN_POINT('Ctrl Pts',(-4.48800969217396,1.47921903836149,8.24656052999656E-18));
#56353=CARTESIAN_POINT('Ctrl Pts',(-4.47484214689978,1.52575396812219,5.55111512312578E-17));
#56354=CARTESIAN_POINT('Ctrl Pts',(-4.46954654891505,1.54446894309507,7.45195742938095E-17));
#56355=CARTESIAN_POINT('Ctrl Pts',(-4.4641321445575,1.56316001192783,2.98076212871544E-17));
#56356=CARTESIAN_POINT('Ctrl Pts',(-4.45860111065483,1.58182037106622,2.77555756156289E-17));
#56357=CARTESIAN_POINT('Ctrl Pts',(-4.41871853179728,1.7163744631118,1.29589074421813E-17));
#56358=CARTESIAN_POINT('Ctrl Pts',(-4.37289155988743,1.84894716867807,-3.65495115057949E-16));
#56359=CARTESIAN_POINT('Ctrl Pts',(-4.32143318995775,1.97915634222774,-3.60822483003176E-16));
#56360=CARTESIAN_POINT('Ctrl Pts',(-4.26919198995651,2.11134637247354,-3.56078766751783E-16));
#56361=CARTESIAN_POINT('Ctrl Pts',(-4.21114654432903,2.24110115829447,1.76811505571791E-16));
#56362=CARTESIAN_POINT('Ctrl Pts',(-4.147570486657,2.36801906886784,1.66533453693773E-16));
#56363=CARTESIAN_POINT('Ctrl Pts',(-4.08343929176894,2.49604520883007,1.56165655308743E-16));
#56364=CARTESIAN_POINT('Ctrl Pts',(-4.01368020422711,2.62118552486071,-5.6466401912637E-17));
#56365=CARTESIAN_POINT('Ctrl Pts',(-3.93852341174026,2.7430141593252,-2.77555756156289E-17));
#56366=CARTESIAN_POINT('Ctrl Pts',(-3.9294168218154,2.75777587784009,-2.4276745388323E-17));
#56367=CARTESIAN_POINT('Ctrl Pts',(-3.9202309270139,2.77248895031151,-1.25624424874937E-18));
#56368=CARTESIAN_POINT('Ctrl Pts',(-3.91096608990011,2.78715259668566,0.));
#56369=CARTESIAN_POINT('Ctrl Pts',(-3.85692740501027,2.87268072373382,-4.76202655277902E-17));
#56370=CARTESIAN_POINT('Ctrl Pts',(-3.80020397437343,2.95652797095731,1.2876992925575E-16));
#56371=CARTESIAN_POINT('Ctrl Pts',(-3.74088150109056,3.03859647479229,1.66533453693773E-16));
#56372=CARTESIAN_POINT('Ctrl Pts',(-3.7149279190293,3.0745014452201,1.83054995635409E-16));
#56373=CARTESIAN_POINT('Ctrl Pts',(-3.68847672600951,3.11006585723381,-1.71465257258441E-16));
#56374=CARTESIAN_POINT('Ctrl Pts',(-3.66153447975748,3.14528103385681,-1.66533453693773E-16));
#56375=CARTESIAN_POINT('Ctrl Pts',(-3.64469680263863,3.16728891575776,-1.6345130103068E-16));
#56376=CARTESIAN_POINT('Ctrl Pts',(-3.62766732852701,3.18916039136048,2.64610714971295E-16));
#56377=CARTESIAN_POINT('Ctrl Pts',(-3.6104475878738,3.21089327815198,2.77555756156289E-16));
#56378=CARTESIAN_POINT('Ctrl Pts',(-3.59895112257703,3.22540286826887,2.86198291473495E-16));
#56379=CARTESIAN_POINT('Ctrl Pts',(-3.58737284218715,3.23984685581822,3.27202329850872E-16));
#56380=CARTESIAN_POINT('Ctrl Pts',(-3.57571845845413,3.25421848714644,3.33066907387547E-16));
#56381=CARTESIAN_POINT('Ctrl Pts',(-3.4847651283665,3.36637780487935,3.78835338283328E-16));
#56382=CARTESIAN_POINT('Ctrl Pts',(-3.38908875605728,3.4742480319481,-5.71170610872501E-17));
#56383=CARTESIAN_POINT('Ctrl Pts',(-3.28901395033307,3.5775964314093,-5.55111512312578E-17));
#56384=CARTESIAN_POINT('Ctrl Pts',(-3.1878935796381,3.68202459780562,-5.38884630954632E-17));
#56385=CARTESIAN_POINT('Ctrl Pts',(-3.08228201196636,3.78183656326097,2.20761671403476E-16));
#56386=CARTESIAN_POINT('Ctrl Pts',(-2.97246730240431,3.87676781486652,2.77555756156289E-16));
#56387=CARTESIAN_POINT('Ctrl Pts',(-2.86296602007246,3.97142811880605,3.34187742290929E-16));
#56388=CARTESIAN_POINT('Ctrl Pts',(-2.74928508452755,4.0612360937228,2.13145292818159E-16));
#56389=CARTESIAN_POINT('Ctrl Pts',(-2.63167026985783,4.14589663192155,2.22044604925031E-16));
#56390=CARTESIAN_POINT('Ctrl Pts',(-2.51583556938655,4.22927582281283,2.3080922488549E-16));
#56391=CARTESIAN_POINT('Ctrl Pts',(-2.39618466430397,4.30766267709754,-5.76377990669945E-17));
#56392=CARTESIAN_POINT('Ctrl Pts',(-2.27292097783335,4.38073587186789,-1.11022302462516E-16));
#56393=CARTESIAN_POINT('Ctrl Pts',(-2.23861641107446,4.40107230963037,-1.25879332241991E-16));
#56394=CARTESIAN_POINT('Ctrl Pts',(-2.2040318620339,4.42099693210222,2.77555756156289E-16));
#56395=CARTESIAN_POINT('Ctrl Pts',(-2.1691713542861,4.440502182833,2.77555756156289E-16));
#56396=CARTESIAN_POINT('Origin',(0.,0.,0.));
#56397=CARTESIAN_POINT('Origin',(-2.30940107675851,-4.,-10.));
#56398=CARTESIAN_POINT('',(-2.30940107675851,-4.,-10.));
#56399=CARTESIAN_POINT('',(2.3094010767585,-4.,-10.));
#56400=CARTESIAN_POINT('',(-1.15470053837925,-4.,-10.));
#56401=CARTESIAN_POINT('',(-2.30940107675851,-4.,-4.));
#56402=CARTESIAN_POINT('',(-2.30940107675851,-4.,-10.));
#56403=CARTESIAN_POINT('',(2.3094010767585,-4.,-4.));
#56404=CARTESIAN_POINT('',(-2.30940107675851,-4.,-4.));
#56405=CARTESIAN_POINT('',(2.3094010767585,-4.,-10.));
#56406=CARTESIAN_POINT('Origin',(-4.61880215351701,5.6564012731995E-16,
-10.));
#56407=CARTESIAN_POINT('',(-4.61880215351701,5.6564012731995E-16,-10.));
#56408=CARTESIAN_POINT('',(-4.04145188432738,-0.999999999999999,-10.));
#56409=CARTESIAN_POINT('',(-4.61880215351701,5.55111512312578E-16,-4.));
#56410=CARTESIAN_POINT('',(-4.61880215351701,5.6564012731995E-16,-10.));
#56411=CARTESIAN_POINT('',(-4.61880215351701,5.6564012731995E-16,-4.));
#56412=CARTESIAN_POINT('Origin',(-2.3094010767585,4.,-10.));
#56413=CARTESIAN_POINT('',(-2.3094010767585,4.,-10.));
#56414=CARTESIAN_POINT('',(-2.88675134594813,3.,-10.));
#56415=CARTESIAN_POINT('',(-2.3094010767585,4.,-4.));
#56416=CARTESIAN_POINT('',(-2.3094010767585,4.,-10.));
#56417=CARTESIAN_POINT('',(-2.3094010767585,4.,-4.));
#56418=CARTESIAN_POINT('Origin',(2.3094010767585,4.,-10.));
#56419=CARTESIAN_POINT('',(2.3094010767585,4.,-10.));
#56420=CARTESIAN_POINT('',(1.15470053837925,4.,-10.));
#56421=CARTESIAN_POINT('',(2.3094010767585,4.,-4.));
#56422=CARTESIAN_POINT('',(2.3094010767585,4.,-10.));
#56423=CARTESIAN_POINT('',(2.3094010767585,4.,-4.));
#56424=CARTESIAN_POINT('Origin',(4.61880215351701,0.,-10.));
#56425=CARTESIAN_POINT('',(4.61880215351701,0.,-10.));
#56426=CARTESIAN_POINT('',(4.04145188432738,1.,-10.));
#56427=CARTESIAN_POINT('',(4.61880215351701,0.,-4.));
#56428=CARTESIAN_POINT('',(4.61880215351701,0.,-10.));
#56429=CARTESIAN_POINT('',(4.61880215351701,0.,-4.));
#56430=CARTESIAN_POINT('Origin',(2.3094010767585,-4.,-10.));
#56431=CARTESIAN_POINT('',(2.88675134594813,-3.,-10.));
#56432=CARTESIAN_POINT('',(2.3094010767585,-4.,-4.));
#56433=CARTESIAN_POINT('Origin',(0.,0.,-4.));
#56434=CARTESIAN_POINT('Origin',(0.,0.,0.));
#56435=CARTESIAN_POINT('',(-8.,-9.79717439317883E-16,0.));
#56436=CARTESIAN_POINT('Origin',(0.,0.,0.));
#56437=CARTESIAN_POINT('Origin',(0.,0.,-10.));
#56438=CARTESIAN_POINT('',(-8.,-9.79717439317883E-16,-10.));
#56439=CARTESIAN_POINT('',(-8.,-9.79717439317883E-16,-10.));
#56440=CARTESIAN_POINT('Origin',(0.,0.,-10.));
#56441=CARTESIAN_POINT('Origin',(0.,0.,-10.));
#56442=CARTESIAN_POINT('Origin',(0.,0.,20.));
#97440=UNCERTAINTY_MEASURE_WITH_UNIT(LENGTH_MEASURE(0.01),#97476,
'DISTANCE_ACCURACY_VALUE',
'Maximum model space distance between geometric entities at asserted c
onnectivities');
#97452=UNCERTAINTY_MEASURE_WITH_UNIT(LENGTH_MEASURE(0.01),#97476,
'DISTANCE_ACCURACY_VALUE',
'Maximum model space distance between geometric entities at asserted c
onnectivities');
#97463=(
GEOMETRIC_REPRESENTATION_CONTEXT(3)
GLOBAL_UNCERTAINTY_ASSIGNED_CONTEXT((#97440))
GLOBAL_UNIT_ASSIGNED_CONTEXT((#97476,#97478,#97479))
REPRESENTATION_CONTEXT('','3D')
);
#97475=(
GEOMETRIC_REPRESENTATION_CONTEXT(3)
GLOBAL_UNCERTAINTY_ASSIGNED_CONTEXT((#97452))
GLOBAL_UNIT_ASSIGNED_CONTEXT((#97476,#97478,#97479))
REPRESENTATION_CONTEXT('','3D')
);
#97476=(
LENGTH_UNIT()
NAMED_UNIT(*)
SI_UNIT(.MILLI.,.METRE.)
);
#97478=(
NAMED_UNIT(*)
PLANE_ANGLE_UNIT()
SI_UNIT($,.RADIAN.)
);
#97479=(
NAMED_UNIT(*)
SI_UNIT($,.STERADIAN.)
SOLID_ANGLE_UNIT()
);
#97490=SHAPE_DEFINITION_REPRESENTATION(#97552,#97613);
#97552=PRODUCT_DEFINITION_SHAPE('',$,#97636);
#97613=SHAPE_REPRESENTATION('',(#22635),#97463);
#97625=PRODUCT_DEFINITION_CONTEXT('part definition',#97693,'design');
#97636=PRODUCT_DEFINITION('Socket head cap screw M10x20',
'Socket head cap screw M10x20',#97658,#97625);
#97658=PRODUCT_DEFINITION_FORMATION('',$,#97705);
#97693=APPLICATION_CONTEXT(
'Core Data for Automotive Mechanical Design Process');
#97694=PRODUCT_CONTEXT('part definition',#97693,'mechanical');
#97705=PRODUCT('Socket head cap screw M10x20',
'Socket head cap screw M10x20',$,(#97694));
#97720=PRESENTATION_STYLE_ASSIGNMENT((#97727));
#97727=SURFACE_STYLE_USAGE(.BOTH.,#97734);
#97734=SURFACE_SIDE_STYLE('',(#97741));
#97741=SURFACE_STYLE_FILL_AREA(#97748);
#97748=FILL_AREA_STYLE('Dark gray',(#97755));
#97755=FILL_AREA_STYLE_COLOUR('Dark gray',#97762);
#97762=COLOUR_RGB('Dark gray',0.250980392156863,0.282352941176471,0.32156862745098);
ENDSEC;
END-ISO-10303-21;
